ISO-10303-21;
HEADER;
/* Generated by software containing ST-Developer
 * from STEP Tools, Inc. (www.steptools.com) 
 */

FILE_DESCRIPTION(
/* description */ (''),
/* implementation_level */ '2;1');

FILE_NAME(
/* name */ '17_Faucet_Oil_Filler_Screw_M10x1.step',
/* time_stamp */ '2026-10-26T03:55:20-07:00',
/* author */ (''),
/* organization */ (''),
/* preprocessor_version */ 'ST-DEVELOPER v20.2',
/* originating_system */ 'Autodesk Translation Framework v15.15.0.0',
/* authorisation */ '');

FILE_SCHEMA (('AUTOMOTIVE_DESIGN { 1 0 10303 214 3 1 1 }'));
ENDSEC;

DATA;
#10=MECHANICAL_DESIGN_GEOMETRIC_PRESENTATION_REPRESENTATION('',(#185),#45236);
#131=(
BOUNDED_CURVE()
B_SPLINE_CURVE(2,(#38201,#38202,#38203),.UNSPECIFIED.,.F.,.F.)
B_SPLINE_CURVE_WITH_KNOTS((3,3),(0.,0.0727386053931439),.UNSPECIFIED.)
CURVE()
GEOMETRIC_REPRESENTATION_ITEM()
RATIONAL_B_SPLINE_CURVE((1.,1.,1.))
REPRESENTATION_ITEM('')
);
#132=(
BOUNDED_CURVE()
B_SPLINE_CURVE(2,(#38207,#38208,#38209),.UNSPECIFIED.,.F.,.F.)
B_SPLINE_CURVE_WITH_KNOTS((3,3),(0.,0.0727386053931439),.UNSPECIFIED.)
CURVE()
GEOMETRIC_REPRESENTATION_ITEM()
RATIONAL_B_SPLINE_CURVE((1.,1.,1.))
REPRESENTATION_ITEM('')
);
#133=(
BOUNDED_CURVE()
B_SPLINE_CURVE(2,(#38220,#38221,#38222),.UNSPECIFIED.,.F.,.F.)
B_SPLINE_CURVE_WITH_KNOTS((3,3),(0.,0.0727386053931439),.UNSPECIFIED.)
CURVE()
GEOMETRIC_REPRESENTATION_ITEM()
RATIONAL_B_SPLINE_CURVE((1.,1.,1.))
REPRESENTATION_ITEM('')
);
#134=(
BOUNDED_CURVE()
B_SPLINE_CURVE(2,(#38226,#38227,#38228),.UNSPECIFIED.,.F.,.F.)
B_SPLINE_CURVE_WITH_KNOTS((3,3),(0.,0.0727386053931439),.UNSPECIFIED.)
CURVE()
GEOMETRIC_REPRESENTATION_ITEM()
RATIONAL_B_SPLINE_CURVE((1.,1.,1.))
REPRESENTATION_ITEM('')
);
#145=SHAPE_REPRESENTATION_RELATIONSHIP('SRR','None',#45324,#165);
#165=ADVANCED_BREP_SHAPE_REPRESENTATION('',(#205),#45226);
#185=STYLED_ITEM('',(#45491),#205);
#205=MANIFOLD_SOLID_BREP('Body1',#16527);
#248=ELLIPSE('',#17373,9.89949493661173,7.);
#249=ELLIPSE('',#17374,9.89949493661173,7.);
#250=ELLIPSE('',#17378,9.89949493661173,7.);
#251=ELLIPSE('',#17379,9.89949493661173,7.);
#629=B_SPLINE_CURVE_WITH_KNOTS('',3,(#36664,#36665,#36666,#36667,#36668,
#36669,#36670,#36671,#36672,#36673,#36674,#36675,#36676,#36677,#36678,#36679),
 .UNSPECIFIED.,.F.,.F.,(4,3,3,3,3,4),(-4.09293042013086,-3.98050199480518,
-3.48293924545453,-2.98537649610388,-2.48781374675323,-2.06773127522693),
 .UNSPECIFIED.);
#630=B_SPLINE_CURVE_WITH_KNOTS('',3,(#36682,#36683,#36684,#36685,#36686,
#36687,#36688,#36689,#36690,#36691),.UNSPECIFIED.,.F.,.F.,(4,3,3,4),(0.,
0.497562749350642,0.995125498701295,1.11639350868636),.UNSPECIFIED.);
#631=B_SPLINE_CURVE_WITH_KNOTS('',3,(#36696,#36697,#36698,#36699,#36700,
#36701,#36702,#36703,#36704,#36705,#36706,#36707,#36708,#36709,#36710,#36711,
#36712,#36713,#36714,#36715,#36716,#36717,#36718,#36719,#36720,#36721,#36722,
#36723,#36724,#36725,#36726,#36727,#36728,#36729,#36730,#36731,#36732,#36733,
#36734,#36735),.UNSPECIFIED.,.F.,.F.,(4,3,3,3,3,3,3,3,3,3,3,3,3,4),(-10.3761157273103,
-9.95125498701294,-9.45369223766229,-8.95612948831165,-8.458566738961,-7.96100398961035,
-7.46344124025971,-6.96587849090906,-6.46831574155841,-5.97075299220777,
-5.47319024285712,-4.97562749350647,-4.47806474415583,-4.09293042013086),
 .UNSPECIFIED.);
#632=B_SPLINE_CURVE_WITH_KNOTS('',3,(#36736,#36737,#36738,#36739,#36740,
#36741,#36742,#36743,#36744,#36745,#36746,#36747,#36748,#36749,#36750,#36751,
#36752,#36753,#36754,#36755,#36756,#36757,#36758,#36759,#36760,#36761,#36762,
#36763,#36764,#36765,#36766,#36767,#36768,#36769,#36770,#36771,#36772,#36773,
#36774,#36775),.UNSPECIFIED.,.F.,.F.,(4,3,3,3,3,3,3,3,3,3,3,3,3,4),(1.11639350868636,
1.49268824805194,1.99025099740259,2.48781374675324,2.98537649610388,3.48293924545453,
3.98050199480518,4.47806474415582,4.97562749350647,5.47319024285711,5.97075299220776,
6.46831574155841,6.96587849090906,7.39957881586581),.UNSPECIFIED.);
#633=B_SPLINE_CURVE_WITH_KNOTS('',3,(#36780,#36781,#36782,#36783,#36784,
#36785,#36786,#36787,#36788,#36789,#36790,#36791,#36792,#36793,#36794,#36795,
#36796,#36797,#36798,#36799,#36800,#36801,#36802,#36803,#36804,#36805,#36806,
#36807,#36808,#36809,#36810,#36811,#36812,#36813,#36814,#36815,#36816,#36817,
#36818,#36819,#36820,#36821,#36822),.UNSPECIFIED.,.F.,.F.,(4,3,3,3,3,3,
3,3,3,3,3,3,3,3,4),(-16.65930103449,-16.4195707285714,-15.9220079792207,
-15.4244452298701,-14.9268824805194,-14.4293197311688,-13.9317569818181,
-13.4341942324675,-12.9366314831168,-12.4390687337662,-11.9415059844155,
-11.4439432350649,-10.9463804857142,-10.4488177363636,-10.3761157273103),
 .UNSPECIFIED.);
#634=B_SPLINE_CURVE_WITH_KNOTS('',3,(#36823,#36824,#36825,#36826,#36827,
#36828,#36829,#36830,#36831,#36832,#36833,#36834,#36835,#36836,#36837,#36838,
#36839,#36840,#36841,#36842,#36843,#36844,#36845,#36846,#36847,#36848,#36849,
#36850,#36851,#36852,#36853,#36854,#36855,#36856,#36857,#36858,#36859,#36860,
#36861,#36862,#36863,#36864,#36865),.UNSPECIFIED.,.F.,.F.,(4,3,3,3,3,3,
3,3,3,3,3,3,3,3,4),(7.39957881586581,7.4634412402597,7.96100398961035,8.45856673896099,
8.95612948831164,9.45369223766228,9.95125498701293,10.4488177363636,10.9463804857142,
11.4439432350649,11.9415059844155,12.4390687337662,12.9366314831168,13.4341942324675,
13.6827641230455),.UNSPECIFIED.);
#635=B_SPLINE_CURVE_WITH_KNOTS('',3,(#36870,#36871,#36872,#36873,#36874,
#36875,#36876,#36877,#36878,#36879,#36880,#36881,#36882,#36883,#36884,#36885,
#36886,#36887,#36888,#36889,#36890,#36891,#36892,#36893,#36894,#36895,#36896,
#36897,#36898,#36899,#36900,#36901,#36902,#36903,#36904,#36905,#36906,#36907,
#36908,#36909,#36910,#36911,#36912),.UNSPECIFIED.,.F.,.F.,(4,3,3,3,3,3,
3,3,3,3,3,3,3,3,4),(-22.9424863416697,-22.8878864701298,-22.3903237207791,
-21.8927609714285,-21.3951982220778,-20.8976354727272,-20.4000727233765,
-19.9025099740259,-19.4049472246752,-18.9073844753246,-18.4098217259739,
-17.9122589766233,-17.4146962272727,-16.917133477922,-16.65930103449),
 .UNSPECIFIED.);
#636=B_SPLINE_CURVE_WITH_KNOTS('',3,(#36913,#36914,#36915,#36916,#36917,
#36918,#36919,#36920,#36921,#36922,#36923,#36924,#36925,#36926,#36927,#36928,
#36929,#36930,#36931,#36932,#36933,#36934,#36935,#36936,#36937,#36938,#36939,
#36940,#36941,#36942,#36943,#36944,#36945,#36946,#36947,#36948,#36949,#36950,
#36951,#36952,#36953,#36954,#36955),.UNSPECIFIED.,.F.,.F.,(4,3,3,3,3,3,
3,3,3,3,3,3,3,3,4),(13.6827641230455,13.9317569818181,14.4293197311687,
14.9268824805194,15.42444522987,15.9220079792207,16.4195707285713,16.917133477922,
17.4146962272726,17.9122589766233,18.4098217259739,18.9073844753246,19.4049472246752,
19.9025099740259,19.9659494302252),.UNSPECIFIED.);
#637=B_SPLINE_CURVE_WITH_KNOTS('',3,(#36960,#36961,#36962,#36963,#36964,
#36965,#36966,#36967,#36968,#36969,#36970,#36971,#36972,#36973,#36974,#36975,
#36976,#36977,#36978,#36979,#36980,#36981,#36982,#36983,#36984,#36985,#36986,
#36987,#36988,#36989,#36990,#36991,#36992,#36993,#36994,#36995,#36996,#36997,
#36998,#36999),.UNSPECIFIED.,.F.,.F.,(4,3,3,3,3,3,3,3,3,3,3,3,3,4),(-29.2256716488491,
-28.8586394623375,-28.3610767129869,-27.8635139636362,-27.3659512142856,
-26.8683884649349,-26.3708257155843,-25.8732629662337,-25.375700216883,
-24.8781374675324,-24.3805747181817,-23.8830119688311,-23.3854492194804,
-22.9424863416697),.UNSPECIFIED.);
#638=B_SPLINE_CURVE_WITH_KNOTS('',3,(#37000,#37001,#37002,#37003,#37004,
#37005,#37006,#37007,#37008,#37009,#37010,#37011,#37012,#37013,#37014,#37015,
#37016,#37017,#37018,#37019,#37020,#37021,#37022,#37023,#37024,#37025,#37026,
#37027,#37028,#37029,#37030,#37031,#37032,#37033,#37034,#37035,#37036,#37037,
#37038,#37039),.UNSPECIFIED.,.F.,.F.,(4,3,3,3,3,3,3,3,3,3,3,3,3,4),(19.9659494302252,
20.4000727233765,20.8976354727272,21.3951982220778,21.8927609714285,22.3903237207791,
22.8878864701297,23.3854492194804,23.883011968831,24.3805747181817,24.8781374675323,
25.375700216883,25.8732629662336,26.2491347374046),.UNSPECIFIED.);
#639=B_SPLINE_CURVE_WITH_KNOTS('',3,(#37044,#37045,#37046,#37047,#37048,
#37049,#37050,#37051,#37052,#37053,#37054,#37055,#37056,#37057,#37058,#37059,
#37060,#37061,#37062,#37063,#37064,#37065,#37066,#37067,#37068,#37069,#37070,
#37071,#37072,#37073,#37074,#37075,#37076,#37077,#37078,#37079,#37080,#37081,
#37082,#37083,#37084,#37085,#37086),.UNSPECIFIED.,.F.,.F.,(4,3,3,3,3,3,
3,3,3,3,3,3,3,3,4),(-35.5088569560288,-35.3269552038959,-34.8293924545453,
-34.3318297051947,-33.834266955844,-33.3367042064934,-32.8391414571427,
-32.3415787077921,-31.8440159584414,-31.3464532090908,-30.8488904597401,
-30.3513277103895,-29.8537649610388,-29.3562022116882,-29.2256716488491),
 .UNSPECIFIED.);
#640=B_SPLINE_CURVE_WITH_KNOTS('',3,(#37087,#37088,#37089,#37090,#37091,
#37092,#37093,#37094,#37095,#37096,#37097,#37098,#37099,#37100,#37101,#37102,
#37103,#37104,#37105,#37106,#37107,#37108,#37109,#37110,#37111,#37112,#37113,
#37114,#37115,#37116,#37117,#37118,#37119,#37120,#37121,#37122,#37123,#37124,
#37125,#37126,#37127,#37128,#37129),.UNSPECIFIED.,.F.,.F.,(4,3,3,3,3,3,
3,3,3,3,3,3,3,3,4),(26.2491347374046,26.3708257155843,26.8683884649349,
27.3659512142856,27.8635139636362,28.3610767129869,28.8586394623375,29.3562022116881,
29.8537649610388,30.3513277103894,30.8488904597401,31.3464532090907,31.8440159584414,
32.341578707792,32.5323200445843),.UNSPECIFIED.);
#641=B_SPLINE_CURVE_WITH_KNOTS('',3,(#37134,#37135,#37136,#37137,#37138,
#37139,#37140,#37141,#37142,#37143,#37144,#37145,#37146,#37147,#37148,#37149,
#37150,#37151,#37152,#37153,#37154,#37155,#37156,#37157,#37158,#37159,#37160,
#37161,#37162,#37163,#37164,#37165,#37166,#37167,#37168,#37169,#37170,#37171,
#37172,#37173),.UNSPECIFIED.,.F.,.F.,(4,3,3,3,3,3,3,3,3,3,3,3,3,4),(-41.7920422632082,
-41.2977081961037,-40.8001454467531,-40.3025826974024,-39.8050199480518,
-39.3074571987011,-38.8098944493505,-38.3123316999998,-37.8147689506492,
-37.3172062012985,-36.8196434519479,-36.3220807025972,-35.8245179532466,
-35.5088569560288),.UNSPECIFIED.);
#642=B_SPLINE_CURVE_WITH_KNOTS('',3,(#37174,#37175,#37176,#37177,#37178,
#37179,#37180,#37181,#37182,#37183,#37184,#37185,#37186,#37187,#37188,#37189,
#37190,#37191,#37192,#37193,#37194,#37195,#37196,#37197,#37198,#37199,#37200,
#37201,#37202,#37203,#37204,#37205,#37206,#37207,#37208,#37209,#37210,#37211,
#37212,#37213,#37214,#37215,#37216),.UNSPECIFIED.,.F.,.F.,(4,3,3,3,3,3,
3,3,3,3,3,3,3,3,4),(32.5323200445843,32.8391414571427,33.3367042064933,
33.834266955844,34.3318297051946,34.8293924545453,35.3269552038959,35.8245179532466,
36.3220807025972,36.8196434519478,37.3172062012985,37.8147689506491,38.3123316999998,
38.8098944493504,38.815505351764),.UNSPECIFIED.);
#643=B_SPLINE_CURVE_WITH_KNOTS('',3,(#37221,#37222,#37223,#37224,#37225,
#37226,#37227,#37228,#37229,#37230,#37231,#37232,#37233,#37234,#37235,#37236,
#37237,#37238,#37239,#37240,#37241,#37242,#37243,#37244,#37245,#37246,#37247,
#37248,#37249,#37250,#37251,#37252,#37253,#37254,#37255,#37256,#37257,#37258,
#37259,#37260,#37261,#37262,#37263),.UNSPECIFIED.,.F.,.F.,(4,3,3,3,3,3,
3,3,3,3,3,3,3,3,4),(-48.0752275703879,-47.7660239376621,-47.2684611883115,
-46.7708984389608,-46.2733356896102,-45.7757729402595,-45.2782101909089,
-44.7806474415582,-44.2830846922076,-43.7855219428569,-43.2879591935063,
-42.7903964441556,-42.292833694805,-41.7952709454544,-41.7920422632082),
 .UNSPECIFIED.);
#644=B_SPLINE_CURVE_WITH_KNOTS('',3,(#37264,#37265,#37266,#37267,#37268,
#37269,#37270,#37271,#37272,#37273,#37274,#37275,#37276,#37277,#37278,#37279,
#37280,#37281,#37282,#37283,#37284,#37285,#37286,#37287,#37288,#37289,#37290,
#37291,#37292,#37293,#37294,#37295,#37296,#37297,#37298,#37299,#37300,#37301,
#37302,#37303),.UNSPECIFIED.,.F.,.F.,(4,3,3,3,3,3,3,3,3,3,3,3,3,4),(38.815505351764,
39.3074571987011,39.8050199480517,40.3025826974024,40.800145446753,41.2977081961037,
41.7952709454543,42.292833694805,42.7903964441556,43.2879591935063,43.7855219428569,
44.2830846922076,44.7806474415582,45.0986906589434),.UNSPECIFIED.);
#645=B_SPLINE_CURVE_WITH_KNOTS('',3,(#37308,#37309,#37310,#37311,#37312,
#37313,#37314,#37315,#37316,#37317,#37318,#37319,#37320,#37321,#37322,#37323,
#37324,#37325,#37326,#37327,#37328,#37329,#37330,#37331,#37332,#37333,#37334,
#37335,#37336,#37337,#37338,#37339,#37340,#37341,#37342,#37343,#37344,#37345,
#37346,#37347,#37348,#37349,#37350),.UNSPECIFIED.,.F.,.F.,(4,3,3,3,3,3,
3,3,3,3,3,3,3,3,4),(-54.3584128775676,-54.2343396792205,-53.7367769298699,
-53.2392141805192,-52.7416514311686,-52.2440886818179,-51.7465259324673,
-51.2489631831167,-50.751400433766,-50.2538376844154,-49.7562749350647,
-49.2587121857141,-48.7611494363634,-48.2635866870128,-48.0752275703879),
 .UNSPECIFIED.);
#646=B_SPLINE_CURVE_WITH_KNOTS('',3,(#37351,#37352,#37353,#37354,#37355,
#37356,#37357,#37358,#37359,#37360,#37361,#37362,#37363,#37364,#37365,#37366,
#37367,#37368,#37369,#37370,#37371,#37372,#37373,#37374,#37375,#37376,#37377,
#37378,#37379,#37380,#37381,#37382,#37383,#37384,#37385,#37386,#37387,#37388,
#37389,#37390,#37391,#37392,#37393),.UNSPECIFIED.,.F.,.F.,(4,3,3,3,3,3,
3,3,3,3,3,3,3,3,4),(45.0986906589434,45.2782101909088,45.7757729402595,
46.2733356896101,46.7708984389608,47.2684611883114,47.7660239376621,48.2635866870127,
48.7611494363634,49.258712185714,49.7562749350647,50.2538376844153,50.751400433766,
51.2489631831166,51.3818759661231),.UNSPECIFIED.);
#647=B_SPLINE_CURVE_WITH_KNOTS('',3,(#37398,#37399,#37400,#37401,#37402,
#37403,#37404,#37405,#37406,#37407,#37408,#37409,#37410,#37411,#37412,#37413,
#37414,#37415,#37416,#37417,#37418,#37419,#37420,#37421,#37422,#37423,#37424,
#37425,#37426,#37427,#37428,#37429,#37430,#37431,#37432,#37433,#37434,#37435,
#37436,#37437),.UNSPECIFIED.,.F.,.F.,(4,3,3,3,3,3,3,3,3,3,3,3,3,4),(-60.641598184747,
-60.2050926714283,-59.7075299220777,-59.209967172727,-58.7124044233764,
-58.2148416740257,-57.7172789246751,-57.2197161753244,-56.7221534259738,
-56.2245906766231,-55.7270279272725,-55.2294651779218,-54.7319024285712,
-54.3584128775676),.UNSPECIFIED.);
#648=B_SPLINE_CURVE_WITH_KNOTS('',3,(#37438,#37439,#37440,#37441,#37442,
#37443,#37444,#37445,#37446,#37447,#37448,#37449,#37450,#37451,#37452,#37453,
#37454,#37455,#37456,#37457,#37458,#37459,#37460,#37461,#37462,#37463,#37464,
#37465,#37466,#37467,#37468,#37469,#37470,#37471,#37472,#37473,#37474,#37475,
#37476,#37477),.UNSPECIFIED.,.F.,.F.,(4,3,3,3,3,3,3,3,3,3,3,3,3,4),(51.3818759661231,
51.7465259324672,52.2440886818179,52.7416514311685,53.2392141805192,53.7367769298698,
54.2343396792205,54.7319024285711,55.2294651779218,55.7270279272724,56.2245906766231,
56.7221534259737,57.2197161753244,57.6650612733025),.UNSPECIFIED.);
#649=B_SPLINE_CURVE_WITH_KNOTS('',3,(#37482,#37483,#37484,#37485,#37486,
#37487,#37488,#37489,#37490,#37491,#37492,#37493,#37494,#37495,#37496,#37497,
#37498,#37499,#37500,#37501,#37502,#37503,#37504,#37505,#37506,#37507,#37508,
#37509,#37510,#37511,#37512,#37513,#37514,#37515,#37516,#37517,#37518,#37519,
#37520,#37521,#37522,#37523,#37524),.UNSPECIFIED.,.F.,.F.,(4,3,3,3,3,3,
3,3,3,3,3,3,3,3,4),(-66.9247834919267,-66.6734084129867,-66.1758456636361,
-65.6782829142854,-65.1807201649348,-64.6831574155841,-64.1855946662335,
-63.6880319168828,-63.1904691675322,-62.6929064181815,-62.1953436688309,
-61.6977809194803,-61.2002181701296,-60.702655420779,-60.641598184747),
 .UNSPECIFIED.);
#650=B_SPLINE_CURVE_WITH_KNOTS('',3,(#37525,#37526,#37527,#37528,#37529,
#37530,#37531,#37532,#37533,#37534,#37535,#37536,#37537,#37538,#37539,#37540,
#37541,#37542,#37543,#37544,#37545,#37546,#37547,#37548,#37549,#37550,#37551,
#37552,#37553,#37554,#37555,#37556,#37557,#37558,#37559,#37560,#37561,#37562,
#37563,#37564,#37565,#37566,#37567),.UNSPECIFIED.,.F.,.F.,(4,3,3,3,3,3,
3,3,3,3,3,3,3,3,4),(57.6650612733025,57.717278924675,58.2148416740257,58.7124044233763,
59.2099671727269,59.7075299220776,60.2050926714282,60.7026554207789,61.2002181701295,
61.6977809194802,62.1953436688308,62.6929064181815,63.1904691675321,63.6880319168828,
63.9482465804822),.UNSPECIFIED.);
#651=B_SPLINE_CURVE_WITH_KNOTS('',3,(#37572,#37573,#37574,#37575,#37576,
#37577,#37578,#37579,#37580,#37581,#37582,#37583,#37584,#37585,#37586,#37587,
#37588,#37589,#37590,#37591,#37592,#37593,#37594,#37595,#37596,#37597,#37598,
#37599,#37600,#37601,#37602,#37603,#37604,#37605,#37606,#37607,#37608,#37609,
#37610,#37611,#37612,#37613,#37614),.UNSPECIFIED.,.F.,.F.,(4,3,3,3,3,3,
3,3,3,3,3,3,3,3,4),(-73.2079687991064,-73.1417241545451,-72.6441614051945,
-72.1465986558438,-71.6490359064932,-71.1514731571425,-70.6539104077919,
-70.1563476584412,-69.6587849090906,-69.1612221597399,-68.6636594103893,
-68.1660966610387,-67.668533911688,-67.1709711623374,-66.9247834919267),
 .UNSPECIFIED.);
#652=B_SPLINE_CURVE_WITH_KNOTS('',3,(#37615,#37616,#37617,#37618,#37619,
#37620,#37621,#37622,#37623,#37624,#37625,#37626,#37627,#37628,#37629,#37630,
#37631,#37632,#37633,#37634,#37635,#37636,#37637,#37638,#37639,#37640,#37641,
#37642,#37643,#37644,#37645,#37646,#37647,#37648,#37649,#37650,#37651,#37652,
#37653,#37654,#37655,#37656,#37657),.UNSPECIFIED.,.F.,.F.,(4,3,3,3,3,3,
3,3,3,3,3,3,3,3,4),(63.9482465804822,64.1855946662334,64.6831574155841,
65.1807201649347,65.6782829142853,66.175845663636,66.6734084129866,67.1709711623373,
67.6685339116879,68.1660966610386,68.6636594103892,69.1612221597399,69.6587849090905,
70.1563476584412,70.2314318876619),.UNSPECIFIED.);
#653=B_SPLINE_CURVE_WITH_KNOTS('',3,(#37662,#37663,#37664,#37665,#37666,
#37667,#37668,#37669,#37670,#37671,#37672,#37673,#37674,#37675,#37676,#37677,
#37678,#37679,#37680,#37681,#37682,#37683,#37684,#37685,#37686,#37687,#37688,
#37689,#37690,#37691,#37692,#37693,#37694,#37695,#37696,#37697,#37698,#37699,
#37700,#37701),.UNSPECIFIED.,.F.,.F.,(4,3,3,3,3,3,3,3,3,3,3,3,3,4),(-79.4911541062858,
-79.1124771467529,-78.6149143974022,-78.1173516480516,-77.6197888987009,
-77.1222261493503,-76.6246633999996,-76.127100650649,-75.6295379012984,
-75.1319751519477,-74.6344124025971,-74.1368496532464,-73.6392869038958,
-73.2079687991064),.UNSPECIFIED.);
#654=B_SPLINE_CURVE_WITH_KNOTS('',3,(#37702,#37703,#37704,#37705,#37706,
#37707,#37708,#37709,#37710,#37711,#37712,#37713,#37714,#37715,#37716,#37717,
#37718,#37719,#37720,#37721,#37722,#37723,#37724,#37725,#37726,#37727,#37728,
#37729,#37730,#37731,#37732,#37733,#37734,#37735,#37736,#37737,#37738,#37739,
#37740,#37741),.UNSPECIFIED.,.F.,.F.,(4,3,3,3,3,3,3,3,3,3,3,3,3,4),(70.2314318876619,
70.6539104077918,71.1514731571425,71.6490359064931,72.1465986558438,72.6441614051944,
73.141724154545,73.6392869038957,74.1368496532463,74.634412402597,75.1319751519476,
75.6295379012983,76.1271006506489,76.5146171948413),.UNSPECIFIED.);
#655=B_SPLINE_CURVE_WITH_KNOTS('',3,(#37747,#37748,#37749,#37750),
 .UNSPECIFIED.,.F.,.F.,(4,4),(91.1061869541039,91.1475924660972),
 .UNSPECIFIED.);
#656=B_SPLINE_CURVE_WITH_KNOTS('',3,(#37756,#37757,#37758,#37759,#37760,
#37761,#37762,#37763,#37764,#37765,#37766,#37767,#37768,#37769,#37770,#37771),
 .UNSPECIFIED.,.F.,.F.,(4,1,1,1,1,1,1,1,1,1,1,1,1,4),(84.8230016469245,
85.2543197517139,85.7518825010645,86.2494452504152,86.7470079997658,87.2445707491165,
87.7421334984671,88.2396962478177,88.7372589971684,89.234821746519,89.7323844958697,
90.2299472452203,90.727509994571,91.1061869541039),.UNSPECIFIED.);
#657=B_SPLINE_CURVE_WITH_KNOTS('',3,(#37774,#37775,#37776,#37777,#37778,
#37779,#37780,#37781,#37782,#37783,#37784,#37785,#37786,#37787),
 .UNSPECIFIED.,.F.,.F.,(4,1,1,1,1,1,1,1,1,1,1,4),(84.8230016469245,84.9330478520825,
85.4306106014332,85.9281733507838,86.4257361001345,86.9232988494851,87.4208615988357,
87.9184243481864,88.415987097537,88.9135498468877,89.4111125962383,89.908675345589),
 .UNSPECIFIED.);
#658=B_SPLINE_CURVE_WITH_KNOTS('',3,(#37792,#37793,#37794,#37795,#37796,
#37797,#37798,#37799,#37800,#37801,#37802,#37803,#37804,#37805,#37806,#37807,
#37808),.UNSPECIFIED.,.F.,.F.,(4,1,1,1,1,1,1,1,1,1,1,1,1,1,4),(78.5398163397448,
78.7860040101555,79.2835667595061,79.7811295088568,80.2786922582074,80.776255007558,
81.2738177569087,81.7713805062593,82.26894325561,82.7665060049606,83.2640687543113,
83.7616315036619,84.2591942530126,84.7567570023632,84.8230016469245),
 .UNSPECIFIED.);
#659=B_SPLINE_CURVE_WITH_KNOTS('',3,(#37809,#37810,#37811,#37812,#37813,
#37814,#37815,#37816,#37817,#37818,#37819,#37820,#37821,#37822,#37823,#37824),
 .UNSPECIFIED.,.F.,.F.,(4,1,1,1,1,1,1,1,1,1,1,1,1,4),(78.5398163397448,
78.9622948598747,79.4598576092254,79.957420358576,80.4549831079267,80.9525458572773,
81.450108606628,81.9476713559786,82.4452341053293,82.9427968546799,83.4403596040306,
83.9379223533812,84.4354851027319,84.8230016469245),.UNSPECIFIED.);
#660=B_SPLINE_CURVE_WITH_KNOTS('',3,(#37829,#37830,#37831,#37832,#37833,
#37834,#37835,#37836,#37837,#37838,#37839,#37840,#37841,#37842,#37843,#37844,
#37845),.UNSPECIFIED.,.F.,.F.,(4,1,1,1,1,1,1,1,1,1,1,1,1,1,4),(72.2566310325652,
72.317688268597,72.8152510179477,73.3128137672983,73.810376516649,74.3079392659996,
74.8055020153503,75.3030647647009,75.8006275140516,76.2981902634022,76.7957530127529,
77.2933157621035,77.7908785114542,78.2884412608048,78.5398163397448),
 .UNSPECIFIED.);
#661=B_SPLINE_CURVE_WITH_KNOTS('',3,(#37846,#37847,#37848,#37849,#37850,
#37851,#37852,#37853,#37854,#37855,#37856,#37857,#37858,#37859,#37860,#37861,
#37862),.UNSPECIFIED.,.F.,.F.,(4,1,1,1,1,1,1,1,1,1,1,1,1,1,4),(72.2566310325651,
72.4939791183163,72.991541867667,73.4891046170176,73.9866673663683,74.4842301157189,
74.9817928650696,75.4793556144202,75.9769183637709,76.4744811131215,76.9720438624722,
77.4696066118228,77.9671693611735,78.4647321105241,78.5398163397448),
 .UNSPECIFIED.);
#662=B_SPLINE_CURVE_WITH_KNOTS('',3,(#37867,#37868,#37869,#37870,#37871,
#37872,#37873,#37874,#37875,#37876,#37877,#37878,#37879,#37880,#37881,#37882),
 .UNSPECIFIED.,.F.,.F.,(4,1,1,1,1,1,1,1,1,1,1,1,1,4),(65.9734457253857,
66.3469352763893,66.8444980257399,67.3420607750906,67.8396235244412,68.3371862737919,
68.8347490231425,69.3323117724932,69.8298745218438,70.3274372711945,70.8250000205451,
71.3225627698958,71.8201255192464,72.2566310325652),.UNSPECIFIED.);
#663=B_SPLINE_CURVE_WITH_KNOTS('',3,(#37883,#37884,#37885,#37886,#37887,
#37888,#37889,#37890,#37891,#37892,#37893,#37894,#37895,#37896,#37897,#37898,
#37899),.UNSPECIFIED.,.F.,.F.,(4,1,1,1,1,1,1,1,1,1,1,1,1,1,4),(65.9734457253857,
66.0256633767579,66.5232261261086,67.0207888754592,67.5183516248099,68.0159143741605,
68.5134771235112,69.0110398728618,69.5086026222125,70.0061653715631,70.5037281209138,
71.0012908702644,71.498853619615,71.9964163689657,72.2566310325651),
 .UNSPECIFIED.);
#664=B_SPLINE_CURVE_WITH_KNOTS('',3,(#37904,#37905,#37906,#37907,#37908,
#37909,#37910,#37911,#37912,#37913,#37914,#37915,#37916,#37917,#37918,#37919,
#37920),.UNSPECIFIED.,.F.,.F.,(4,1,1,1,1,1,1,1,1,1,1,1,1,1,4),(59.690260418206,
59.8786195348309,60.3761822841815,60.8737450335322,61.3713077828828,61.8688705322335,
62.3664332815841,62.8639960309348,63.3615587802854,63.859121529636,64.3566842789867,
64.8542470283373,65.351809777688,65.8493725270386,65.9734457253857),
 .UNSPECIFIED.);
#665=B_SPLINE_CURVE_WITH_KNOTS('',3,(#37921,#37922,#37923,#37924,#37925,
#37926,#37927,#37928,#37929,#37930,#37931,#37932,#37933,#37934,#37935,#37936),
 .UNSPECIFIED.,.F.,.F.,(4,1,1,1,1,1,1,1,1,1,1,1,1,4),(59.690260418206,60.0549103845502,
60.5524731339008,61.0500358832515,61.5475986326021,62.0451613819528,62.5427241313034,
63.0402868806541,63.5378496300047,64.0354123793553,64.532975128706,65.0305378780566,
65.5281006274073,65.9734457253857),.UNSPECIFIED.);
#666=B_SPLINE_CURVE_WITH_KNOTS('',3,(#37941,#37942,#37943,#37944,#37945,
#37946,#37947,#37948,#37949,#37950,#37951,#37952,#37953,#37954,#37955,#37956,
#37957),.UNSPECIFIED.,.F.,.F.,(4,1,1,1,1,1,1,1,1,1,1,1,1,1,4),(53.4070751110263,
53.4103037932725,53.9078665426231,54.4054292919737,54.9029920413244,55.400554790675,
55.8981175400257,56.3956802893763,56.893243038727,57.3908057880776,57.8883685374283,
58.3859312867789,58.8834940361296,59.3810567854802,59.690260418206),
 .UNSPECIFIED.);
#667=B_SPLINE_CURVE_WITH_KNOTS('',3,(#37958,#37959,#37960,#37961,#37962,
#37963,#37964,#37965,#37966,#37967,#37968,#37969,#37970,#37971,#37972,#37973,
#37974),.UNSPECIFIED.,.F.,.F.,(4,1,1,1,1,1,1,1,1,1,1,1,1,1,4),(53.4070751110263,
53.5865946429918,54.0841573923424,54.5817201416931,55.0792828910437,55.5768456403944,
56.074408389745,56.5719711390957,57.0695338884463,57.5670966377969,58.0646593871476,
58.5622221364982,59.0597848858489,59.5573476351995,59.690260418206),
 .UNSPECIFIED.);
#668=B_SPLINE_CURVE_WITH_KNOTS('',3,(#37979,#37980,#37981,#37982,#37983,
#37984,#37985,#37986,#37987,#37988,#37989,#37990,#37991,#37992,#37993,#37994),
 .UNSPECIFIED.,.F.,.F.,(4,1,1,1,1,1,1,1,1,1,1,1,1,4),(47.1238898038469,
47.4395508010647,47.9371135504153,48.434676299766,48.9322390491166,49.4298017984673,
49.9273645478179,50.4249272971686,50.9224900465192,51.4200527958699,51.9176155452205,
52.4151782945712,52.9127410439218,53.4070751110263),.UNSPECIFIED.);
#669=B_SPLINE_CURVE_WITH_KNOTS('',3,(#37995,#37996,#37997,#37998,#37999,
#38000,#38001,#38002,#38003,#38004,#38005,#38006,#38007,#38008,#38009,#38010),
 .UNSPECIFIED.,.F.,.F.,(4,1,1,1,1,1,1,1,1,1,1,1,1,4),(47.1238898038469,
47.615841650784,48.1134044001347,48.6109671494853,49.108529898836,49.6060926481866,
50.1036553975372,50.6012181468879,51.0987808962385,51.5963436455892,52.0939063949398,
52.5914691442905,53.0890318936411,53.4070751110263),.UNSPECIFIED.);
#670=B_SPLINE_CURVE_WITH_KNOTS('',3,(#38015,#38016,#38017,#38018,#38019,
#38020,#38021,#38022,#38023,#38024,#38025,#38026,#38027,#38028,#38029,#38030,
#38031),.UNSPECIFIED.,.F.,.F.,(4,1,1,1,1,1,1,1,1,1,1,1,1,1,4),(40.8407044966672,
40.9712350595063,41.4687978088569,41.9663605582076,42.4639233075582,42.9614860569089,
43.4590488062595,43.9566115556102,44.4541743049608,44.9517370543115,45.4492998036621,
45.9468625530127,46.4444253023634,46.941988051714,47.1238898038469),
 .UNSPECIFIED.);
#671=B_SPLINE_CURVE_WITH_KNOTS('',3,(#38032,#38033,#38034,#38035,#38036,
#38037,#38038,#38039,#38040,#38041,#38042,#38043,#38044,#38045,#38046,#38047,
#38048),.UNSPECIFIED.,.F.,.F.,(4,1,1,1,1,1,1,1,1,1,1,1,1,1,4),(40.8407044966672,
41.1475259092256,41.6450886585762,42.1426514079269,42.6402141572775,43.1377769066282,
43.6353396559788,44.1329024053295,44.6304651546801,45.1280279040308,45.6255906533814,
46.1231534027321,46.6207161520827,47.1182789014334,47.1238898038469),
 .UNSPECIFIED.);
#672=B_SPLINE_CURVE_WITH_KNOTS('',3,(#38053,#38054,#38055,#38056,#38057,
#38058,#38059,#38060,#38061,#38062,#38063,#38064,#38065,#38066,#38067,#38068),
 .UNSPECIFIED.,.F.,.F.,(4,1,1,1,1,1,1,1,1,1,1,1,1,4),(34.5575191894878,
35.0004820672985,35.4980448166492,35.9956075659998,36.4931703153505,36.9907330647011,
37.4882958140517,37.9858585634024,38.483421312753,38.9809840621037,39.4785468114543,
39.976109560805,40.4736723101556,40.8407044966672),.UNSPECIFIED.);
#673=B_SPLINE_CURVE_WITH_KNOTS('',3,(#38069,#38070,#38071,#38072,#38073,
#38074,#38075,#38076,#38077,#38078,#38079,#38080,#38081,#38082,#38083,#38084,
#38085),.UNSPECIFIED.,.F.,.F.,(4,1,1,1,1,1,1,1,1,1,1,1,1,1,4),(34.5575191894878,
34.6792101676672,35.1767729170178,35.6743356663685,36.1718984157191,36.6694611650698,
37.1670239144204,37.6645866637711,38.1621494131217,38.6597121624724,39.157274911823,
39.6548376611737,40.1524004105243,40.649963159875,40.8407044966672),
 .UNSPECIFIED.);
#674=B_SPLINE_CURVE_WITH_KNOTS('',3,(#38090,#38091,#38092,#38093,#38094,
#38095,#38096,#38097,#38098,#38099,#38100,#38101,#38102,#38103,#38104,#38105,
#38106),.UNSPECIFIED.,.F.,.F.,(4,1,1,1,1,1,1,1,1,1,1,1,1,1,4),(28.2743338823081,
28.5321663257401,29.0297290750907,29.5272918244414,30.024854573792,30.5224173231427,
31.0199800724933,31.517542821844,32.0151055711946,32.5126683205453,33.0102310698959,
33.5077938192466,34.0053565685972,34.5029193179479,34.5575191894878),
 .UNSPECIFIED.);
#675=B_SPLINE_CURVE_WITH_KNOTS('',3,(#38107,#38108,#38109,#38110,#38111,
#38112,#38113,#38114,#38115,#38116,#38117,#38118,#38119,#38120,#38121,#38122),
 .UNSPECIFIED.,.F.,.F.,(4,1,1,1,1,1,1,1,1,1,1,1,1,4),(28.2743338823081,
28.7084571754594,29.2060199248101,29.7035826741607,30.2011454235114,30.698708172862,
31.1962709222127,31.6938336715633,32.191396420914,32.6889591702646,33.1865219196153,
33.6840846689659,34.1816474183166,34.5575191894878),.UNSPECIFIED.);
#676=B_SPLINE_CURVE_WITH_KNOTS('',3,(#38127,#38128,#38129,#38130,#38131,
#38132,#38133,#38134,#38135,#38136,#38137,#38138,#38139,#38140,#38141,#38142,
#38143),.UNSPECIFIED.,.F.,.F.,(4,1,1,1,1,1,1,1,1,1,1,1,1,1,4),(21.9911485751284,
22.0638505841817,22.5614133335323,23.058976082883,23.5565388322336,24.0541015815843,
24.5516643309349,25.0492270802856,25.5467898296362,26.0443525789869,26.5419153283375,
27.0394780776882,27.5370408270388,28.0346035763895,28.2743338823081),
 .UNSPECIFIED.);
#677=B_SPLINE_CURVE_WITH_KNOTS('',3,(#38144,#38145,#38146,#38147,#38148,
#38149,#38150,#38151,#38152,#38153,#38154,#38155,#38156,#38157,#38158,#38159,
#38160),.UNSPECIFIED.,.F.,.F.,(4,1,1,1,1,1,1,1,1,1,1,1,1,1,4),(21.9911485751284,
22.240141433901,22.7377041832517,23.2352669326023,23.732829681953,24.2303924313036,
24.7279551806543,25.2255179300049,25.7230806793556,26.2206434287062,26.7182061780569,
27.2157689274075,27.7133316767581,28.2108944261088,28.2743338823081),
 .UNSPECIFIED.);
#678=B_SPLINE_CURVE_WITH_KNOTS('',3,(#38165,#38166,#38167,#38168,#38169,
#38170,#38171,#38172,#38173,#38174,#38175,#38176,#38177,#38178,#38179,#38180),
 .UNSPECIFIED.,.F.,.F.,(4,1,1,1,1,1,1,1,1,1,1,1,1,4),(15.707963267949,16.0930975919739,
16.5906603413246,17.0882230906752,17.5857858400259,18.0833485893765,18.5809113387272,
19.0784740880778,19.5760368374285,20.0735995867791,20.5711623361297,21.0687250854804,
21.566287834831,21.9911485751284),.UNSPECIFIED.);
#679=B_SPLINE_CURVE_WITH_KNOTS('',3,(#38181,#38182,#38183,#38184,#38185,
#38186,#38187,#38188,#38189,#38190,#38191,#38192,#38193,#38194,#38195,#38196,
#38197),.UNSPECIFIED.,.F.,.F.,(4,1,1,1,1,1,1,1,1,1,1,1,1,1,4),(15.707963267949,
15.7718256923426,16.2693884416933,16.7669511910439,17.2645139403946,17.7620766897452,
18.2596394390959,18.7572021884465,19.2547649377972,19.7523276871478,20.2498904364984,
20.7474531858491,21.2450159351997,21.7425786845504,21.9911485751284),
 .UNSPECIFIED.);
#680=B_SPLINE_CURVE_WITH_KNOTS('',3,(#39121,#39122,#39123,#39124,#39125,
#39126,#39127,#39128,#39129,#39130,#39131,#39132,#39133,#39134,#39135,#39136,
#39137,#39138,#39139,#39140,#39141,#39142,#39143,#39144,#39145,#39146,#39147,
#39148,#39149,#39150,#39151,#39152,#39153,#39154,#39155,#39156,#39157,#39158,
#39159,#39160,#39161,#39162,#39163,#39164,#39165,#39166,#39167,#39168,#39169,
#39170,#39171,#39172,#39173,#39174,#39175,#39176,#39177,#39178,#39179,#39180,
#39181,#39182,#39183,#39184,#39185,#39186,#39187,#39188,#39189,#39190,#39191,
#39192,#39193,#39194,#39195,#39196,#39197,#39198,#39199,#39200,#39201,#39202,
#39203,#39204,#39205,#39206,#39207,#39208,#39209,#39210,#39211,#39212,#39213,
#39214,#39215,#39216,#39217,#39218,#39219,#39220),.UNSPECIFIED.,.F.,.F.,
(4,3,3,3,3,3,3,3,3,3,3,3,3,3,3,3,3,3,3,3,3,3,3,3,3,3,3,3,3,3,3,3,3,4),(-0.965990216419489,
-0.927769800274492,-0.884036457391411,-0.859296340292785,-0.841593944822978,
-0.834687190942105,-0.791436271578584,-0.748447260876285,-0.715784640354957,
-0.71037803066556,-0.686115520602401,-0.643612953198282,-0.600900815509313,
-0.56335340930662,-0.5351928546546,-0.529195526613789,-0.487304945489095,
-0.450711190698541,-0.408716440645001,-0.366944220009338,-0.350749948869511,
-0.345333544484853,-0.304097381748682,-0.263026243379112,-0.221955105009542,
-0.19421071688335,-0.181344115531761,-0.173002718621388,-0.167235292303527,
-0.125426469227645,-0.0849353464330531,-0.0447936733152677,-0.00549740928954664,
0.),.UNSPECIFIED.);
#681=B_SPLINE_CURVE_WITH_KNOTS('',3,(#39221,#39222,#39223,#39224,#39225,
#39226,#39227,#39228,#39229,#39230,#39231,#39232,#39233,#39234,#39235,#39236,
#39237,#39238,#39239,#39240,#39241,#39242),.UNSPECIFIED.,.F.,.F.,(4,3,3,
3,3,3,3,4),(76.5146171948413,76.6246633999996,77.1222261493502,77.6197888987009,
78.1173516480515,78.6149143974022,79.1124771467528,79.5325596182791),
 .UNSPECIFIED.);
#682=B_SPLINE_CURVE_WITH_KNOTS('',3,(#39244,#39245,#39246,#39247,#39248,
#39249,#39250,#39251,#39252,#39253,#39254,#39255,#39256,#39257,#39258,#39259,
#39260,#39261,#39262,#39263,#39264,#39265,#39266,#39267,#39268,#39269,#39270,
#39271,#39272,#39273,#39274,#39275,#39276,#39277,#39278,#39279,#39280,#39281,
#39282,#39283,#39284,#39285,#39286,#39287,#39288,#39289,#39290,#39291,#39292,
#39293,#39294,#39295,#39296,#39297,#39298,#39299,#39300,#39301,#39302,#39303,
#39304,#39305,#39306,#39307,#39308,#39309,#39310,#39311,#39312,#39313,#39314,
#39315,#39316,#39317,#39318,#39319,#39320,#39321,#39322,#39323,#39324,#39325,
#39326,#39327,#39328,#39329,#39330,#39331,#39332,#39333,#39334,#39335,#39336,
#39337,#39338,#39339,#39340,#39341,#39342,#39343,#39344,#39345,#39346),
 .UNSPECIFIED.,.F.,.F.,(4,3,3,3,3,3,3,3,3,3,3,3,3,3,3,3,3,3,3,3,3,3,3,3,
3,3,3,3,3,3,3,3,3,3,4),(-0.968477696161936,-0.934343797368491,-0.894226277483961,
-0.871339551305548,-0.855822539845121,-0.849949261747619,-0.809088844038457,
-0.768077284767626,-0.751532687618365,-0.742536577619449,-0.734141406691584,
-0.711132468056658,-0.670310088690189,-0.628911606809814,-0.591876013787433,
-0.564099319020647,-0.556019424396184,-0.51377696547059,-0.48076923472029,
-0.438727307185997,-0.396438608516356,-0.380090389242943,-0.373382824706804,
-0.330696753861742,-0.287182914486212,-0.243669075110682,-0.213210440721847,
-0.199884788176731,-0.191537541849349,-0.185963421418205,-0.14306631876944,
-0.0993786244214358,-0.0556350222056884,-0.0124004253203635,0.),
 .UNSPECIFIED.);
#683=B_SPLINE_CURVE_WITH_KNOTS('',3,(#39347,#39348,#39349,#39350,#39351,
#39352,#39353,#39354,#39355,#39356,#39357,#39358,#39359,#39360),
 .UNSPECIFIED.,.F.,.F.,(4,1,1,1,1,1,1,1,1,1,1,4),(10.3761157273099,10.7961981988362,
11.2937609481868,11.7913236975375,12.2888864468881,12.7864491962387,13.2840119455894,
13.78157469494,14.2791374442907,14.7767001936413,15.274262942992,15.707963267949),
 .UNSPECIFIED.);
#684=B_SPLINE_CURVE_WITH_KNOTS('',3,(#39366,#39367,#39368,#39369,#39370,
#39371,#39372,#39373,#39374,#39375,#39376,#39377,#39378,#39379,#39380,#39381,
#39382,#39383,#39384,#39385,#39386,#39387,#39388,#39389,#39390,#39391,#39392,
#39393,#39394,#39395,#39396,#39397,#39398,#39399,#39400,#39401,#39402,#39403,
#39404,#39405,#39406,#39407,#39408,#39409,#39410,#39411,#39412,#39413,#39414,
#39415,#39416,#39417,#39418,#39419,#39420,#39421,#39422,#39423,#39424,#39425,
#39426,#39427,#39428,#39429,#39430,#39431,#39432,#39433,#39434,#39435,#39436,
#39437,#39438,#39439,#39440,#39441,#39442,#39443,#39444,#39445,#39446,#39447,
#39448,#39449,#39450,#39451,#39452,#39453,#39454,#39455,#39456,#39457,#39458,
#39459,#39460,#39461,#39462,#39463,#39464,#39465),.UNSPECIFIED.,.F.,.F.,
(4,3,3,3,3,3,3,3,3,3,3,3,3,3,3,3,3,3,3,3,3,3,3,3,3,3,3,3,3,3,3,3,3,4),(-0.965990216419325,
-0.927769800274406,-0.884036457390911,-0.85929634029234,-0.841593944851099,
-0.834687190844098,-0.791436271424871,-0.74844726071717,-0.715784639906417,
-0.710378030072974,-0.686115520602341,-0.643612953183401,-0.600900815160043,
-0.563353409044655,-0.535192854458115,-0.529195526619761,-0.487304944852415,
-0.450711190698493,-0.408716441214337,-0.366944223277963,-0.350749948031817,
-0.345333543994406,-0.304097381804349,-0.263026243406926,-0.221955105009502,
-0.194210716883314,-0.181344115695033,-0.1730027188061,-0.167235292295272,
-0.125426469221454,-0.0849353441299271,-0.0447936662663009,-0.00549739522862838,
0.),.UNSPECIFIED.);
#685=B_SPLINE_CURVE_WITH_KNOTS('',3,(#39468,#39469,#39470,#39471,#39472,
#39473,#39474,#39475,#39476,#39477,#39478,#39479),.UNSPECIFIED.,.F.,.F.,
(4,1,1,1,1,1,1,1,1,4),(11.6150328478181,12.1125955971687,12.6101583465194,
13.10772109587,13.6052838452207,14.1028465945713,14.600409343922,15.0979720932726,
15.5955348426233,15.707963267949),.UNSPECIFIED.);
#686=B_SPLINE_CURVE_WITH_KNOTS('',3,(#40149,#40150,#40151,#40152,#40153,
#40154,#40155,#40156,#40157,#40158,#40159,#40160,#40161,#40162,#40163,#40164,
#40165,#40166,#40167,#40168,#40169,#40170,#40171,#40172,#40173,#40174,#40175,
#40176,#40177,#40178,#40179,#40180,#40181,#40182,#40183,#40184,#40185,#40186,
#40187,#40188,#40189,#40190,#40191,#40192,#40193,#40194,#40195,#40196,#40197,
#40198,#40199,#40200,#40201,#40202,#40203,#40204,#40205,#40206,#40207,#40208,
#40209,#40210,#40211,#40212,#40213,#40214,#40215,#40216,#40217,#40218,#40219,
#40220,#40221,#40222,#40223,#40224,#40225,#40226,#40227,#40228,#40229,#40230,
#40231,#40232,#40233,#40234,#40235,#40236,#40237,#40238,#40239,#40240,#40241,
#40242,#40243,#40244,#40245,#40246,#40247,#40248,#40249,#40250,#40251),
 .UNSPECIFIED.,.F.,.F.,(4,3,3,3,3,3,3,3,3,3,3,3,3,3,3,3,3,3,3,3,3,3,3,3,
3,3,3,3,3,3,3,3,3,3,4),(-0.968477696161912,-0.934343797368481,-0.894226277807462,
-0.871339551588618,-0.85582253996102,-0.849949261921466,-0.80908884435452,
-0.768077285019809,-0.751532687806619,-0.742536577935966,-0.734141406720873,
-0.711132468056709,-0.670310088248261,-0.628911606247961,-0.591876013366052,
-0.564099318704621,-0.556019424467619,-0.51377696546797,-0.480769234720327,
-0.438727306412881,-0.39643860794713,-0.380090388267127,-0.373382824556077,
-0.330696752907007,-0.287182914008866,-0.243669075110725,-0.213210440721885,
-0.199884788176767,-0.191537541538495,-0.185963421107643,-0.143066322667477,
-0.099378629805352,-0.0556350264235498,-0.0124004243521518,0.),
 .UNSPECIFIED.);
#687=B_SPLINE_CURVE_WITH_KNOTS('',3,(#40252,#40253,#40254,#40255,#40256,
#40257,#40258,#40259,#40260,#40261,#40262,#40263,#40264,#40265,#40266,#40267),
 .UNSPECIFIED.,.F.,.F.,(4,3,3,3,3,4),(-81.6002908935061,-81.1027281441555,
-80.6051653948048,-80.1076026454542,-79.6100398961035,-79.4911541062858),
 .UNSPECIFIED.);
#905=B_SPLINE_SURFACE_WITH_KNOTS('',3,3,((#38452,#38453,#38454,#38455,#38456,
#38457,#38458,#38459,#38460,#38461,#38462,#38463,#38464,#38465,#38466,#38467,
#38468,#38469,#38470,#38471,#38472,#38473,#38474,#38475,#38476,#38477,#38478,
#38479,#38480,#38481,#38482,#38483,#38484,#38485,#38486,#38487,#38488,#38489,
#38490,#38491,#38492,#38493,#38494,#38495,#38496,#38497,#38498,#38499,#38500,
#38501,#38502,#38503,#38504,#38505,#38506,#38507,#38508,#38509,#38510,#38511,
#38512,#38513,#38514,#38515,#38516,#38517,#38518,#38519,#38520,#38521,#38522,
#38523,#38524,#38525,#38526,#38527,#38528,#38529,#38530,#38531,#38532,#38533,
#38534,#38535,#38536,#38537,#38538,#38539,#38540,#38541,#38542,#38543,#38544,
#38545,#38546,#38547,#38548,#38549,#38550,#38551,#38552,#38553,#38554,#38555,
#38556,#38557,#38558,#38559,#38560,#38561,#38562,#38563,#38564,#38565,#38566,
#38567,#38568,#38569,#38570,#38571,#38572,#38573,#38574,#38575,#38576,#38577,
#38578,#38579,#38580,#38581,#38582,#38583,#38584,#38585,#38586,#38587,#38588,
#38589,#38590,#38591,#38592,#38593,#38594,#38595,#38596,#38597,#38598,#38599,
#38600,#38601,#38602,#38603,#38604,#38605,#38606,#38607,#38608,#38609,#38610,
#38611,#38612,#38613,#38614,#38615,#38616,#38617,#38618),(#38619,#38620,
#38621,#38622,#38623,#38624,#38625,#38626,#38627,#38628,#38629,#38630,#38631,
#38632,#38633,#38634,#38635,#38636,#38637,#38638,#38639,#38640,#38641,#38642,
#38643,#38644,#38645,#38646,#38647,#38648,#38649,#38650,#38651,#38652,#38653,
#38654,#38655,#38656,#38657,#38658,#38659,#38660,#38661,#38662,#38663,#38664,
#38665,#38666,#38667,#38668,#38669,#38670,#38671,#38672,#38673,#38674,#38675,
#38676,#38677,#38678,#38679,#38680,#38681,#38682,#38683,#38684,#38685,#38686,
#38687,#38688,#38689,#38690,#38691,#38692,#38693,#38694,#38695,#38696,#38697,
#38698,#38699,#38700,#38701,#38702,#38703,#38704,#38705,#38706,#38707,#38708,
#38709,#38710,#38711,#38712,#38713,#38714,#38715,#38716,#38717,#38718,#38719,
#38720,#38721,#38722,#38723,#38724,#38725,#38726,#38727,#38728,#38729,#38730,
#38731,#38732,#38733,#38734,#38735,#38736,#38737,#38738,#38739,#38740,#38741,
#38742,#38743,#38744,#38745,#38746,#38747,#38748,#38749,#38750,#38751,#38752,
#38753,#38754,#38755,#38756,#38757,#38758,#38759,#38760,#38761,#38762,#38763,
#38764,#38765,#38766,#38767,#38768,#38769,#38770,#38771,#38772,#38773,#38774,
#38775,#38776,#38777,#38778,#38779,#38780,#38781,#38782,#38783,#38784,#38785),
(#38786,#38787,#38788,#38789,#38790,#38791,#38792,#38793,#38794,#38795,
#38796,#38797,#38798,#38799,#38800,#38801,#38802,#38803,#38804,#38805,#38806,
#38807,#38808,#38809,#38810,#38811,#38812,#38813,#38814,#38815,#38816,#38817,
#38818,#38819,#38820,#38821,#38822,#38823,#38824,#38825,#38826,#38827,#38828,
#38829,#38830,#38831,#38832,#38833,#38834,#38835,#38836,#38837,#38838,#38839,
#38840,#38841,#38842,#38843,#38844,#38845,#38846,#38847,#38848,#38849,#38850,
#38851,#38852,#38853,#38854,#38855,#38856,#38857,#38858,#38859,#38860,#38861,
#38862,#38863,#38864,#38865,#38866,#38867,#38868,#38869,#38870,#38871,#38872,
#38873,#38874,#38875,#38876,#38877,#38878,#38879,#38880,#38881,#38882,#38883,
#38884,#38885,#38886,#38887,#38888,#38889,#38890,#38891,#38892,#38893,#38894,
#38895,#38896,#38897,#38898,#38899,#38900,#38901,#38902,#38903,#38904,#38905,
#38906,#38907,#38908,#38909,#38910,#38911,#38912,#38913,#38914,#38915,#38916,
#38917,#38918,#38919,#38920,#38921,#38922,#38923,#38924,#38925,#38926,#38927,
#38928,#38929,#38930,#38931,#38932,#38933,#38934,#38935,#38936,#38937,#38938,
#38939,#38940,#38941,#38942,#38943,#38944,#38945,#38946,#38947,#38948,#38949,
#38950,#38951,#38952),(#38953,#38954,#38955,#38956,#38957,#38958,#38959,
#38960,#38961,#38962,#38963,#38964,#38965,#38966,#38967,#38968,#38969,#38970,
#38971,#38972,#38973,#38974,#38975,#38976,#38977,#38978,#38979,#38980,#38981,
#38982,#38983,#38984,#38985,#38986,#38987,#38988,#38989,#38990,#38991,#38992,
#38993,#38994,#38995,#38996,#38997,#38998,#38999,#39000,#39001,#39002,#39003,
#39004,#39005,#39006,#39007,#39008,#39009,#39010,#39011,#39012,#39013,#39014,
#39015,#39016,#39017,#39018,#39019,#39020,#39021,#39022,#39023,#39024,#39025,
#39026,#39027,#39028,#39029,#39030,#39031,#39032,#39033,#39034,#39035,#39036,
#39037,#39038,#39039,#39040,#39041,#39042,#39043,#39044,#39045,#39046,#39047,
#39048,#39049,#39050,#39051,#39052,#39053,#39054,#39055,#39056,#39057,#39058,
#39059,#39060,#39061,#39062,#39063,#39064,#39065,#39066,#39067,#39068,#39069,
#39070,#39071,#39072,#39073,#39074,#39075,#39076,#39077,#39078,#39079,#39080,
#39081,#39082,#39083,#39084,#39085,#39086,#39087,#39088,#39089,#39090,#39091,
#39092,#39093,#39094,#39095,#39096,#39097,#39098,#39099,#39100,#39101,#39102,
#39103,#39104,#39105,#39106,#39107,#39108,#39109,#39110,#39111,#39112,#39113,
#39114,#39115,#39116,#39117,#39118,#39119)),.UNSPECIFIED.,.F.,.F.,.F.,(4,
4),(4,1,1,1,1,1,1,1,1,1,1,1,1,1,1,1,1,1,1,1,1,1,1,1,1,1,1,1,1,1,1,1,1,1,
1,1,1,1,1,1,1,1,1,1,1,1,1,1,1,1,1,1,1,1,1,1,1,1,1,1,1,1,1,1,1,1,1,1,1,1,
1,1,1,1,1,1,1,1,1,1,1,1,1,1,1,1,1,1,1,1,1,1,1,1,1,1,1,1,1,1,1,1,1,1,1,1,
1,1,1,1,1,1,1,1,1,1,1,1,1,1,1,1,1,1,1,1,1,1,1,1,1,1,1,1,1,1,1,1,1,1,1,1,
1,1,1,1,1,1,1,1,1,1,1,1,1,1,1,1,1,1,1,1,1,1,4),(0.,0.0658179306876167),
(8.30838445208293,8.80594720143358,9.30350995078422,9.80107270013487,10.2986354494855,
10.7961981988362,11.2937609481868,11.7913236975375,12.2888864468881,12.7864491962387,
13.2840119455894,13.78157469494,14.2791374442907,14.7767001936413,15.274262942992,
15.7718256923426,16.2693884416933,16.7669511910439,17.2645139403946,17.7620766897452,
18.2596394390959,18.7572021884465,19.2547649377972,19.7523276871478,20.2498904364984,
20.7474531858491,21.2450159351997,21.7425786845504,22.240141433901,22.7377041832517,
23.2352669326023,23.732829681953,24.2303924313036,24.7279551806543,25.2255179300049,
25.7230806793556,26.2206434287062,26.7182061780569,27.2157689274075,27.7133316767581,
28.2108944261088,28.7084571754594,29.2060199248101,29.7035826741607,30.2011454235114,
30.698708172862,31.1962709222127,31.6938336715633,32.191396420914,32.6889591702646,
33.1865219196153,33.6840846689659,34.1816474183166,34.6792101676672,35.1767729170178,
35.6743356663685,36.1718984157191,36.6694611650698,37.1670239144204,37.6645866637711,
38.1621494131217,38.6597121624724,39.157274911823,39.6548376611737,40.1524004105243,
40.649963159875,41.1475259092256,41.6450886585762,42.1426514079269,42.6402141572775,
43.1377769066282,43.6353396559788,44.1329024053295,44.6304651546801,45.1280279040308,
45.6255906533814,46.1231534027321,46.6207161520827,47.1182789014334,47.615841650784,
48.1134044001347,48.6109671494853,49.108529898836,49.6060926481866,50.1036553975372,
50.6012181468879,51.0987808962385,51.5963436455892,52.0939063949398,52.5914691442905,
53.0890318936411,53.5865946429918,54.0841573923424,54.5817201416931,55.0792828910437,
55.5768456403944,56.074408389745,56.5719711390957,57.0695338884463,57.5670966377969,
58.0646593871476,58.5622221364982,59.0597848858489,59.5573476351995,60.0549103845502,
60.5524731339008,61.0500358832515,61.5475986326021,62.0451613819528,62.5427241313034,
63.0402868806541,63.5378496300047,64.0354123793553,64.532975128706,65.0305378780566,
65.5281006274073,66.0256633767579,66.5232261261086,67.0207888754592,67.5183516248099,
68.0159143741605,68.5134771235112,69.0110398728618,69.5086026222125,70.0061653715631,
70.5037281209138,71.0012908702644,71.498853619615,71.9964163689657,72.4939791183163,
72.991541867667,73.4891046170176,73.9866673663683,74.4842301157189,74.9817928650696,
75.4793556144202,75.9769183637709,76.4744811131215,76.9720438624722,77.4696066118228,
77.9671693611735,78.4647321105241,78.9622948598747,79.4598576092254,79.957420358576,
80.4549831079267,80.9525458572773,81.450108606628,81.9476713559786,82.4452341053293,
82.9427968546799,83.4403596040306,83.9379223533812,84.4354851027319,84.9330478520825,
85.4306106014332,85.9281733507838,86.4257361001345,86.9232988494851,87.4208615988357,
87.9184243481864,88.415987097537,88.9135498468877,89.4111125962383,89.908675345589),
 .UNSPECIFIED.);
#906=B_SPLINE_SURFACE_WITH_KNOTS('',3,3,((#39480,#39481,#39482,#39483,#39484,
#39485,#39486,#39487,#39488,#39489,#39490,#39491,#39492,#39493,#39494,#39495,
#39496,#39497,#39498,#39499,#39500,#39501,#39502,#39503,#39504,#39505,#39506,
#39507,#39508,#39509,#39510,#39511,#39512,#39513,#39514,#39515,#39516,#39517,
#39518,#39519,#39520,#39521,#39522,#39523,#39524,#39525,#39526,#39527,#39528,
#39529,#39530,#39531,#39532,#39533,#39534,#39535,#39536,#39537,#39538,#39539,
#39540,#39541,#39542,#39543,#39544,#39545,#39546,#39547,#39548,#39549,#39550,
#39551,#39552,#39553,#39554,#39555,#39556,#39557,#39558,#39559,#39560,#39561,
#39562,#39563,#39564,#39565,#39566,#39567,#39568,#39569,#39570,#39571,#39572,
#39573,#39574,#39575,#39576,#39577,#39578,#39579,#39580,#39581,#39582,#39583,
#39584,#39585,#39586,#39587,#39588,#39589,#39590,#39591,#39592,#39593,#39594,
#39595,#39596,#39597,#39598,#39599,#39600,#39601,#39602,#39603,#39604,#39605,
#39606,#39607,#39608,#39609,#39610,#39611,#39612,#39613,#39614,#39615,#39616,
#39617,#39618,#39619,#39620,#39621,#39622,#39623,#39624,#39625,#39626,#39627,
#39628,#39629,#39630,#39631,#39632,#39633,#39634,#39635,#39636,#39637,#39638,
#39639,#39640,#39641,#39642,#39643,#39644,#39645,#39646),(#39647,#39648,
#39649,#39650,#39651,#39652,#39653,#39654,#39655,#39656,#39657,#39658,#39659,
#39660,#39661,#39662,#39663,#39664,#39665,#39666,#39667,#39668,#39669,#39670,
#39671,#39672,#39673,#39674,#39675,#39676,#39677,#39678,#39679,#39680,#39681,
#39682,#39683,#39684,#39685,#39686,#39687,#39688,#39689,#39690,#39691,#39692,
#39693,#39694,#39695,#39696,#39697,#39698,#39699,#39700,#39701,#39702,#39703,
#39704,#39705,#39706,#39707,#39708,#39709,#39710,#39711,#39712,#39713,#39714,
#39715,#39716,#39717,#39718,#39719,#39720,#39721,#39722,#39723,#39724,#39725,
#39726,#39727,#39728,#39729,#39730,#39731,#39732,#39733,#39734,#39735,#39736,
#39737,#39738,#39739,#39740,#39741,#39742,#39743,#39744,#39745,#39746,#39747,
#39748,#39749,#39750,#39751,#39752,#39753,#39754,#39755,#39756,#39757,#39758,
#39759,#39760,#39761,#39762,#39763,#39764,#39765,#39766,#39767,#39768,#39769,
#39770,#39771,#39772,#39773,#39774,#39775,#39776,#39777,#39778,#39779,#39780,
#39781,#39782,#39783,#39784,#39785,#39786,#39787,#39788,#39789,#39790,#39791,
#39792,#39793,#39794,#39795,#39796,#39797,#39798,#39799,#39800,#39801,#39802,
#39803,#39804,#39805,#39806,#39807,#39808,#39809,#39810,#39811,#39812,#39813),
(#39814,#39815,#39816,#39817,#39818,#39819,#39820,#39821,#39822,#39823,
#39824,#39825,#39826,#39827,#39828,#39829,#39830,#39831,#39832,#39833,#39834,
#39835,#39836,#39837,#39838,#39839,#39840,#39841,#39842,#39843,#39844,#39845,
#39846,#39847,#39848,#39849,#39850,#39851,#39852,#39853,#39854,#39855,#39856,
#39857,#39858,#39859,#39860,#39861,#39862,#39863,#39864,#39865,#39866,#39867,
#39868,#39869,#39870,#39871,#39872,#39873,#39874,#39875,#39876,#39877,#39878,
#39879,#39880,#39881,#39882,#39883,#39884,#39885,#39886,#39887,#39888,#39889,
#39890,#39891,#39892,#39893,#39894,#39895,#39896,#39897,#39898,#39899,#39900,
#39901,#39902,#39903,#39904,#39905,#39906,#39907,#39908,#39909,#39910,#39911,
#39912,#39913,#39914,#39915,#39916,#39917,#39918,#39919,#39920,#39921,#39922,
#39923,#39924,#39925,#39926,#39927,#39928,#39929,#39930,#39931,#39932,#39933,
#39934,#39935,#39936,#39937,#39938,#39939,#39940,#39941,#39942,#39943,#39944,
#39945,#39946,#39947,#39948,#39949,#39950,#39951,#39952,#39953,#39954,#39955,
#39956,#39957,#39958,#39959,#39960,#39961,#39962,#39963,#39964,#39965,#39966,
#39967,#39968,#39969,#39970,#39971,#39972,#39973,#39974,#39975,#39976,#39977,
#39978,#39979,#39980),(#39981,#39982,#39983,#39984,#39985,#39986,#39987,
#39988,#39989,#39990,#39991,#39992,#39993,#39994,#39995,#39996,#39997,#39998,
#39999,#40000,#40001,#40002,#40003,#40004,#40005,#40006,#40007,#40008,#40009,
#40010,#40011,#40012,#40013,#40014,#40015,#40016,#40017,#40018,#40019,#40020,
#40021,#40022,#40023,#40024,#40025,#40026,#40027,#40028,#40029,#40030,#40031,
#40032,#40033,#40034,#40035,#40036,#40037,#40038,#40039,#40040,#40041,#40042,
#40043,#40044,#40045,#40046,#40047,#40048,#40049,#40050,#40051,#40052,#40053,
#40054,#40055,#40056,#40057,#40058,#40059,#40060,#40061,#40062,#40063,#40064,
#40065,#40066,#40067,#40068,#40069,#40070,#40071,#40072,#40073,#40074,#40075,
#40076,#40077,#40078,#40079,#40080,#40081,#40082,#40083,#40084,#40085,#40086,
#40087,#40088,#40089,#40090,#40091,#40092,#40093,#40094,#40095,#40096,#40097,
#40098,#40099,#40100,#40101,#40102,#40103,#40104,#40105,#40106,#40107,#40108,
#40109,#40110,#40111,#40112,#40113,#40114,#40115,#40116,#40117,#40118,#40119,
#40120,#40121,#40122,#40123,#40124,#40125,#40126,#40127,#40128,#40129,#40130,
#40131,#40132,#40133,#40134,#40135,#40136,#40137,#40138,#40139,#40140,#40141,
#40142,#40143,#40144,#40145,#40146,#40147)),.UNSPECIFIED.,.F.,.F.,.F.,(4,
4),(4,1,1,1,1,1,1,1,1,1,1,1,1,1,1,1,1,1,1,1,1,1,1,1,1,1,1,1,1,1,1,1,1,1,
1,1,1,1,1,1,1,1,1,1,1,1,1,1,1,1,1,1,1,1,1,1,1,1,1,1,1,1,1,1,1,1,1,1,1,1,
1,1,1,1,1,1,1,1,1,1,1,1,1,1,1,1,1,1,1,1,1,1,1,1,1,1,1,1,1,1,1,1,1,1,1,1,
1,1,1,1,1,1,1,1,1,1,1,1,1,1,1,1,1,1,1,1,1,1,1,1,1,1,1,1,1,1,1,1,1,1,1,1,
1,1,1,1,1,1,1,1,1,1,1,1,1,1,1,1,1,1,1,1,1,1,4),(0.,0.0658179306876167),
(11.6150328478181,12.1125955971687,12.6101583465194,13.10772109587,13.6052838452207,
14.1028465945713,14.600409343922,15.0979720932726,15.5955348426233,16.0930975919739,
16.5906603413246,17.0882230906752,17.5857858400259,18.0833485893765,18.5809113387272,
19.0784740880778,19.5760368374285,20.0735995867791,20.5711623361297,21.0687250854804,
21.566287834831,22.0638505841817,22.5614133335323,23.058976082883,23.5565388322336,
24.0541015815843,24.5516643309349,25.0492270802856,25.5467898296362,26.0443525789869,
26.5419153283375,27.0394780776882,27.5370408270388,28.0346035763895,28.5321663257401,
29.0297290750907,29.5272918244414,30.024854573792,30.5224173231427,31.0199800724933,
31.517542821844,32.0151055711946,32.5126683205453,33.0102310698959,33.5077938192466,
34.0053565685972,34.5029193179479,35.0004820672985,35.4980448166492,35.9956075659998,
36.4931703153505,36.9907330647011,37.4882958140517,37.9858585634024,38.483421312753,
38.9809840621037,39.4785468114543,39.976109560805,40.4736723101556,40.9712350595063,
41.4687978088569,41.9663605582076,42.4639233075582,42.9614860569089,43.4590488062595,
43.9566115556102,44.4541743049608,44.9517370543115,45.4492998036621,45.9468625530127,
46.4444253023634,46.941988051714,47.4395508010647,47.9371135504153,48.434676299766,
48.9322390491166,49.4298017984673,49.9273645478179,50.4249272971686,50.9224900465192,
51.4200527958699,51.9176155452205,52.4151782945712,52.9127410439218,53.4103037932725,
53.9078665426231,54.4054292919737,54.9029920413244,55.400554790675,55.8981175400257,
56.3956802893763,56.893243038727,57.3908057880776,57.8883685374283,58.3859312867789,
58.8834940361296,59.3810567854802,59.8786195348309,60.3761822841815,60.8737450335322,
61.3713077828828,61.8688705322335,62.3664332815841,62.8639960309348,63.3615587802854,
63.859121529636,64.3566842789867,64.8542470283373,65.351809777688,65.8493725270386,
66.3469352763893,66.8444980257399,67.3420607750906,67.8396235244412,68.3371862737919,
68.8347490231425,69.3323117724932,69.8298745218438,70.3274372711945,70.8250000205451,
71.3225627698958,71.8201255192464,72.317688268597,72.8152510179477,73.3128137672983,
73.810376516649,74.3079392659996,74.8055020153503,75.3030647647009,75.8006275140516,
76.2981902634022,76.7957530127529,77.2933157621035,77.7908785114542,78.2884412608048,
78.7860040101555,79.2835667595061,79.7811295088568,80.2786922582074,80.776255007558,
81.2738177569087,81.7713805062593,82.26894325561,82.7665060049606,83.2640687543113,
83.7616315036619,84.2591942530126,84.7567570023632,85.2543197517139,85.7518825010645,
86.2494452504152,86.7470079997658,87.2445707491165,87.7421334984671,88.2396962478177,
88.7372589971684,89.234821746519,89.7323844958697,90.2299472452203,90.727509994571,
91.2250727439216,91.7226354932723,92.2201982426229,92.7177609919736,93.2153237413242),
 .UNSPECIFIED.);
#979=FACE_BOUND('',#3322,.T.);
#980=FACE_BOUND('',#3323,.T.);
#981=FACE_BOUND('',#3324,.T.);
#982=FACE_BOUND('',#3325,.T.);
#983=FACE_BOUND('',#3326,.T.);
#984=FACE_BOUND('',#3327,.T.);
#985=FACE_BOUND('',#3328,.T.);
#986=FACE_BOUND('',#3329,.T.);
#987=FACE_BOUND('',#3330,.T.);
#988=FACE_BOUND('',#3331,.T.);
#989=FACE_BOUND('',#3332,.T.);
#990=FACE_BOUND('',#3333,.T.);
#991=FACE_BOUND('',#3334,.T.);
#992=FACE_BOUND('',#3335,.T.);
#993=FACE_BOUND('',#3336,.T.);
#994=FACE_BOUND('',#3337,.T.);
#995=FACE_BOUND('',#3338,.T.);
#996=FACE_BOUND('',#3339,.T.);
#997=FACE_BOUND('',#3340,.T.);
#998=FACE_BOUND('',#3341,.T.);
#999=FACE_BOUND('',#3342,.T.);
#1000=FACE_BOUND('',#3450,.T.);
#1225=PLANE('',#17372);
#1226=PLANE('',#17375);
#1227=PLANE('',#17377);
#1228=PLANE('',#17439);
#1229=PLANE('',#17440);
#1230=PLANE('',#17445);
#1231=PLANE('',#17446);
#1232=PLANE('',#17447);
#1233=PLANE('',#17448);
#1234=PLANE('',#17449);
#1235=PLANE('',#17450);
#1236=PLANE('',#17451);
#1237=PLANE('',#17452);
#1238=PLANE('',#17453);
#1239=PLANE('',#17454);
#1240=PLANE('',#17455);
#1241=PLANE('',#17456);
#1242=PLANE('',#17457);
#1243=PLANE('',#17458);
#1244=PLANE('',#17459);
#1245=PLANE('',#17460);
#1246=PLANE('',#17461);
#1247=PLANE('',#17462);
#1248=PLANE('',#17463);
#1249=PLANE('',#17464);
#1250=PLANE('',#17465);
#1251=PLANE('',#17466);
#1252=PLANE('',#17467);
#1253=PLANE('',#17468);
#1254=PLANE('',#17469);
#1255=PLANE('',#17470);
#1256=PLANE('',#17471);
#1257=PLANE('',#17472);
#1258=PLANE('',#17473);
#1259=PLANE('',#17474);
#1260=PLANE('',#17475);
#1261=PLANE('',#17476);
#1262=PLANE('',#17477);
#1263=PLANE('',#17478);
#1264=PLANE('',#17479);
#1265=PLANE('',#17480);
#1266=PLANE('',#17481);
#1267=PLANE('',#17482);
#1268=PLANE('',#17483);
#1269=PLANE('',#17484);
#1270=PLANE('',#17485);
#1271=PLANE('',#17486);
#1272=PLANE('',#17487);
#1273=PLANE('',#17488);
#1274=PLANE('',#17489);
#1275=PLANE('',#17490);
#1276=PLANE('',#17491);
#1277=PLANE('',#17492);
#1278=PLANE('',#17493);
#1279=PLANE('',#17494);
#1280=PLANE('',#17495);
#1281=PLANE('',#17496);
#1282=PLANE('',#17497);
#1283=PLANE('',#17498);
#1284=PLANE('',#17499);
#1285=PLANE('',#17500);
#1286=PLANE('',#17501);
#1287=PLANE('',#17502);
#1288=PLANE('',#17503);
#1289=PLANE('',#17504);
#1290=PLANE('',#17505);
#1291=PLANE('',#17506);
#1292=PLANE('',#17507);
#1293=PLANE('',#17508);
#1294=PLANE('',#17509);
#1295=PLANE('',#17510);
#1296=PLANE('',#17511);
#1297=PLANE('',#17512);
#1298=PLANE('',#17513);
#1299=PLANE('',#17514);
#1300=PLANE('',#17515);
#1301=PLANE('',#17516);
#1302=PLANE('',#17517);
#1303=PLANE('',#17518);
#1304=PLANE('',#17519);
#1305=PLANE('',#17520);
#1306=PLANE('',#17521);
#1307=PLANE('',#17522);
#1308=PLANE('',#17523);
#1309=PLANE('',#17524);
#1310=PLANE('',#17525);
#1311=PLANE('',#17526);
#1312=PLANE('',#17527);
#1313=PLANE('',#17528);
#1314=PLANE('',#17529);
#1315=PLANE('',#17530);
#1316=PLANE('',#17531);
#1317=PLANE('',#17532);
#1318=PLANE('',#17533);
#1319=PLANE('',#17534);
#1320=PLANE('',#17535);
#1321=PLANE('',#17536);
#1322=PLANE('',#17537);
#1323=PLANE('',#17538);
#1324=PLANE('',#17539);
#1325=PLANE('',#17540);
#1326=PLANE('',#17541);
#1327=PLANE('',#17542);
#1328=PLANE('',#17547);
#1718=CYLINDRICAL_SURFACE('',#17343,4.942);
#1719=CYLINDRICAL_SURFACE('',#17345,4.942);
#1720=CYLINDRICAL_SURFACE('',#17346,4.942);
#1721=CYLINDRICAL_SURFACE('',#17347,4.942);
#1722=CYLINDRICAL_SURFACE('',#17348,4.942);
#1723=CYLINDRICAL_SURFACE('',#17349,4.942);
#1724=CYLINDRICAL_SURFACE('',#17350,4.942);
#1725=CYLINDRICAL_SURFACE('',#17351,4.942);
#1726=CYLINDRICAL_SURFACE('',#17352,4.942);
#1727=CYLINDRICAL_SURFACE('',#17353,4.942);
#1728=CYLINDRICAL_SURFACE('',#17354,4.942);
#1729=CYLINDRICAL_SURFACE('',#17355,4.942);
#1730=CYLINDRICAL_SURFACE('',#17356,4.942);
#1731=CYLINDRICAL_SURFACE('',#17357,4.372);
#1732=CYLINDRICAL_SURFACE('',#17359,4.372);
#1733=CYLINDRICAL_SURFACE('',#17361,4.372);
#1734=CYLINDRICAL_SURFACE('',#17362,4.372);
#1735=CYLINDRICAL_SURFACE('',#17363,4.372);
#1736=CYLINDRICAL_SURFACE('',#17364,4.372);
#1737=CYLINDRICAL_SURFACE('',#17365,4.372);
#1738=CYLINDRICAL_SURFACE('',#17366,4.372);
#1739=CYLINDRICAL_SURFACE('',#17367,4.372);
#1740=CYLINDRICAL_SURFACE('',#17368,4.372);
#1741=CYLINDRICAL_SURFACE('',#17369,4.372);
#1742=CYLINDRICAL_SURFACE('',#17370,4.372);
#1743=CYLINDRICAL_SURFACE('',#17371,4.372);
#1744=CYLINDRICAL_SURFACE('',#17380,7.);
#1745=CYLINDRICAL_SURFACE('',#17444,4.372);
#1746=CYLINDRICAL_SURFACE('',#17545,4.942);
#2278=FACE_OUTER_BOUND('',#3292,.T.);
#2279=FACE_OUTER_BOUND('',#3293,.T.);
#2280=FACE_OUTER_BOUND('',#3294,.T.);
#2281=FACE_OUTER_BOUND('',#3295,.T.);
#2282=FACE_OUTER_BOUND('',#3296,.T.);
#2283=FACE_OUTER_BOUND('',#3297,.T.);
#2284=FACE_OUTER_BOUND('',#3298,.T.);
#2285=FACE_OUTER_BOUND('',#3299,.T.);
#2286=FACE_OUTER_BOUND('',#3300,.T.);
#2287=FACE_OUTER_BOUND('',#3301,.T.);
#2288=FACE_OUTER_BOUND('',#3302,.T.);
#2289=FACE_OUTER_BOUND('',#3303,.T.);
#2290=FACE_OUTER_BOUND('',#3304,.T.);
#2291=FACE_OUTER_BOUND('',#3305,.T.);
#2292=FACE_OUTER_BOUND('',#3306,.T.);
#2293=FACE_OUTER_BOUND('',#3307,.T.);
#2294=FACE_OUTER_BOUND('',#3308,.T.);
#2295=FACE_OUTER_BOUND('',#3309,.T.);
#2296=FACE_OUTER_BOUND('',#3310,.T.);
#2297=FACE_OUTER_BOUND('',#3311,.T.);
#2298=FACE_OUTER_BOUND('',#3312,.T.);
#2299=FACE_OUTER_BOUND('',#3313,.T.);
#2300=FACE_OUTER_BOUND('',#3314,.T.);
#2301=FACE_OUTER_BOUND('',#3315,.T.);
#2302=FACE_OUTER_BOUND('',#3316,.T.);
#2303=FACE_OUTER_BOUND('',#3317,.T.);
#2304=FACE_OUTER_BOUND('',#3318,.T.);
#2305=FACE_OUTER_BOUND('',#3319,.T.);
#2306=FACE_OUTER_BOUND('',#3320,.T.);
#2307=FACE_OUTER_BOUND('',#3321,.T.);
#2308=FACE_OUTER_BOUND('',#3343,.T.);
#2309=FACE_OUTER_BOUND('',#3344,.T.);
#2310=FACE_OUTER_BOUND('',#3345,.T.);
#2311=FACE_OUTER_BOUND('',#3346,.T.);
#2312=FACE_OUTER_BOUND('',#3347,.T.);
#2313=FACE_OUTER_BOUND('',#3348,.T.);
#2314=FACE_OUTER_BOUND('',#3349,.T.);
#2315=FACE_OUTER_BOUND('',#3350,.T.);
#2316=FACE_OUTER_BOUND('',#3351,.T.);
#2317=FACE_OUTER_BOUND('',#3352,.T.);
#2318=FACE_OUTER_BOUND('',#3353,.T.);
#2319=FACE_OUTER_BOUND('',#3354,.T.);
#2320=FACE_OUTER_BOUND('',#3355,.T.);
#2321=FACE_OUTER_BOUND('',#3356,.T.);
#2322=FACE_OUTER_BOUND('',#3357,.T.);
#2323=FACE_OUTER_BOUND('',#3358,.T.);
#2324=FACE_OUTER_BOUND('',#3359,.T.);
#2325=FACE_OUTER_BOUND('',#3360,.T.);
#2326=FACE_OUTER_BOUND('',#3361,.T.);
#2327=FACE_OUTER_BOUND('',#3362,.T.);
#2328=FACE_OUTER_BOUND('',#3363,.T.);
#2329=FACE_OUTER_BOUND('',#3364,.T.);
#2330=FACE_OUTER_BOUND('',#3365,.T.);
#2331=FACE_OUTER_BOUND('',#3366,.T.);
#2332=FACE_OUTER_BOUND('',#3367,.T.);
#2333=FACE_OUTER_BOUND('',#3368,.T.);
#2334=FACE_OUTER_BOUND('',#3369,.T.);
#2335=FACE_OUTER_BOUND('',#3370,.T.);
#2336=FACE_OUTER_BOUND('',#3371,.T.);
#2337=FACE_OUTER_BOUND('',#3372,.T.);
#2338=FACE_OUTER_BOUND('',#3373,.T.);
#2339=FACE_OUTER_BOUND('',#3374,.T.);
#2340=FACE_OUTER_BOUND('',#3375,.T.);
#2341=FACE_OUTER_BOUND('',#3376,.T.);
#2342=FACE_OUTER_BOUND('',#3377,.T.);
#2343=FACE_OUTER_BOUND('',#3378,.T.);
#2344=FACE_OUTER_BOUND('',#3379,.T.);
#2345=FACE_OUTER_BOUND('',#3380,.T.);
#2346=FACE_OUTER_BOUND('',#3381,.T.);
#2347=FACE_OUTER_BOUND('',#3382,.T.);
#2348=FACE_OUTER_BOUND('',#3383,.T.);
#2349=FACE_OUTER_BOUND('',#3384,.T.);
#2350=FACE_OUTER_BOUND('',#3385,.T.);
#2351=FACE_OUTER_BOUND('',#3386,.T.);
#2352=FACE_OUTER_BOUND('',#3387,.T.);
#2353=FACE_OUTER_BOUND('',#3388,.T.);
#2354=FACE_OUTER_BOUND('',#3389,.T.);
#2355=FACE_OUTER_BOUND('',#3390,.T.);
#2356=FACE_OUTER_BOUND('',#3391,.T.);
#2357=FACE_OUTER_BOUND('',#3392,.T.);
#2358=FACE_OUTER_BOUND('',#3393,.T.);
#2359=FACE_OUTER_BOUND('',#3394,.T.);
#2360=FACE_OUTER_BOUND('',#3395,.T.);
#2361=FACE_OUTER_BOUND('',#3396,.T.);
#2362=FACE_OUTER_BOUND('',#3397,.T.);
#2363=FACE_OUTER_BOUND('',#3398,.T.);
#2364=FACE_OUTER_BOUND('',#3399,.T.);
#2365=FACE_OUTER_BOUND('',#3400,.T.);
#2366=FACE_OUTER_BOUND('',#3401,.T.);
#2367=FACE_OUTER_BOUND('',#3402,.T.);
#2368=FACE_OUTER_BOUND('',#3403,.T.);
#2369=FACE_OUTER_BOUND('',#3404,.T.);
#2370=FACE_OUTER_BOUND('',#3405,.T.);
#2371=FACE_OUTER_BOUND('',#3406,.T.);
#2372=FACE_OUTER_BOUND('',#3407,.T.);
#2373=FACE_OUTER_BOUND('',#3408,.T.);
#2374=FACE_OUTER_BOUND('',#3409,.T.);
#2375=FACE_OUTER_BOUND('',#3410,.T.);
#2376=FACE_OUTER_BOUND('',#3411,.T.);
#2377=FACE_OUTER_BOUND('',#3412,.T.);
#2378=FACE_OUTER_BOUND('',#3413,.T.);
#2379=FACE_OUTER_BOUND('',#3414,.T.);
#2380=FACE_OUTER_BOUND('',#3415,.T.);
#2381=FACE_OUTER_BOUND('',#3416,.T.);
#2382=FACE_OUTER_BOUND('',#3417,.T.);
#2383=FACE_OUTER_BOUND('',#3418,.T.);
#2384=FACE_OUTER_BOUND('',#3419,.T.);
#2385=FACE_OUTER_BOUND('',#3420,.T.);
#2386=FACE_OUTER_BOUND('',#3421,.T.);
#2387=FACE_OUTER_BOUND('',#3422,.T.);
#2388=FACE_OUTER_BOUND('',#3423,.T.);
#2389=FACE_OUTER_BOUND('',#3424,.T.);
#2390=FACE_OUTER_BOUND('',#3425,.T.);
#2391=FACE_OUTER_BOUND('',#3426,.T.);
#2392=FACE_OUTER_BOUND('',#3427,.T.);
#2393=FACE_OUTER_BOUND('',#3428,.T.);
#2394=FACE_OUTER_BOUND('',#3429,.T.);
#2395=FACE_OUTER_BOUND('',#3430,.T.);
#2396=FACE_OUTER_BOUND('',#3431,.T.);
#2397=FACE_OUTER_BOUND('',#3432,.T.);
#2398=FACE_OUTER_BOUND('',#3433,.T.);
#2399=FACE_OUTER_BOUND('',#3434,.T.);
#2400=FACE_OUTER_BOUND('',#3435,.T.);
#2401=FACE_OUTER_BOUND('',#3436,.T.);
#2402=FACE_OUTER_BOUND('',#3437,.T.);
#2403=FACE_OUTER_BOUND('',#3438,.T.);
#2404=FACE_OUTER_BOUND('',#3439,.T.);
#2405=FACE_OUTER_BOUND('',#3440,.T.);
#2406=FACE_OUTER_BOUND('',#3441,.T.);
#2407=FACE_OUTER_BOUND('',#3442,.T.);
#2408=FACE_OUTER_BOUND('',#3443,.T.);
#2409=FACE_OUTER_BOUND('',#3444,.T.);
#2410=FACE_OUTER_BOUND('',#3445,.T.);
#2411=FACE_OUTER_BOUND('',#3446,.T.);
#2412=FACE_OUTER_BOUND('',#3447,.T.);
#2413=FACE_OUTER_BOUND('',#3448,.T.);
#2414=FACE_OUTER_BOUND('',#3449,.T.);
#2415=FACE_OUTER_BOUND('',#3451,.T.);
#2416=FACE_OUTER_BOUND('',#3452,.T.);
#3292=EDGE_LOOP('',(#13084,#13085,#13086,#13087));
#3293=EDGE_LOOP('',(#13088,#13089,#13090,#13091));
#3294=EDGE_LOOP('',(#13092,#13093,#13094,#13095));
#3295=EDGE_LOOP('',(#13096,#13097,#13098,#13099));
#3296=EDGE_LOOP('',(#13100,#13101,#13102,#13103));
#3297=EDGE_LOOP('',(#13104,#13105,#13106,#13107));
#3298=EDGE_LOOP('',(#13108,#13109,#13110,#13111));
#3299=EDGE_LOOP('',(#13112,#13113,#13114,#13115));
#3300=EDGE_LOOP('',(#13116,#13117,#13118,#13119));
#3301=EDGE_LOOP('',(#13120,#13121,#13122,#13123));
#3302=EDGE_LOOP('',(#13124,#13125,#13126,#13127));
#3303=EDGE_LOOP('',(#13128,#13129,#13130,#13131));
#3304=EDGE_LOOP('',(#13132,#13133,#13134,#13135));
#3305=EDGE_LOOP('',(#13136,#13137,#13138));
#3306=EDGE_LOOP('',(#13139,#13140,#13141,#13142,#13143));
#3307=EDGE_LOOP('',(#13144,#13145,#13146,#13147));
#3308=EDGE_LOOP('',(#13148,#13149,#13150,#13151));
#3309=EDGE_LOOP('',(#13152,#13153,#13154,#13155));
#3310=EDGE_LOOP('',(#13156,#13157,#13158,#13159));
#3311=EDGE_LOOP('',(#13160,#13161,#13162,#13163));
#3312=EDGE_LOOP('',(#13164,#13165,#13166,#13167));
#3313=EDGE_LOOP('',(#13168,#13169,#13170,#13171));
#3314=EDGE_LOOP('',(#13172,#13173,#13174,#13175));
#3315=EDGE_LOOP('',(#13176,#13177,#13178,#13179));
#3316=EDGE_LOOP('',(#13180,#13181,#13182,#13183));
#3317=EDGE_LOOP('',(#13184,#13185,#13186,#13187));
#3318=EDGE_LOOP('',(#13188,#13189,#13190,#13191,#13192,#13193));
#3319=EDGE_LOOP('',(#13194,#13195));
#3320=EDGE_LOOP('',(#13196,#13197,#13198,#13199,#13200,#13201));
#3321=EDGE_LOOP('',(#13202,#13203,#13204,#13205,#13206,#13207,#13208,#13209,
#13210,#13211,#13212,#13213,#13214,#13215,#13216,#13217,#13218,#13219,#13220,
#13221,#13222,#13223,#13224,#13225,#13226,#13227,#13228,#13229,#13230,#13231,
#13232,#13233));
#3322=EDGE_LOOP('',(#13234,#13235,#13236,#13237));
#3323=EDGE_LOOP('',(#13238,#13239,#13240,#13241));
#3324=EDGE_LOOP('',(#13242,#13243,#13244,#13245));
#3325=EDGE_LOOP('',(#13246,#13247,#13248,#13249));
#3326=EDGE_LOOP('',(#13250,#13251,#13252,#13253));
#3327=EDGE_LOOP('',(#13254,#13255,#13256,#13257));
#3328=EDGE_LOOP('',(#13258,#13259,#13260,#13261));
#3329=EDGE_LOOP('',(#13262,#13263,#13264,#13265));
#3330=EDGE_LOOP('',(#13266,#13267,#13268,#13269));
#3331=EDGE_LOOP('',(#13270,#13271,#13272,#13273));
#3332=EDGE_LOOP('',(#13274,#13275,#13276,#13277));
#3333=EDGE_LOOP('',(#13278,#13279,#13280,#13281));
#3334=EDGE_LOOP('',(#13282,#13283,#13284,#13285));
#3335=EDGE_LOOP('',(#13286,#13287,#13288,#13289));
#3336=EDGE_LOOP('',(#13290,#13291,#13292,#13293));
#3337=EDGE_LOOP('',(#13294,#13295,#13296,#13297));
#3338=EDGE_LOOP('',(#13298,#13299,#13300,#13301));
#3339=EDGE_LOOP('',(#13302,#13303,#13304,#13305));
#3340=EDGE_LOOP('',(#13306,#13307,#13308,#13309));
#3341=EDGE_LOOP('',(#13310,#13311,#13312,#13313));
#3342=EDGE_LOOP('',(#13314,#13315,#13316,#13317));
#3343=EDGE_LOOP('',(#13318,#13319,#13320,#13321,#13322));
#3344=EDGE_LOOP('',(#13323,#13324));
#3345=EDGE_LOOP('',(#13325,#13326,#13327,#13328,#13329,#13330,#13331,#13332,
#13333,#13334,#13335,#13336,#13337,#13338,#13339,#13340,#13341,#13342,#13343,
#13344,#13345,#13346,#13347,#13348,#13349,#13350,#13351,#13352,#13353));
#3346=EDGE_LOOP('',(#13354,#13355,#13356,#13357,#13358));
#3347=EDGE_LOOP('',(#13359,#13360,#13361,#13362));
#3348=EDGE_LOOP('',(#13363,#13364,#13365,#13366,#13367,#13368,#13369,#13370,
#13371,#13372,#13373,#13374,#13375,#13376,#13377,#13378,#13379,#13380,#13381,
#13382,#13383,#13384,#13385,#13386,#13387,#13388,#13389,#13390,#13391,#13392));
#3349=EDGE_LOOP('',(#13393,#13394,#13395,#13396));
#3350=EDGE_LOOP('',(#13397,#13398,#13399,#13400,#13401,#13402,#13403,#13404,
#13405,#13406));
#3351=EDGE_LOOP('',(#13407,#13408,#13409,#13410));
#3352=EDGE_LOOP('',(#13411,#13412,#13413,#13414));
#3353=EDGE_LOOP('',(#13415,#13416,#13417,#13418));
#3354=EDGE_LOOP('',(#13419,#13420,#13421));
#3355=EDGE_LOOP('',(#13422,#13423,#13424,#13425));
#3356=EDGE_LOOP('',(#13426,#13427,#13428));
#3357=EDGE_LOOP('',(#13429,#13430,#13431,#13432));
#3358=EDGE_LOOP('',(#13433,#13434,#13435));
#3359=EDGE_LOOP('',(#13436,#13437,#13438,#13439));
#3360=EDGE_LOOP('',(#13440,#13441,#13442));
#3361=EDGE_LOOP('',(#13443,#13444,#13445,#13446));
#3362=EDGE_LOOP('',(#13447,#13448,#13449));
#3363=EDGE_LOOP('',(#13450,#13451,#13452,#13453));
#3364=EDGE_LOOP('',(#13454,#13455,#13456));
#3365=EDGE_LOOP('',(#13457,#13458,#13459,#13460));
#3366=EDGE_LOOP('',(#13461,#13462,#13463));
#3367=EDGE_LOOP('',(#13464,#13465,#13466,#13467));
#3368=EDGE_LOOP('',(#13468,#13469,#13470));
#3369=EDGE_LOOP('',(#13471,#13472,#13473,#13474));
#3370=EDGE_LOOP('',(#13475,#13476,#13477));
#3371=EDGE_LOOP('',(#13478,#13479,#13480,#13481));
#3372=EDGE_LOOP('',(#13482,#13483,#13484));
#3373=EDGE_LOOP('',(#13485,#13486,#13487,#13488));
#3374=EDGE_LOOP('',(#13489,#13490,#13491));
#3375=EDGE_LOOP('',(#13492,#13493,#13494,#13495));
#3376=EDGE_LOOP('',(#13496,#13497,#13498));
#3377=EDGE_LOOP('',(#13499,#13500,#13501,#13502));
#3378=EDGE_LOOP('',(#13503,#13504,#13505));
#3379=EDGE_LOOP('',(#13506,#13507,#13508,#13509));
#3380=EDGE_LOOP('',(#13510,#13511,#13512));
#3381=EDGE_LOOP('',(#13513,#13514,#13515,#13516));
#3382=EDGE_LOOP('',(#13517,#13518,#13519));
#3383=EDGE_LOOP('',(#13520,#13521,#13522,#13523));
#3384=EDGE_LOOP('',(#13524,#13525,#13526));
#3385=EDGE_LOOP('',(#13527,#13528,#13529,#13530));
#3386=EDGE_LOOP('',(#13531,#13532,#13533));
#3387=EDGE_LOOP('',(#13534,#13535,#13536,#13537));
#3388=EDGE_LOOP('',(#13538,#13539,#13540));
#3389=EDGE_LOOP('',(#13541,#13542,#13543,#13544));
#3390=EDGE_LOOP('',(#13545,#13546,#13547));
#3391=EDGE_LOOP('',(#13548,#13549,#13550,#13551));
#3392=EDGE_LOOP('',(#13552,#13553,#13554));
#3393=EDGE_LOOP('',(#13555,#13556,#13557,#13558));
#3394=EDGE_LOOP('',(#13559,#13560,#13561));
#3395=EDGE_LOOP('',(#13562,#13563,#13564,#13565));
#3396=EDGE_LOOP('',(#13566,#13567,#13568,#13569));
#3397=EDGE_LOOP('',(#13570,#13571,#13572,#13573));
#3398=EDGE_LOOP('',(#13574,#13575,#13576,#13577));
#3399=EDGE_LOOP('',(#13578,#13579,#13580,#13581));
#3400=EDGE_LOOP('',(#13582,#13583,#13584));
#3401=EDGE_LOOP('',(#13585,#13586,#13587,#13588));
#3402=EDGE_LOOP('',(#13589,#13590,#13591));
#3403=EDGE_LOOP('',(#13592,#13593,#13594,#13595));
#3404=EDGE_LOOP('',(#13596,#13597,#13598));
#3405=EDGE_LOOP('',(#13599,#13600,#13601,#13602));
#3406=EDGE_LOOP('',(#13603,#13604,#13605));
#3407=EDGE_LOOP('',(#13606,#13607,#13608,#13609));
#3408=EDGE_LOOP('',(#13610,#13611,#13612));
#3409=EDGE_LOOP('',(#13613,#13614,#13615,#13616));
#3410=EDGE_LOOP('',(#13617,#13618,#13619));
#3411=EDGE_LOOP('',(#13620,#13621,#13622,#13623));
#3412=EDGE_LOOP('',(#13624,#13625,#13626));
#3413=EDGE_LOOP('',(#13627,#13628,#13629,#13630));
#3414=EDGE_LOOP('',(#13631,#13632,#13633));
#3415=EDGE_LOOP('',(#13634,#13635,#13636,#13637));
#3416=EDGE_LOOP('',(#13638,#13639,#13640));
#3417=EDGE_LOOP('',(#13641,#13642,#13643,#13644));
#3418=EDGE_LOOP('',(#13645,#13646,#13647));
#3419=EDGE_LOOP('',(#13648,#13649,#13650,#13651));
#3420=EDGE_LOOP('',(#13652,#13653,#13654));
#3421=EDGE_LOOP('',(#13655,#13656,#13657,#13658));
#3422=EDGE_LOOP('',(#13659,#13660,#13661,#13662));
#3423=EDGE_LOOP('',(#13663,#13664,#13665));
#3424=EDGE_LOOP('',(#13666,#13667,#13668,#13669));
#3425=EDGE_LOOP('',(#13670,#13671,#13672));
#3426=EDGE_LOOP('',(#13673,#13674,#13675,#13676));
#3427=EDGE_LOOP('',(#13677,#13678,#13679));
#3428=EDGE_LOOP('',(#13680,#13681,#13682,#13683));
#3429=EDGE_LOOP('',(#13684,#13685,#13686));
#3430=EDGE_LOOP('',(#13687,#13688,#13689,#13690));
#3431=EDGE_LOOP('',(#13691,#13692,#13693));
#3432=EDGE_LOOP('',(#13694,#13695,#13696,#13697));
#3433=EDGE_LOOP('',(#13698,#13699,#13700));
#3434=EDGE_LOOP('',(#13701,#13702,#13703,#13704));
#3435=EDGE_LOOP('',(#13705,#13706,#13707));
#3436=EDGE_LOOP('',(#13708,#13709,#13710,#13711));
#3437=EDGE_LOOP('',(#13712,#13713,#13714));
#3438=EDGE_LOOP('',(#13715,#13716,#13717,#13718));
#3439=EDGE_LOOP('',(#13719,#13720,#13721));
#3440=EDGE_LOOP('',(#13722,#13723,#13724,#13725));
#3441=EDGE_LOOP('',(#13726,#13727,#13728));
#3442=EDGE_LOOP('',(#13729,#13730,#13731,#13732));
#3443=EDGE_LOOP('',(#13733,#13734,#13735));
#3444=EDGE_LOOP('',(#13736,#13737,#13738,#13739));
#3445=EDGE_LOOP('',(#13740,#13741,#13742));
#3446=EDGE_LOOP('',(#13743));
#3447=EDGE_LOOP('',(#13744,#13745,#13746,#13747,#13748,#13749));
#3448=EDGE_LOOP('',(#13750,#13751,#13752,#13753));
#3449=EDGE_LOOP('',(#13754));
#3450=EDGE_LOOP('',(#13755,#13756,#13757,#13758,#13759));
#3451=EDGE_LOOP('',(#13760,#13761,#13762,#13763));
#3452=EDGE_LOOP('',(#13764,#13765,#13766,#13767));
#4453=LINE('',#36662,#5764);
#4454=LINE('',#36695,#5765);
#4455=LINE('',#36779,#5766);
#4456=LINE('',#36869,#5767);
#4457=LINE('',#36959,#5768);
#4458=LINE('',#37043,#5769);
#4459=LINE('',#37133,#5770);
#4460=LINE('',#37220,#5771);
#4461=LINE('',#37307,#5772);
#4462=LINE('',#37397,#5773);
#4463=LINE('',#37481,#5774);
#4464=LINE('',#37571,#5775);
#4465=LINE('',#37661,#5776);
#4466=LINE('',#37745,#5777);
#4467=LINE('',#37755,#5778);
#4468=LINE('',#37791,#5779);
#4469=LINE('',#37828,#5780);
#4470=LINE('',#37866,#5781);
#4471=LINE('',#37903,#5782);
#4472=LINE('',#37940,#5783);
#4473=LINE('',#37978,#5784);
#4474=LINE('',#38014,#5785);
#4475=LINE('',#38052,#5786);
#4476=LINE('',#38089,#5787);
#4477=LINE('',#38126,#5788);
#4478=LINE('',#38164,#5789);
#4479=LINE('',#38205,#5790);
#4480=LINE('',#38213,#5791);
#4481=LINE('',#38224,#5792);
#4482=LINE('',#38232,#5793);
#4483=LINE('',#38237,#5794);
#4484=LINE('',#38241,#5795);
#4485=LINE('',#38245,#5796);
#4486=LINE('',#38248,#5797);
#4487=LINE('',#38252,#5798);
#4488=LINE('',#38256,#5799);
#4489=LINE('',#38260,#5800);
#4490=LINE('',#38265,#5801);
#4491=LINE('',#38269,#5802);
#4492=LINE('',#38273,#5803);
#4493=LINE('',#38277,#5804);
#4494=LINE('',#38280,#5805);
#4495=LINE('',#38283,#5806);
#4496=LINE('',#38287,#5807);
#4497=LINE('',#38291,#5808);
#4498=LINE('',#38295,#5809);
#4499=LINE('',#38299,#5810);
#4500=LINE('',#38303,#5811);
#4501=LINE('',#38307,#5812);
#4502=LINE('',#38311,#5813);
#4503=LINE('',#38315,#5814);
#4504=LINE('',#38319,#5815);
#4505=LINE('',#38323,#5816);
#4506=LINE('',#38327,#5817);
#4507=LINE('',#38331,#5818);
#4508=LINE('',#38335,#5819);
#4509=LINE('',#38339,#5820);
#4510=LINE('',#38343,#5821);
#4511=LINE('',#38347,#5822);
#4512=LINE('',#38351,#5823);
#4513=LINE('',#38355,#5824);
#4514=LINE('',#38359,#5825);
#4515=LINE('',#38363,#5826);
#4516=LINE('',#38367,#5827);
#4517=LINE('',#38371,#5828);
#4518=LINE('',#38375,#5829);
#4519=LINE('',#38379,#5830);
#4520=LINE('',#38383,#5831);
#4521=LINE('',#38387,#5832);
#4522=LINE('',#38391,#5833);
#4523=LINE('',#38395,#5834);
#4524=LINE('',#38399,#5835);
#4525=LINE('',#38403,#5836);
#4526=LINE('',#38407,#5837);
#4527=LINE('',#38411,#5838);
#4528=LINE('',#38415,#5839);
#4529=LINE('',#38419,#5840);
#4530=LINE('',#38423,#5841);
#4531=LINE('',#38427,#5842);
#4532=LINE('',#38431,#5843);
#4533=LINE('',#38435,#5844);
#4534=LINE('',#38439,#5845);
#4535=LINE('',#38443,#5846);
#4536=LINE('',#38447,#5847);
#4537=LINE('',#40269,#5848);
#4538=LINE('',#40271,#5849);
#4539=LINE('',#40273,#5850);
#4540=LINE('',#40274,#5851);
#4541=LINE('',#40276,#5852);
#4542=LINE('',#40277,#5853);
#4543=LINE('',#40281,#5854);
#4544=LINE('',#40282,#5855);
#4545=LINE('',#40285,#5856);
#4546=LINE('',#40287,#5857);
#4547=LINE('',#40288,#5858);
#4548=LINE('',#40290,#5859);
#4549=LINE('',#40292,#5860);
#4550=LINE('',#40296,#5861);
#4551=LINE('',#40298,#5862);
#4552=LINE('',#40299,#5863);
#4553=LINE('',#40301,#5864);
#4554=LINE('',#40303,#5865);
#4555=LINE('',#40307,#5866);
#4556=LINE('',#40309,#5867);
#4557=LINE('',#40310,#5868);
#4558=LINE('',#40312,#5869);
#4559=LINE('',#40314,#5870);
#4560=LINE('',#40318,#5871);
#4561=LINE('',#40320,#5872);
#4562=LINE('',#40321,#5873);
#4563=LINE('',#40323,#5874);
#4564=LINE('',#40325,#5875);
#4565=LINE('',#40329,#5876);
#4566=LINE('',#40331,#5877);
#4567=LINE('',#40332,#5878);
#4568=LINE('',#40334,#5879);
#4569=LINE('',#40336,#5880);
#4570=LINE('',#40339,#5881);
#4571=LINE('',#40343,#5882);
#4572=LINE('',#40345,#5883);
#4573=LINE('',#40346,#5884);
#4574=LINE('',#40348,#5885);
#4575=LINE('',#40350,#5886);
#4576=LINE('',#40354,#5887);
#4577=LINE('',#40356,#5888);
#4578=LINE('',#40357,#5889);
#4579=LINE('',#40359,#5890);
#4580=LINE('',#40361,#5891);
#4581=LINE('',#40365,#5892);
#4582=LINE('',#40367,#5893);
#4583=LINE('',#40368,#5894);
#4584=LINE('',#40370,#5895);
#4585=LINE('',#40372,#5896);
#4586=LINE('',#40376,#5897);
#4587=LINE('',#40378,#5898);
#4588=LINE('',#40379,#5899);
#4589=LINE('',#40381,#5900);
#4590=LINE('',#40383,#5901);
#4591=LINE('',#40387,#5902);
#4592=LINE('',#40389,#5903);
#4593=LINE('',#40390,#5904);
#4594=LINE('',#40392,#5905);
#4595=LINE('',#40394,#5906);
#4596=LINE('',#40398,#5907);
#4597=LINE('',#40400,#5908);
#4598=LINE('',#40401,#5909);
#4599=LINE('',#40403,#5910);
#4600=LINE('',#40405,#5911);
#4601=LINE('',#40409,#5912);
#4602=LINE('',#40411,#5913);
#4603=LINE('',#40412,#5914);
#4604=LINE('',#40414,#5915);
#4605=LINE('',#40416,#5916);
#4606=LINE('',#40420,#5917);
#4607=LINE('',#40422,#5918);
#4608=LINE('',#40423,#5919);
#4609=LINE('',#40425,#5920);
#4610=LINE('',#40427,#5921);
#4611=LINE('',#40431,#5922);
#4612=LINE('',#40433,#5923);
#4613=LINE('',#40434,#5924);
#4614=LINE('',#40436,#5925);
#4615=LINE('',#40438,#5926);
#4616=LINE('',#40442,#5927);
#4617=LINE('',#40444,#5928);
#4618=LINE('',#40445,#5929);
#4619=LINE('',#40447,#5930);
#4620=LINE('',#40449,#5931);
#4621=LINE('',#40453,#5932);
#4622=LINE('',#40455,#5933);
#4623=LINE('',#40456,#5934);
#4624=LINE('',#40458,#5935);
#4625=LINE('',#40460,#5936);
#4626=LINE('',#40464,#5937);
#4627=LINE('',#40465,#5938);
#4628=LINE('',#40467,#5939);
#4629=LINE('',#40471,#5940);
#4630=LINE('',#40473,#5941);
#4631=LINE('',#40474,#5942);
#4632=LINE('',#40476,#5943);
#4633=LINE('',#40478,#5944);
#4634=LINE('',#40482,#5945);
#4635=LINE('',#40484,#5946);
#4636=LINE('',#40485,#5947);
#4637=LINE('',#40487,#5948);
#4638=LINE('',#40489,#5949);
#4639=LINE('',#40493,#5950);
#4640=LINE('',#40495,#5951);
#4641=LINE('',#40496,#5952);
#4642=LINE('',#40498,#5953);
#4643=LINE('',#40500,#5954);
#4644=LINE('',#40504,#5955);
#4645=LINE('',#40506,#5956);
#4646=LINE('',#40507,#5957);
#4647=LINE('',#40509,#5958);
#4648=LINE('',#40511,#5959);
#4649=LINE('',#40515,#5960);
#4650=LINE('',#40517,#5961);
#4651=LINE('',#40518,#5962);
#4652=LINE('',#40520,#5963);
#4653=LINE('',#40522,#5964);
#4654=LINE('',#40526,#5965);
#4655=LINE('',#40528,#5966);
#4656=LINE('',#40529,#5967);
#4657=LINE('',#40531,#5968);
#4658=LINE('',#40533,#5969);
#4659=LINE('',#40539,#5970);
#4660=LINE('',#40546,#5971);
#5764=VECTOR('',#19862,5.);
#5765=VECTOR('',#19867,5.);
#5766=VECTOR('',#19870,5.);
#5767=VECTOR('',#19873,5.);
#5768=VECTOR('',#19876,5.);
#5769=VECTOR('',#19879,5.);
#5770=VECTOR('',#19882,5.);
#5771=VECTOR('',#19885,5.);
#5772=VECTOR('',#19888,5.);
#5773=VECTOR('',#19891,5.);
#5774=VECTOR('',#19894,5.);
#5775=VECTOR('',#19897,5.);
#5776=VECTOR('',#19900,5.);
#5777=VECTOR('',#19903,4.372);
#5778=VECTOR('',#19908,4.372);
#5779=VECTOR('',#19913,4.372);
#5780=VECTOR('',#19916,4.372);
#5781=VECTOR('',#19919,4.372);
#5782=VECTOR('',#19922,4.372);
#5783=VECTOR('',#19925,4.372);
#5784=VECTOR('',#19928,4.372);
#5785=VECTOR('',#19931,4.372);
#5786=VECTOR('',#19934,4.372);
#5787=VECTOR('',#19937,4.372);
#5788=VECTOR('',#19940,4.372);
#5789=VECTOR('',#19943,4.372);
#5790=VECTOR('',#19946,10.);
#5791=VECTOR('',#19949,10.);
#5792=VECTOR('',#19958,10.);
#5793=VECTOR('',#19961,10.);
#5794=VECTOR('',#19968,10.);
#5795=VECTOR('',#19971,10.);
#5796=VECTOR('',#19974,10.);
#5797=VECTOR('',#19977,10.);
#5798=VECTOR('',#19980,7.);
#5799=VECTOR('',#19983,10.);
#5800=VECTOR('',#19986,7.);
#5801=VECTOR('',#19991,10.);
#5802=VECTOR('',#19996,10.);
#5803=VECTOR('',#19999,10.);
#5804=VECTOR('',#20002,10.);
#5805=VECTOR('',#20005,10.);
#5806=VECTOR('',#20006,10.);
#5807=VECTOR('',#20009,10.);
#5808=VECTOR('',#20012,10.);
#5809=VECTOR('',#20015,10.);
#5810=VECTOR('',#20018,10.);
#5811=VECTOR('',#20021,10.);
#5812=VECTOR('',#20024,10.);
#5813=VECTOR('',#20027,10.);
#5814=VECTOR('',#20030,10.);
#5815=VECTOR('',#20033,10.);
#5816=VECTOR('',#20036,10.);
#5817=VECTOR('',#20039,10.);
#5818=VECTOR('',#20042,10.);
#5819=VECTOR('',#20045,10.);
#5820=VECTOR('',#20048,10.);
#5821=VECTOR('',#20051,10.);
#5822=VECTOR('',#20054,10.);
#5823=VECTOR('',#20057,10.);
#5824=VECTOR('',#20060,10.);
#5825=VECTOR('',#20063,10.);
#5826=VECTOR('',#20066,10.);
#5827=VECTOR('',#20069,10.);
#5828=VECTOR('',#20072,10.);
#5829=VECTOR('',#20075,10.);
#5830=VECTOR('',#20078,10.);
#5831=VECTOR('',#20081,10.);
#5832=VECTOR('',#20084,10.);
#5833=VECTOR('',#20087,10.);
#5834=VECTOR('',#20090,10.);
#5835=VECTOR('',#20093,10.);
#5836=VECTOR('',#20096,10.);
#5837=VECTOR('',#20099,10.);
#5838=VECTOR('',#20102,10.);
#5839=VECTOR('',#20105,10.);
#5840=VECTOR('',#20108,10.);
#5841=VECTOR('',#20111,10.);
#5842=VECTOR('',#20114,10.);
#5843=VECTOR('',#20117,10.);
#5844=VECTOR('',#20120,10.);
#5845=VECTOR('',#20123,10.);
#5846=VECTOR('',#20126,10.);
#5847=VECTOR('',#20129,10.);
#5848=VECTOR('',#20150,10.);
#5849=VECTOR('',#20153,10.);
#5850=VECTOR('',#20154,10.);
#5851=VECTOR('',#20155,10.);
#5852=VECTOR('',#20156,10.);
#5853=VECTOR('',#20157,10.);
#5854=VECTOR('',#20162,10.);
#5855=VECTOR('',#20163,10.);
#5856=VECTOR('',#20166,10.);
#5857=VECTOR('',#20167,10.);
#5858=VECTOR('',#20168,10.);
#5859=VECTOR('',#20171,10.);
#5860=VECTOR('',#20174,10.);
#5861=VECTOR('',#20179,10.);
#5862=VECTOR('',#20180,10.);
#5863=VECTOR('',#20181,10.);
#5864=VECTOR('',#20184,10.);
#5865=VECTOR('',#20187,10.);
#5866=VECTOR('',#20192,10.);
#5867=VECTOR('',#20193,10.);
#5868=VECTOR('',#20194,10.);
#5869=VECTOR('',#20197,10.);
#5870=VECTOR('',#20200,10.);
#5871=VECTOR('',#20205,10.);
#5872=VECTOR('',#20206,10.);
#5873=VECTOR('',#20207,10.);
#5874=VECTOR('',#20210,10.);
#5875=VECTOR('',#20213,10.);
#5876=VECTOR('',#20218,10.);
#5877=VECTOR('',#20219,10.);
#5878=VECTOR('',#20220,10.);
#5879=VECTOR('',#20223,10.);
#5880=VECTOR('',#20226,10.);
#5881=VECTOR('',#20231,10.);
#5882=VECTOR('',#20236,10.);
#5883=VECTOR('',#20237,10.);
#5884=VECTOR('',#20238,10.);
#5885=VECTOR('',#20241,10.);
#5886=VECTOR('',#20244,10.);
#5887=VECTOR('',#20249,10.);
#5888=VECTOR('',#20250,10.);
#5889=VECTOR('',#20251,10.);
#5890=VECTOR('',#20254,10.);
#5891=VECTOR('',#20257,10.);
#5892=VECTOR('',#20262,10.);
#5893=VECTOR('',#20263,10.);
#5894=VECTOR('',#20264,10.);
#5895=VECTOR('',#20267,10.);
#5896=VECTOR('',#20270,10.);
#5897=VECTOR('',#20275,10.);
#5898=VECTOR('',#20276,10.);
#5899=VECTOR('',#20277,10.);
#5900=VECTOR('',#20280,10.);
#5901=VECTOR('',#20283,10.);
#5902=VECTOR('',#20288,10.);
#5903=VECTOR('',#20289,10.);
#5904=VECTOR('',#20290,10.);
#5905=VECTOR('',#20293,10.);
#5906=VECTOR('',#20296,10.);
#5907=VECTOR('',#20301,10.);
#5908=VECTOR('',#20302,10.);
#5909=VECTOR('',#20303,10.);
#5910=VECTOR('',#20306,10.);
#5911=VECTOR('',#20309,10.);
#5912=VECTOR('',#20314,10.);
#5913=VECTOR('',#20315,10.);
#5914=VECTOR('',#20316,10.);
#5915=VECTOR('',#20319,10.);
#5916=VECTOR('',#20322,10.);
#5917=VECTOR('',#20327,10.);
#5918=VECTOR('',#20328,10.);
#5919=VECTOR('',#20329,10.);
#5920=VECTOR('',#20332,10.);
#5921=VECTOR('',#20335,10.);
#5922=VECTOR('',#20340,10.);
#5923=VECTOR('',#20341,10.);
#5924=VECTOR('',#20342,10.);
#5925=VECTOR('',#20345,10.);
#5926=VECTOR('',#20348,10.);
#5927=VECTOR('',#20353,10.);
#5928=VECTOR('',#20354,10.);
#5929=VECTOR('',#20355,10.);
#5930=VECTOR('',#20358,10.);
#5931=VECTOR('',#20361,10.);
#5932=VECTOR('',#20366,10.);
#5933=VECTOR('',#20367,10.);
#5934=VECTOR('',#20368,10.);
#5935=VECTOR('',#20371,10.);
#5936=VECTOR('',#20374,10.);
#5937=VECTOR('',#20379,10.);
#5938=VECTOR('',#20380,10.);
#5939=VECTOR('',#20383,10.);
#5940=VECTOR('',#20388,10.);
#5941=VECTOR('',#20389,10.);
#5942=VECTOR('',#20390,10.);
#5943=VECTOR('',#20393,10.);
#5944=VECTOR('',#20396,10.);
#5945=VECTOR('',#20401,10.);
#5946=VECTOR('',#20402,10.);
#5947=VECTOR('',#20403,10.);
#5948=VECTOR('',#20406,10.);
#5949=VECTOR('',#20409,10.);
#5950=VECTOR('',#20414,10.);
#5951=VECTOR('',#20415,10.);
#5952=VECTOR('',#20416,10.);
#5953=VECTOR('',#20419,10.);
#5954=VECTOR('',#20422,10.);
#5955=VECTOR('',#20427,10.);
#5956=VECTOR('',#20428,10.);
#5957=VECTOR('',#20429,10.);
#5958=VECTOR('',#20432,10.);
#5959=VECTOR('',#20435,10.);
#5960=VECTOR('',#20440,10.);
#5961=VECTOR('',#20441,10.);
#5962=VECTOR('',#20442,10.);
#5963=VECTOR('',#20445,10.);
#5964=VECTOR('',#20448,10.);
#5965=VECTOR('',#20453,10.);
#5966=VECTOR('',#20454,10.);
#5967=VECTOR('',#20455,10.);
#5968=VECTOR('',#20458,10.);
#5969=VECTOR('',#20461,10.);
#5970=VECTOR('',#20470,4.8);
#5971=VECTOR('',#20481,6.8);
#6707=CIRCLE('',#17344,4.942);
#6708=CIRCLE('',#17358,4.372);
#6709=CIRCLE('',#17360,4.372);
#6710=CIRCLE('',#17376,6.6);
#6711=CIRCLE('',#17381,7.);
#6712=CIRCLE('',#17382,7.);
#6713=CIRCLE('',#17383,7.);
#6714=CIRCLE('',#17384,7.);
#6715=CIRCLE('',#17385,7.);
#6716=CIRCLE('',#17386,7.);
#6717=CIRCLE('',#17387,7.);
#6718=CIRCLE('',#17388,7.);
#6719=CIRCLE('',#17389,7.);
#6720=CIRCLE('',#17390,7.);
#6721=CIRCLE('',#17391,7.);
#6722=CIRCLE('',#17392,7.);
#6723=CIRCLE('',#17393,7.);
#6724=CIRCLE('',#17394,7.);
#6725=CIRCLE('',#17395,7.);
#6726=CIRCLE('',#17396,7.);
#6727=CIRCLE('',#17397,7.);
#6728=CIRCLE('',#17398,7.);
#6729=CIRCLE('',#17399,7.);
#6730=CIRCLE('',#17400,7.);
#6731=CIRCLE('',#17401,7.);
#6732=CIRCLE('',#17402,7.);
#6733=CIRCLE('',#17403,7.);
#6734=CIRCLE('',#17404,7.);
#6735=CIRCLE('',#17405,7.);
#6736=CIRCLE('',#17406,7.);
#6737=CIRCLE('',#17407,7.);
#6738=CIRCLE('',#17408,7.);
#6739=CIRCLE('',#17409,7.);
#6740=CIRCLE('',#17410,7.);
#6741=CIRCLE('',#17411,7.);
#6742=CIRCLE('',#17412,7.);
#6743=CIRCLE('',#17413,7.);
#6744=CIRCLE('',#17414,7.);
#6745=CIRCLE('',#17415,7.);
#6746=CIRCLE('',#17416,7.);
#6747=CIRCLE('',#17417,7.);
#6748=CIRCLE('',#17418,7.);
#6749=CIRCLE('',#17419,7.);
#6750=CIRCLE('',#17420,7.);
#6751=CIRCLE('',#17421,7.);
#6752=CIRCLE('',#17422,7.);
#6753=CIRCLE('',#17423,7.);
#6754=CIRCLE('',#17424,7.);
#6755=CIRCLE('',#17425,7.);
#6756=CIRCLE('',#17426,7.);
#6757=CIRCLE('',#17427,7.);
#6758=CIRCLE('',#17428,7.);
#6759=CIRCLE('',#17429,7.);
#6760=CIRCLE('',#17430,7.);
#6761=CIRCLE('',#17431,7.);
#6762=CIRCLE('',#17432,7.);
#6763=CIRCLE('',#17433,7.);
#6764=CIRCLE('',#17434,7.);
#6765=CIRCLE('',#17435,7.);
#6766=CIRCLE('',#17436,7.);
#6767=CIRCLE('',#17438,6.6);
#6768=CIRCLE('',#17441,4.942);
#6769=CIRCLE('',#17442,4.942);
#6770=CIRCLE('',#17443,4.372);
#6771=CIRCLE('',#17543,4.6);
#6772=CIRCLE('',#17546,4.942);
#6773=CIRCLE('',#17548,6.6);
#7689=VERTEX_POINT('',#36660);
#7690=VERTEX_POINT('',#36661);
#7691=VERTEX_POINT('',#36663);
#7692=VERTEX_POINT('',#36680);
#7693=VERTEX_POINT('',#36693);
#7694=VERTEX_POINT('',#36694);
#7695=VERTEX_POINT('',#36777);
#7696=VERTEX_POINT('',#36778);
#7697=VERTEX_POINT('',#36867);
#7698=VERTEX_POINT('',#36868);
#7699=VERTEX_POINT('',#36957);
#7700=VERTEX_POINT('',#36958);
#7701=VERTEX_POINT('',#37041);
#7702=VERTEX_POINT('',#37042);
#7703=VERTEX_POINT('',#37131);
#7704=VERTEX_POINT('',#37132);
#7705=VERTEX_POINT('',#37218);
#7706=VERTEX_POINT('',#37219);
#7707=VERTEX_POINT('',#37305);
#7708=VERTEX_POINT('',#37306);
#7709=VERTEX_POINT('',#37395);
#7710=VERTEX_POINT('',#37396);
#7711=VERTEX_POINT('',#37479);
#7712=VERTEX_POINT('',#37480);
#7713=VERTEX_POINT('',#37569);
#7714=VERTEX_POINT('',#37570);
#7715=VERTEX_POINT('',#37659);
#7716=VERTEX_POINT('',#37660);
#7717=VERTEX_POINT('',#37743);
#7718=VERTEX_POINT('',#37744);
#7719=VERTEX_POINT('',#37746);
#7720=VERTEX_POINT('',#37753);
#7721=VERTEX_POINT('',#37754);
#7722=VERTEX_POINT('',#37772);
#7723=VERTEX_POINT('',#37789);
#7724=VERTEX_POINT('',#37790);
#7725=VERTEX_POINT('',#37826);
#7726=VERTEX_POINT('',#37827);
#7727=VERTEX_POINT('',#37864);
#7728=VERTEX_POINT('',#37865);
#7729=VERTEX_POINT('',#37901);
#7730=VERTEX_POINT('',#37902);
#7731=VERTEX_POINT('',#37938);
#7732=VERTEX_POINT('',#37939);
#7733=VERTEX_POINT('',#37976);
#7734=VERTEX_POINT('',#37977);
#7735=VERTEX_POINT('',#38012);
#7736=VERTEX_POINT('',#38013);
#7737=VERTEX_POINT('',#38050);
#7738=VERTEX_POINT('',#38051);
#7739=VERTEX_POINT('',#38087);
#7740=VERTEX_POINT('',#38088);
#7741=VERTEX_POINT('',#38124);
#7742=VERTEX_POINT('',#38125);
#7743=VERTEX_POINT('',#38162);
#7744=VERTEX_POINT('',#38163);
#7745=VERTEX_POINT('',#38199);
#7746=VERTEX_POINT('',#38200);
#7747=VERTEX_POINT('',#38204);
#7748=VERTEX_POINT('',#38206);
#7749=VERTEX_POINT('',#38210);
#7750=VERTEX_POINT('',#38212);
#7751=VERTEX_POINT('',#38218);
#7752=VERTEX_POINT('',#38219);
#7753=VERTEX_POINT('',#38223);
#7754=VERTEX_POINT('',#38225);
#7755=VERTEX_POINT('',#38229);
#7756=VERTEX_POINT('',#38231);
#7757=VERTEX_POINT('',#38236);
#7758=VERTEX_POINT('',#38238);
#7759=VERTEX_POINT('',#38240);
#7760=VERTEX_POINT('',#38242);
#7761=VERTEX_POINT('',#38244);
#7762=VERTEX_POINT('',#38246);
#7763=VERTEX_POINT('',#38249);
#7764=VERTEX_POINT('',#38251);
#7765=VERTEX_POINT('',#38253);
#7766=VERTEX_POINT('',#38255);
#7767=VERTEX_POINT('',#38257);
#7768=VERTEX_POINT('',#38259);
#7769=VERTEX_POINT('',#38262);
#7770=VERTEX_POINT('',#38264);
#7771=VERTEX_POINT('',#38268);
#7772=VERTEX_POINT('',#38270);
#7773=VERTEX_POINT('',#38272);
#7774=VERTEX_POINT('',#38274);
#7775=VERTEX_POINT('',#38276);
#7776=VERTEX_POINT('',#38278);
#7777=VERTEX_POINT('',#38281);
#7778=VERTEX_POINT('',#38282);
#7779=VERTEX_POINT('',#38284);
#7780=VERTEX_POINT('',#38286);
#7781=VERTEX_POINT('',#38289);
#7782=VERTEX_POINT('',#38290);
#7783=VERTEX_POINT('',#38292);
#7784=VERTEX_POINT('',#38294);
#7785=VERTEX_POINT('',#38297);
#7786=VERTEX_POINT('',#38298);
#7787=VERTEX_POINT('',#38300);
#7788=VERTEX_POINT('',#38302);
#7789=VERTEX_POINT('',#38305);
#7790=VERTEX_POINT('',#38306);
#7791=VERTEX_POINT('',#38308);
#7792=VERTEX_POINT('',#38310);
#7793=VERTEX_POINT('',#38313);
#7794=VERTEX_POINT('',#38314);
#7795=VERTEX_POINT('',#38316);
#7796=VERTEX_POINT('',#38318);
#7797=VERTEX_POINT('',#38321);
#7798=VERTEX_POINT('',#38322);
#7799=VERTEX_POINT('',#38324);
#7800=VERTEX_POINT('',#38326);
#7801=VERTEX_POINT('',#38329);
#7802=VERTEX_POINT('',#38330);
#7803=VERTEX_POINT('',#38332);
#7804=VERTEX_POINT('',#38334);
#7805=VERTEX_POINT('',#38337);
#7806=VERTEX_POINT('',#38338);
#7807=VERTEX_POINT('',#38340);
#7808=VERTEX_POINT('',#38342);
#7809=VERTEX_POINT('',#38345);
#7810=VERTEX_POINT('',#38346);
#7811=VERTEX_POINT('',#38348);
#7812=VERTEX_POINT('',#38350);
#7813=VERTEX_POINT('',#38353);
#7814=VERTEX_POINT('',#38354);
#7815=VERTEX_POINT('',#38356);
#7816=VERTEX_POINT('',#38358);
#7817=VERTEX_POINT('',#38361);
#7818=VERTEX_POINT('',#38362);
#7819=VERTEX_POINT('',#38364);
#7820=VERTEX_POINT('',#38366);
#7821=VERTEX_POINT('',#38369);
#7822=VERTEX_POINT('',#38370);
#7823=VERTEX_POINT('',#38372);
#7824=VERTEX_POINT('',#38374);
#7825=VERTEX_POINT('',#38377);
#7826=VERTEX_POINT('',#38378);
#7827=VERTEX_POINT('',#38380);
#7828=VERTEX_POINT('',#38382);
#7829=VERTEX_POINT('',#38385);
#7830=VERTEX_POINT('',#38386);
#7831=VERTEX_POINT('',#38388);
#7832=VERTEX_POINT('',#38390);
#7833=VERTEX_POINT('',#38393);
#7834=VERTEX_POINT('',#38394);
#7835=VERTEX_POINT('',#38396);
#7836=VERTEX_POINT('',#38398);
#7837=VERTEX_POINT('',#38401);
#7838=VERTEX_POINT('',#38402);
#7839=VERTEX_POINT('',#38404);
#7840=VERTEX_POINT('',#38406);
#7841=VERTEX_POINT('',#38409);
#7842=VERTEX_POINT('',#38410);
#7843=VERTEX_POINT('',#38412);
#7844=VERTEX_POINT('',#38414);
#7845=VERTEX_POINT('',#38417);
#7846=VERTEX_POINT('',#38418);
#7847=VERTEX_POINT('',#38420);
#7848=VERTEX_POINT('',#38422);
#7849=VERTEX_POINT('',#38425);
#7850=VERTEX_POINT('',#38426);
#7851=VERTEX_POINT('',#38428);
#7852=VERTEX_POINT('',#38430);
#7853=VERTEX_POINT('',#38433);
#7854=VERTEX_POINT('',#38434);
#7855=VERTEX_POINT('',#38436);
#7856=VERTEX_POINT('',#38438);
#7857=VERTEX_POINT('',#38441);
#7858=VERTEX_POINT('',#38442);
#7859=VERTEX_POINT('',#38444);
#7860=VERTEX_POINT('',#38446);
#7861=VERTEX_POINT('',#39120);
#7862=VERTEX_POINT('',#39243);
#7863=VERTEX_POINT('',#39362);
#7864=VERTEX_POINT('',#39365);
#7865=VERTEX_POINT('',#40148);
#7866=VERTEX_POINT('',#40272);
#7867=VERTEX_POINT('',#40275);
#7868=VERTEX_POINT('',#40280);
#7869=VERTEX_POINT('',#40284);
#7870=VERTEX_POINT('',#40286);
#7871=VERTEX_POINT('',#40295);
#7872=VERTEX_POINT('',#40297);
#7873=VERTEX_POINT('',#40306);
#7874=VERTEX_POINT('',#40308);
#7875=VERTEX_POINT('',#40317);
#7876=VERTEX_POINT('',#40319);
#7877=VERTEX_POINT('',#40328);
#7878=VERTEX_POINT('',#40330);
#7879=VERTEX_POINT('',#40342);
#7880=VERTEX_POINT('',#40344);
#7881=VERTEX_POINT('',#40353);
#7882=VERTEX_POINT('',#40355);
#7883=VERTEX_POINT('',#40364);
#7884=VERTEX_POINT('',#40366);
#7885=VERTEX_POINT('',#40375);
#7886=VERTEX_POINT('',#40377);
#7887=VERTEX_POINT('',#40386);
#7888=VERTEX_POINT('',#40388);
#7889=VERTEX_POINT('',#40397);
#7890=VERTEX_POINT('',#40399);
#7891=VERTEX_POINT('',#40408);
#7892=VERTEX_POINT('',#40410);
#7893=VERTEX_POINT('',#40419);
#7894=VERTEX_POINT('',#40421);
#7895=VERTEX_POINT('',#40430);
#7896=VERTEX_POINT('',#40432);
#7897=VERTEX_POINT('',#40441);
#7898=VERTEX_POINT('',#40443);
#7899=VERTEX_POINT('',#40452);
#7900=VERTEX_POINT('',#40454);
#7901=VERTEX_POINT('',#40463);
#7902=VERTEX_POINT('',#40470);
#7903=VERTEX_POINT('',#40472);
#7904=VERTEX_POINT('',#40481);
#7905=VERTEX_POINT('',#40483);
#7906=VERTEX_POINT('',#40492);
#7907=VERTEX_POINT('',#40494);
#7908=VERTEX_POINT('',#40503);
#7909=VERTEX_POINT('',#40505);
#7910=VERTEX_POINT('',#40514);
#7911=VERTEX_POINT('',#40516);
#7912=VERTEX_POINT('',#40525);
#7913=VERTEX_POINT('',#40527);
#7914=VERTEX_POINT('',#40536);
#7915=VERTEX_POINT('',#40543);
#9605=EDGE_CURVE('',#7689,#7690,#4453,.T.);
#9606=EDGE_CURVE('',#7689,#7691,#629,.T.);
#9607=EDGE_CURVE('',#7691,#7692,#6707,.T.);
#9608=EDGE_CURVE('',#7692,#7690,#630,.T.);
#9609=EDGE_CURVE('',#7693,#7694,#4454,.T.);
#9610=EDGE_CURVE('',#7693,#7689,#631,.T.);
#9611=EDGE_CURVE('',#7690,#7694,#632,.T.);
#9612=EDGE_CURVE('',#7695,#7696,#4455,.T.);
#9613=EDGE_CURVE('',#7695,#7693,#633,.T.);
#9614=EDGE_CURVE('',#7694,#7696,#634,.T.);
#9615=EDGE_CURVE('',#7697,#7698,#4456,.T.);
#9616=EDGE_CURVE('',#7697,#7695,#635,.T.);
#9617=EDGE_CURVE('',#7696,#7698,#636,.T.);
#9618=EDGE_CURVE('',#7699,#7700,#4457,.T.);
#9619=EDGE_CURVE('',#7699,#7697,#637,.T.);
#9620=EDGE_CURVE('',#7698,#7700,#638,.T.);
#9621=EDGE_CURVE('',#7701,#7702,#4458,.T.);
#9622=EDGE_CURVE('',#7701,#7699,#639,.T.);
#9623=EDGE_CURVE('',#7700,#7702,#640,.T.);
#9624=EDGE_CURVE('',#7703,#7704,#4459,.T.);
#9625=EDGE_CURVE('',#7703,#7701,#641,.T.);
#9626=EDGE_CURVE('',#7702,#7704,#642,.T.);
#9627=EDGE_CURVE('',#7705,#7706,#4460,.T.);
#9628=EDGE_CURVE('',#7705,#7703,#643,.T.);
#9629=EDGE_CURVE('',#7704,#7706,#644,.T.);
#9630=EDGE_CURVE('',#7707,#7708,#4461,.T.);
#9631=EDGE_CURVE('',#7707,#7705,#645,.T.);
#9632=EDGE_CURVE('',#7706,#7708,#646,.T.);
#9633=EDGE_CURVE('',#7709,#7710,#4462,.T.);
#9634=EDGE_CURVE('',#7709,#7707,#647,.T.);
#9635=EDGE_CURVE('',#7708,#7710,#648,.T.);
#9636=EDGE_CURVE('',#7711,#7712,#4463,.T.);
#9637=EDGE_CURVE('',#7711,#7709,#649,.T.);
#9638=EDGE_CURVE('',#7710,#7712,#650,.T.);
#9639=EDGE_CURVE('',#7713,#7714,#4464,.T.);
#9640=EDGE_CURVE('',#7713,#7711,#651,.T.);
#9641=EDGE_CURVE('',#7712,#7714,#652,.T.);
#9642=EDGE_CURVE('',#7715,#7716,#4465,.T.);
#9643=EDGE_CURVE('',#7715,#7713,#653,.T.);
#9644=EDGE_CURVE('',#7714,#7716,#654,.T.);
#9645=EDGE_CURVE('',#7717,#7718,#4466,.T.);
#9646=EDGE_CURVE('',#7717,#7719,#655,.T.);
#9647=EDGE_CURVE('',#7718,#7719,#6708,.T.);
#9648=EDGE_CURVE('',#7720,#7721,#4467,.T.);
#9649=EDGE_CURVE('',#7720,#7717,#656,.T.);
#9650=EDGE_CURVE('',#7722,#7718,#6709,.T.);
#9651=EDGE_CURVE('',#7721,#7722,#657,.T.);
#9652=EDGE_CURVE('',#7723,#7724,#4468,.T.);
#9653=EDGE_CURVE('',#7723,#7720,#658,.T.);
#9654=EDGE_CURVE('',#7724,#7721,#659,.T.);
#9655=EDGE_CURVE('',#7725,#7726,#4469,.T.);
#9656=EDGE_CURVE('',#7725,#7723,#660,.T.);
#9657=EDGE_CURVE('',#7726,#7724,#661,.T.);
#9658=EDGE_CURVE('',#7727,#7728,#4470,.T.);
#9659=EDGE_CURVE('',#7727,#7725,#662,.T.);
#9660=EDGE_CURVE('',#7728,#7726,#663,.T.);
#9661=EDGE_CURVE('',#7729,#7730,#4471,.T.);
#9662=EDGE_CURVE('',#7729,#7727,#664,.T.);
#9663=EDGE_CURVE('',#7730,#7728,#665,.T.);
#9664=EDGE_CURVE('',#7731,#7732,#4472,.T.);
#9665=EDGE_CURVE('',#7731,#7729,#666,.T.);
#9666=EDGE_CURVE('',#7732,#7730,#667,.T.);
#9667=EDGE_CURVE('',#7733,#7734,#4473,.T.);
#9668=EDGE_CURVE('',#7733,#7731,#668,.T.);
#9669=EDGE_CURVE('',#7734,#7732,#669,.T.);
#9670=EDGE_CURVE('',#7735,#7736,#4474,.T.);
#9671=EDGE_CURVE('',#7735,#7733,#670,.T.);
#9672=EDGE_CURVE('',#7736,#7734,#671,.T.);
#9673=EDGE_CURVE('',#7737,#7738,#4475,.T.);
#9674=EDGE_CURVE('',#7737,#7735,#672,.T.);
#9675=EDGE_CURVE('',#7738,#7736,#673,.T.);
#9676=EDGE_CURVE('',#7739,#7740,#4476,.T.);
#9677=EDGE_CURVE('',#7739,#7737,#674,.T.);
#9678=EDGE_CURVE('',#7740,#7738,#675,.T.);
#9679=EDGE_CURVE('',#7741,#7742,#4477,.T.);
#9680=EDGE_CURVE('',#7741,#7739,#676,.T.);
#9681=EDGE_CURVE('',#7742,#7740,#677,.T.);
#9682=EDGE_CURVE('',#7743,#7744,#4478,.T.);
#9683=EDGE_CURVE('',#7743,#7741,#678,.T.);
#9684=EDGE_CURVE('',#7744,#7742,#679,.T.);
#9685=EDGE_CURVE('',#7745,#7746,#131,.T.);
#9686=EDGE_CURVE('',#7746,#7747,#4479,.T.);
#9687=EDGE_CURVE('',#7747,#7748,#132,.T.);
#9688=EDGE_CURVE('',#7748,#7749,#248,.T.);
#9689=EDGE_CURVE('',#7749,#7750,#4480,.T.);
#9690=EDGE_CURVE('',#7750,#7745,#249,.T.);
#9691=EDGE_CURVE('',#7746,#7747,#6710,.T.);
#9692=EDGE_CURVE('',#7751,#7752,#133,.T.);
#9693=EDGE_CURVE('',#7752,#7753,#4481,.T.);
#9694=EDGE_CURVE('',#7753,#7754,#134,.T.);
#9695=EDGE_CURVE('',#7754,#7755,#250,.T.);
#9696=EDGE_CURVE('',#7755,#7756,#4482,.T.);
#9697=EDGE_CURVE('',#7756,#7751,#251,.T.);
#9698=EDGE_CURVE('',#7745,#7748,#6711,.T.);
#9699=EDGE_CURVE('',#7750,#7757,#4483,.T.);
#9700=EDGE_CURVE('',#7757,#7758,#6712,.T.);
#9701=EDGE_CURVE('',#7758,#7759,#4484,.T.);
#9702=EDGE_CURVE('',#7759,#7760,#6713,.T.);
#9703=EDGE_CURVE('',#7760,#7761,#4485,.T.);
#9704=EDGE_CURVE('',#7761,#7762,#6714,.T.);
#9705=EDGE_CURVE('',#7762,#7755,#4486,.T.);
#9706=EDGE_CURVE('',#7763,#7754,#6715,.T.);
#9707=EDGE_CURVE('',#7763,#7764,#4487,.T.);
#9708=EDGE_CURVE('',#7764,#7765,#6716,.T.);
#9709=EDGE_CURVE('',#7765,#7766,#4488,.T.);
#9710=EDGE_CURVE('',#7766,#7767,#6717,.T.);
#9711=EDGE_CURVE('',#7767,#7768,#4489,.T.);
#9712=EDGE_CURVE('',#7768,#7768,#6718,.T.);
#9713=EDGE_CURVE('',#7767,#7769,#6719,.T.);
#9714=EDGE_CURVE('',#7769,#7770,#4490,.T.);
#9715=EDGE_CURVE('',#7770,#7764,#6720,.T.);
#9716=EDGE_CURVE('',#7751,#7763,#6721,.T.);
#9717=EDGE_CURVE('',#7756,#7771,#4491,.T.);
#9718=EDGE_CURVE('',#7771,#7772,#6722,.T.);
#9719=EDGE_CURVE('',#7772,#7773,#4492,.T.);
#9720=EDGE_CURVE('',#7773,#7774,#6723,.T.);
#9721=EDGE_CURVE('',#7774,#7775,#4493,.T.);
#9722=EDGE_CURVE('',#7775,#7776,#6724,.T.);
#9723=EDGE_CURVE('',#7776,#7749,#4494,.T.);
#9724=EDGE_CURVE('',#7777,#7778,#4495,.T.);
#9725=EDGE_CURVE('',#7778,#7779,#6725,.T.);
#9726=EDGE_CURVE('',#7779,#7780,#4496,.T.);
#9727=EDGE_CURVE('',#7780,#7777,#6726,.T.);
#9728=EDGE_CURVE('',#7781,#7782,#4497,.T.);
#9729=EDGE_CURVE('',#7782,#7783,#6727,.T.);
#9730=EDGE_CURVE('',#7783,#7784,#4498,.T.);
#9731=EDGE_CURVE('',#7784,#7781,#6728,.T.);
#9732=EDGE_CURVE('',#7785,#7786,#4499,.T.);
#9733=EDGE_CURVE('',#7786,#7787,#6729,.T.);
#9734=EDGE_CURVE('',#7787,#7788,#4500,.T.);
#9735=EDGE_CURVE('',#7788,#7785,#6730,.T.);
#9736=EDGE_CURVE('',#7789,#7790,#4501,.T.);
#9737=EDGE_CURVE('',#7790,#7791,#6731,.T.);
#9738=EDGE_CURVE('',#7791,#7792,#4502,.T.);
#9739=EDGE_CURVE('',#7792,#7789,#6732,.T.);
#9740=EDGE_CURVE('',#7793,#7794,#4503,.T.);
#9741=EDGE_CURVE('',#7794,#7795,#6733,.T.);
#9742=EDGE_CURVE('',#7795,#7796,#4504,.T.);
#9743=EDGE_CURVE('',#7796,#7793,#6734,.T.);
#9744=EDGE_CURVE('',#7797,#7798,#4505,.T.);
#9745=EDGE_CURVE('',#7798,#7799,#6735,.T.);
#9746=EDGE_CURVE('',#7799,#7800,#4506,.T.);
#9747=EDGE_CURVE('',#7800,#7797,#6736,.T.);
#9748=EDGE_CURVE('',#7801,#7802,#4507,.T.);
#9749=EDGE_CURVE('',#7802,#7803,#6737,.T.);
#9750=EDGE_CURVE('',#7803,#7804,#4508,.T.);
#9751=EDGE_CURVE('',#7804,#7801,#6738,.T.);
#9752=EDGE_CURVE('',#7805,#7806,#4509,.T.);
#9753=EDGE_CURVE('',#7806,#7807,#6739,.T.);
#9754=EDGE_CURVE('',#7807,#7808,#4510,.T.);
#9755=EDGE_CURVE('',#7808,#7805,#6740,.T.);
#9756=EDGE_CURVE('',#7809,#7810,#4511,.T.);
#9757=EDGE_CURVE('',#7810,#7811,#6741,.T.);
#9758=EDGE_CURVE('',#7811,#7812,#4512,.T.);
#9759=EDGE_CURVE('',#7812,#7809,#6742,.T.);
#9760=EDGE_CURVE('',#7813,#7814,#4513,.T.);
#9761=EDGE_CURVE('',#7814,#7815,#6743,.T.);
#9762=EDGE_CURVE('',#7815,#7816,#4514,.T.);
#9763=EDGE_CURVE('',#7816,#7813,#6744,.T.);
#9764=EDGE_CURVE('',#7817,#7818,#4515,.T.);
#9765=EDGE_CURVE('',#7818,#7819,#6745,.T.);
#9766=EDGE_CURVE('',#7819,#7820,#4516,.T.);
#9767=EDGE_CURVE('',#7820,#7817,#6746,.T.);
#9768=EDGE_CURVE('',#7821,#7822,#4517,.T.);
#9769=EDGE_CURVE('',#7822,#7823,#6747,.T.);
#9770=EDGE_CURVE('',#7823,#7824,#4518,.T.);
#9771=EDGE_CURVE('',#7824,#7821,#6748,.T.);
#9772=EDGE_CURVE('',#7825,#7826,#4519,.T.);
#9773=EDGE_CURVE('',#7826,#7827,#6749,.T.);
#9774=EDGE_CURVE('',#7827,#7828,#4520,.T.);
#9775=EDGE_CURVE('',#7828,#7825,#6750,.T.);
#9776=EDGE_CURVE('',#7829,#7830,#4521,.T.);
#9777=EDGE_CURVE('',#7830,#7831,#6751,.T.);
#9778=EDGE_CURVE('',#7831,#7832,#4522,.T.);
#9779=EDGE_CURVE('',#7832,#7829,#6752,.T.);
#9780=EDGE_CURVE('',#7833,#7834,#4523,.T.);
#9781=EDGE_CURVE('',#7834,#7835,#6753,.T.);
#9782=EDGE_CURVE('',#7835,#7836,#4524,.T.);
#9783=EDGE_CURVE('',#7836,#7833,#6754,.T.);
#9784=EDGE_CURVE('',#7837,#7838,#4525,.T.);
#9785=EDGE_CURVE('',#7838,#7839,#6755,.T.);
#9786=EDGE_CURVE('',#7839,#7840,#4526,.T.);
#9787=EDGE_CURVE('',#7840,#7837,#6756,.T.);
#9788=EDGE_CURVE('',#7841,#7842,#4527,.T.);
#9789=EDGE_CURVE('',#7842,#7843,#6757,.T.);
#9790=EDGE_CURVE('',#7843,#7844,#4528,.T.);
#9791=EDGE_CURVE('',#7844,#7841,#6758,.T.);
#9792=EDGE_CURVE('',#7845,#7846,#4529,.T.);
#9793=EDGE_CURVE('',#7846,#7847,#6759,.T.);
#9794=EDGE_CURVE('',#7847,#7848,#4530,.T.);
#9795=EDGE_CURVE('',#7848,#7845,#6760,.T.);
#9796=EDGE_CURVE('',#7849,#7850,#4531,.T.);
#9797=EDGE_CURVE('',#7850,#7851,#6761,.T.);
#9798=EDGE_CURVE('',#7851,#7852,#4532,.T.);
#9799=EDGE_CURVE('',#7852,#7849,#6762,.T.);
#9800=EDGE_CURVE('',#7853,#7854,#4533,.T.);
#9801=EDGE_CURVE('',#7854,#7855,#6763,.T.);
#9802=EDGE_CURVE('',#7855,#7856,#4534,.T.);
#9803=EDGE_CURVE('',#7856,#7853,#6764,.T.);
#9804=EDGE_CURVE('',#7857,#7858,#4535,.T.);
#9805=EDGE_CURVE('',#7858,#7859,#6765,.T.);
#9806=EDGE_CURVE('',#7859,#7860,#4536,.T.);
#9807=EDGE_CURVE('',#7860,#7857,#6766,.T.);
#9808=EDGE_CURVE('',#7752,#7753,#6767,.T.);
#9809=EDGE_CURVE('',#7861,#7722,#680,.T.);
#9810=EDGE_CURVE('',#7716,#7861,#681,.T.);
#9811=EDGE_CURVE('',#7862,#7692,#682,.T.);
#9812=EDGE_CURVE('',#7862,#7744,#683,.T.);
#9813=EDGE_CURVE('',#7692,#7863,#6768,.T.);
#9814=EDGE_CURVE('',#7863,#7691,#6769,.T.);
#9815=EDGE_CURVE('',#7691,#7864,#684,.T.);
#9816=EDGE_CURVE('',#7864,#7862,#6770,.T.);
#9817=EDGE_CURVE('',#7864,#7743,#685,.T.);
#9818=EDGE_CURVE('',#7719,#7865,#686,.T.);
#9819=EDGE_CURVE('',#7865,#7715,#687,.T.);
#9820=EDGE_CURVE('',#7762,#7771,#4537,.T.);
#9821=EDGE_CURVE('',#7776,#7757,#4538,.T.);
#9822=EDGE_CURVE('',#7866,#7775,#4539,.T.);
#9823=EDGE_CURVE('',#7772,#7866,#4540,.T.);
#9824=EDGE_CURVE('',#7867,#7761,#4541,.T.);
#9825=EDGE_CURVE('',#7758,#7867,#4542,.T.);
#9826=EDGE_CURVE('',#7868,#7760,#4543,.T.);
#9827=EDGE_CURVE('',#7868,#7867,#4544,.T.);
#9828=EDGE_CURVE('',#7859,#7869,#4545,.T.);
#9829=EDGE_CURVE('',#7870,#7869,#4546,.T.);
#9830=EDGE_CURVE('',#7860,#7870,#4547,.T.);
#9831=EDGE_CURVE('',#7870,#7857,#4548,.T.);
#9832=EDGE_CURVE('',#7869,#7858,#4549,.T.);
#9833=EDGE_CURVE('',#7855,#7871,#4550,.T.);
#9834=EDGE_CURVE('',#7872,#7871,#4551,.T.);
#9835=EDGE_CURVE('',#7856,#7872,#4552,.T.);
#9836=EDGE_CURVE('',#7872,#7853,#4553,.T.);
#9837=EDGE_CURVE('',#7871,#7854,#4554,.T.);
#9838=EDGE_CURVE('',#7851,#7873,#4555,.T.);
#9839=EDGE_CURVE('',#7874,#7873,#4556,.T.);
#9840=EDGE_CURVE('',#7852,#7874,#4557,.T.);
#9841=EDGE_CURVE('',#7874,#7849,#4558,.T.);
#9842=EDGE_CURVE('',#7873,#7850,#4559,.T.);
#9843=EDGE_CURVE('',#7847,#7875,#4560,.T.);
#9844=EDGE_CURVE('',#7876,#7875,#4561,.T.);
#9845=EDGE_CURVE('',#7848,#7876,#4562,.T.);
#9846=EDGE_CURVE('',#7876,#7845,#4563,.T.);
#9847=EDGE_CURVE('',#7875,#7846,#4564,.T.);
#9848=EDGE_CURVE('',#7843,#7877,#4565,.T.);
#9849=EDGE_CURVE('',#7878,#7877,#4566,.T.);
#9850=EDGE_CURVE('',#7844,#7878,#4567,.T.);
#9851=EDGE_CURVE('',#7878,#7841,#4568,.T.);
#9852=EDGE_CURVE('',#7877,#7842,#4569,.T.);
#9853=EDGE_CURVE('',#7759,#7868,#4570,.T.);
#9854=EDGE_CURVE('',#7839,#7879,#4571,.T.);
#9855=EDGE_CURVE('',#7880,#7879,#4572,.T.);
#9856=EDGE_CURVE('',#7840,#7880,#4573,.T.);
#9857=EDGE_CURVE('',#7880,#7837,#4574,.T.);
#9858=EDGE_CURVE('',#7879,#7838,#4575,.T.);
#9859=EDGE_CURVE('',#7835,#7881,#4576,.T.);
#9860=EDGE_CURVE('',#7882,#7881,#4577,.T.);
#9861=EDGE_CURVE('',#7836,#7882,#4578,.T.);
#9862=EDGE_CURVE('',#7882,#7833,#4579,.T.);
#9863=EDGE_CURVE('',#7881,#7834,#4580,.T.);
#9864=EDGE_CURVE('',#7831,#7883,#4581,.T.);
#9865=EDGE_CURVE('',#7884,#7883,#4582,.T.);
#9866=EDGE_CURVE('',#7832,#7884,#4583,.T.);
#9867=EDGE_CURVE('',#7884,#7829,#4584,.T.);
#9868=EDGE_CURVE('',#7883,#7830,#4585,.T.);
#9869=EDGE_CURVE('',#7827,#7885,#4586,.T.);
#9870=EDGE_CURVE('',#7886,#7885,#4587,.T.);
#9871=EDGE_CURVE('',#7828,#7886,#4588,.T.);
#9872=EDGE_CURVE('',#7886,#7825,#4589,.T.);
#9873=EDGE_CURVE('',#7885,#7826,#4590,.T.);
#9874=EDGE_CURVE('',#7823,#7887,#4591,.T.);
#9875=EDGE_CURVE('',#7888,#7887,#4592,.T.);
#9876=EDGE_CURVE('',#7824,#7888,#4593,.T.);
#9877=EDGE_CURVE('',#7888,#7821,#4594,.T.);
#9878=EDGE_CURVE('',#7887,#7822,#4595,.T.);
#9879=EDGE_CURVE('',#7765,#7889,#4596,.T.);
#9880=EDGE_CURVE('',#7890,#7889,#4597,.T.);
#9881=EDGE_CURVE('',#7766,#7890,#4598,.T.);
#9882=EDGE_CURVE('',#7890,#7769,#4599,.T.);
#9883=EDGE_CURVE('',#7889,#7770,#4600,.T.);
#9884=EDGE_CURVE('',#7819,#7891,#4601,.T.);
#9885=EDGE_CURVE('',#7892,#7891,#4602,.T.);
#9886=EDGE_CURVE('',#7820,#7892,#4603,.T.);
#9887=EDGE_CURVE('',#7892,#7817,#4604,.T.);
#9888=EDGE_CURVE('',#7891,#7818,#4605,.T.);
#9889=EDGE_CURVE('',#7815,#7893,#4606,.T.);
#9890=EDGE_CURVE('',#7894,#7893,#4607,.T.);
#9891=EDGE_CURVE('',#7816,#7894,#4608,.T.);
#9892=EDGE_CURVE('',#7894,#7813,#4609,.T.);
#9893=EDGE_CURVE('',#7893,#7814,#4610,.T.);
#9894=EDGE_CURVE('',#7811,#7895,#4611,.T.);
#9895=EDGE_CURVE('',#7896,#7895,#4612,.T.);
#9896=EDGE_CURVE('',#7812,#7896,#4613,.T.);
#9897=EDGE_CURVE('',#7896,#7809,#4614,.T.);
#9898=EDGE_CURVE('',#7895,#7810,#4615,.T.);
#9899=EDGE_CURVE('',#7807,#7897,#4616,.T.);
#9900=EDGE_CURVE('',#7898,#7897,#4617,.T.);
#9901=EDGE_CURVE('',#7808,#7898,#4618,.T.);
#9902=EDGE_CURVE('',#7898,#7805,#4619,.T.);
#9903=EDGE_CURVE('',#7897,#7806,#4620,.T.);
#9904=EDGE_CURVE('',#7803,#7899,#4621,.T.);
#9905=EDGE_CURVE('',#7900,#7899,#4622,.T.);
#9906=EDGE_CURVE('',#7804,#7900,#4623,.T.);
#9907=EDGE_CURVE('',#7900,#7801,#4624,.T.);
#9908=EDGE_CURVE('',#7899,#7802,#4625,.T.);
#9909=EDGE_CURVE('',#7901,#7866,#4626,.T.);
#9910=EDGE_CURVE('',#7773,#7901,#4627,.T.);
#9911=EDGE_CURVE('',#7901,#7774,#4628,.T.);
#9912=EDGE_CURVE('',#7799,#7902,#4629,.T.);
#9913=EDGE_CURVE('',#7903,#7902,#4630,.T.);
#9914=EDGE_CURVE('',#7800,#7903,#4631,.T.);
#9915=EDGE_CURVE('',#7903,#7797,#4632,.T.);
#9916=EDGE_CURVE('',#7902,#7798,#4633,.T.);
#9917=EDGE_CURVE('',#7795,#7904,#4634,.T.);
#9918=EDGE_CURVE('',#7905,#7904,#4635,.T.);
#9919=EDGE_CURVE('',#7796,#7905,#4636,.T.);
#9920=EDGE_CURVE('',#7905,#7793,#4637,.T.);
#9921=EDGE_CURVE('',#7904,#7794,#4638,.T.);
#9922=EDGE_CURVE('',#7791,#7906,#4639,.T.);
#9923=EDGE_CURVE('',#7907,#7906,#4640,.T.);
#9924=EDGE_CURVE('',#7792,#7907,#4641,.T.);
#9925=EDGE_CURVE('',#7907,#7789,#4642,.T.);
#9926=EDGE_CURVE('',#7906,#7790,#4643,.T.);
#9927=EDGE_CURVE('',#7787,#7908,#4644,.T.);
#9928=EDGE_CURVE('',#7909,#7908,#4645,.T.);
#9929=EDGE_CURVE('',#7788,#7909,#4646,.T.);
#9930=EDGE_CURVE('',#7909,#7785,#4647,.T.);
#9931=EDGE_CURVE('',#7908,#7786,#4648,.T.);
#9932=EDGE_CURVE('',#7783,#7910,#4649,.T.);
#9933=EDGE_CURVE('',#7911,#7910,#4650,.T.);
#9934=EDGE_CURVE('',#7784,#7911,#4651,.T.);
#9935=EDGE_CURVE('',#7911,#7781,#4652,.T.);
#9936=EDGE_CURVE('',#7910,#7782,#4653,.T.);
#9937=EDGE_CURVE('',#7779,#7912,#4654,.T.);
#9938=EDGE_CURVE('',#7913,#7912,#4655,.T.);
#9939=EDGE_CURVE('',#7780,#7913,#4656,.T.);
#9940=EDGE_CURVE('',#7913,#7777,#4657,.T.);
#9941=EDGE_CURVE('',#7912,#7778,#4658,.T.);
#9942=EDGE_CURVE('',#7914,#7914,#6771,.T.);
#9943=EDGE_CURVE('',#7863,#7914,#4659,.T.);
#9944=EDGE_CURVE('',#7865,#7861,#6772,.T.);
#9945=EDGE_CURVE('',#7915,#7915,#6773,.T.);
#9946=EDGE_CURVE('',#7768,#7915,#4660,.T.);
#13084=ORIENTED_EDGE('',*,*,#9605,.F.);
#13085=ORIENTED_EDGE('',*,*,#9606,.T.);
#13086=ORIENTED_EDGE('',*,*,#9607,.T.);
#13087=ORIENTED_EDGE('',*,*,#9608,.T.);
#13088=ORIENTED_EDGE('',*,*,#9609,.F.);
#13089=ORIENTED_EDGE('',*,*,#9610,.T.);
#13090=ORIENTED_EDGE('',*,*,#9605,.T.);
#13091=ORIENTED_EDGE('',*,*,#9611,.T.);
#13092=ORIENTED_EDGE('',*,*,#9612,.F.);
#13093=ORIENTED_EDGE('',*,*,#9613,.T.);
#13094=ORIENTED_EDGE('',*,*,#9609,.T.);
#13095=ORIENTED_EDGE('',*,*,#9614,.T.);
#13096=ORIENTED_EDGE('',*,*,#9615,.F.);
#13097=ORIENTED_EDGE('',*,*,#9616,.T.);
#13098=ORIENTED_EDGE('',*,*,#9612,.T.);
#13099=ORIENTED_EDGE('',*,*,#9617,.T.);
#13100=ORIENTED_EDGE('',*,*,#9618,.F.);
#13101=ORIENTED_EDGE('',*,*,#9619,.T.);
#13102=ORIENTED_EDGE('',*,*,#9615,.T.);
#13103=ORIENTED_EDGE('',*,*,#9620,.T.);
#13104=ORIENTED_EDGE('',*,*,#9621,.F.);
#13105=ORIENTED_EDGE('',*,*,#9622,.T.);
#13106=ORIENTED_EDGE('',*,*,#9618,.T.);
#13107=ORIENTED_EDGE('',*,*,#9623,.T.);
#13108=ORIENTED_EDGE('',*,*,#9624,.F.);
#13109=ORIENTED_EDGE('',*,*,#9625,.T.);
#13110=ORIENTED_EDGE('',*,*,#9621,.T.);
#13111=ORIENTED_EDGE('',*,*,#9626,.T.);
#13112=ORIENTED_EDGE('',*,*,#9627,.F.);
#13113=ORIENTED_EDGE('',*,*,#9628,.T.);
#13114=ORIENTED_EDGE('',*,*,#9624,.T.);
#13115=ORIENTED_EDGE('',*,*,#9629,.T.);
#13116=ORIENTED_EDGE('',*,*,#9630,.F.);
#13117=ORIENTED_EDGE('',*,*,#9631,.T.);
#13118=ORIENTED_EDGE('',*,*,#9627,.T.);
#13119=ORIENTED_EDGE('',*,*,#9632,.T.);
#13120=ORIENTED_EDGE('',*,*,#9633,.F.);
#13121=ORIENTED_EDGE('',*,*,#9634,.T.);
#13122=ORIENTED_EDGE('',*,*,#9630,.T.);
#13123=ORIENTED_EDGE('',*,*,#9635,.T.);
#13124=ORIENTED_EDGE('',*,*,#9636,.F.);
#13125=ORIENTED_EDGE('',*,*,#9637,.T.);
#13126=ORIENTED_EDGE('',*,*,#9633,.T.);
#13127=ORIENTED_EDGE('',*,*,#9638,.T.);
#13128=ORIENTED_EDGE('',*,*,#9639,.F.);
#13129=ORIENTED_EDGE('',*,*,#9640,.T.);
#13130=ORIENTED_EDGE('',*,*,#9636,.T.);
#13131=ORIENTED_EDGE('',*,*,#9641,.T.);
#13132=ORIENTED_EDGE('',*,*,#9642,.F.);
#13133=ORIENTED_EDGE('',*,*,#9643,.T.);
#13134=ORIENTED_EDGE('',*,*,#9639,.T.);
#13135=ORIENTED_EDGE('',*,*,#9644,.T.);
#13136=ORIENTED_EDGE('',*,*,#9645,.F.);
#13137=ORIENTED_EDGE('',*,*,#9646,.T.);
#13138=ORIENTED_EDGE('',*,*,#9647,.F.);
#13139=ORIENTED_EDGE('',*,*,#9648,.F.);
#13140=ORIENTED_EDGE('',*,*,#9649,.T.);
#13141=ORIENTED_EDGE('',*,*,#9645,.T.);
#13142=ORIENTED_EDGE('',*,*,#9650,.F.);
#13143=ORIENTED_EDGE('',*,*,#9651,.F.);
#13144=ORIENTED_EDGE('',*,*,#9652,.F.);
#13145=ORIENTED_EDGE('',*,*,#9653,.T.);
#13146=ORIENTED_EDGE('',*,*,#9648,.T.);
#13147=ORIENTED_EDGE('',*,*,#9654,.F.);
#13148=ORIENTED_EDGE('',*,*,#9655,.F.);
#13149=ORIENTED_EDGE('',*,*,#9656,.T.);
#13150=ORIENTED_EDGE('',*,*,#9652,.T.);
#13151=ORIENTED_EDGE('',*,*,#9657,.F.);
#13152=ORIENTED_EDGE('',*,*,#9658,.F.);
#13153=ORIENTED_EDGE('',*,*,#9659,.T.);
#13154=ORIENTED_EDGE('',*,*,#9655,.T.);
#13155=ORIENTED_EDGE('',*,*,#9660,.F.);
#13156=ORIENTED_EDGE('',*,*,#9661,.F.);
#13157=ORIENTED_EDGE('',*,*,#9662,.T.);
#13158=ORIENTED_EDGE('',*,*,#9658,.T.);
#13159=ORIENTED_EDGE('',*,*,#9663,.F.);
#13160=ORIENTED_EDGE('',*,*,#9664,.F.);
#13161=ORIENTED_EDGE('',*,*,#9665,.T.);
#13162=ORIENTED_EDGE('',*,*,#9661,.T.);
#13163=ORIENTED_EDGE('',*,*,#9666,.F.);
#13164=ORIENTED_EDGE('',*,*,#9667,.F.);
#13165=ORIENTED_EDGE('',*,*,#9668,.T.);
#13166=ORIENTED_EDGE('',*,*,#9664,.T.);
#13167=ORIENTED_EDGE('',*,*,#9669,.F.);
#13168=ORIENTED_EDGE('',*,*,#9670,.F.);
#13169=ORIENTED_EDGE('',*,*,#9671,.T.);
#13170=ORIENTED_EDGE('',*,*,#9667,.T.);
#13171=ORIENTED_EDGE('',*,*,#9672,.F.);
#13172=ORIENTED_EDGE('',*,*,#9673,.F.);
#13173=ORIENTED_EDGE('',*,*,#9674,.T.);
#13174=ORIENTED_EDGE('',*,*,#9670,.T.);
#13175=ORIENTED_EDGE('',*,*,#9675,.F.);
#13176=ORIENTED_EDGE('',*,*,#9676,.F.);
#13177=ORIENTED_EDGE('',*,*,#9677,.T.);
#13178=ORIENTED_EDGE('',*,*,#9673,.T.);
#13179=ORIENTED_EDGE('',*,*,#9678,.F.);
#13180=ORIENTED_EDGE('',*,*,#9679,.F.);
#13181=ORIENTED_EDGE('',*,*,#9680,.T.);
#13182=ORIENTED_EDGE('',*,*,#9676,.T.);
#13183=ORIENTED_EDGE('',*,*,#9681,.F.);
#13184=ORIENTED_EDGE('',*,*,#9682,.F.);
#13185=ORIENTED_EDGE('',*,*,#9683,.T.);
#13186=ORIENTED_EDGE('',*,*,#9679,.T.);
#13187=ORIENTED_EDGE('',*,*,#9684,.F.);
#13188=ORIENTED_EDGE('',*,*,#9685,.T.);
#13189=ORIENTED_EDGE('',*,*,#9686,.T.);
#13190=ORIENTED_EDGE('',*,*,#9687,.T.);
#13191=ORIENTED_EDGE('',*,*,#9688,.T.);
#13192=ORIENTED_EDGE('',*,*,#9689,.T.);
#13193=ORIENTED_EDGE('',*,*,#9690,.T.);
#13194=ORIENTED_EDGE('',*,*,#9686,.F.);
#13195=ORIENTED_EDGE('',*,*,#9691,.T.);
#13196=ORIENTED_EDGE('',*,*,#9692,.T.);
#13197=ORIENTED_EDGE('',*,*,#9693,.T.);
#13198=ORIENTED_EDGE('',*,*,#9694,.T.);
#13199=ORIENTED_EDGE('',*,*,#9695,.T.);
#13200=ORIENTED_EDGE('',*,*,#9696,.T.);
#13201=ORIENTED_EDGE('',*,*,#9697,.T.);
#13202=ORIENTED_EDGE('',*,*,#9688,.F.);
#13203=ORIENTED_EDGE('',*,*,#9698,.F.);
#13204=ORIENTED_EDGE('',*,*,#9690,.F.);
#13205=ORIENTED_EDGE('',*,*,#9699,.T.);
#13206=ORIENTED_EDGE('',*,*,#9700,.T.);
#13207=ORIENTED_EDGE('',*,*,#9701,.T.);
#13208=ORIENTED_EDGE('',*,*,#9702,.T.);
#13209=ORIENTED_EDGE('',*,*,#9703,.T.);
#13210=ORIENTED_EDGE('',*,*,#9704,.T.);
#13211=ORIENTED_EDGE('',*,*,#9705,.T.);
#13212=ORIENTED_EDGE('',*,*,#9695,.F.);
#13213=ORIENTED_EDGE('',*,*,#9706,.F.);
#13214=ORIENTED_EDGE('',*,*,#9707,.T.);
#13215=ORIENTED_EDGE('',*,*,#9708,.T.);
#13216=ORIENTED_EDGE('',*,*,#9709,.T.);
#13217=ORIENTED_EDGE('',*,*,#9710,.T.);
#13218=ORIENTED_EDGE('',*,*,#9711,.T.);
#13219=ORIENTED_EDGE('',*,*,#9712,.T.);
#13220=ORIENTED_EDGE('',*,*,#9711,.F.);
#13221=ORIENTED_EDGE('',*,*,#9713,.T.);
#13222=ORIENTED_EDGE('',*,*,#9714,.T.);
#13223=ORIENTED_EDGE('',*,*,#9715,.T.);
#13224=ORIENTED_EDGE('',*,*,#9707,.F.);
#13225=ORIENTED_EDGE('',*,*,#9716,.F.);
#13226=ORIENTED_EDGE('',*,*,#9697,.F.);
#13227=ORIENTED_EDGE('',*,*,#9717,.T.);
#13228=ORIENTED_EDGE('',*,*,#9718,.T.);
#13229=ORIENTED_EDGE('',*,*,#9719,.T.);
#13230=ORIENTED_EDGE('',*,*,#9720,.T.);
#13231=ORIENTED_EDGE('',*,*,#9721,.T.);
#13232=ORIENTED_EDGE('',*,*,#9722,.T.);
#13233=ORIENTED_EDGE('',*,*,#9723,.T.);
#13234=ORIENTED_EDGE('',*,*,#9724,.T.);
#13235=ORIENTED_EDGE('',*,*,#9725,.T.);
#13236=ORIENTED_EDGE('',*,*,#9726,.T.);
#13237=ORIENTED_EDGE('',*,*,#9727,.T.);
#13238=ORIENTED_EDGE('',*,*,#9728,.T.);
#13239=ORIENTED_EDGE('',*,*,#9729,.T.);
#13240=ORIENTED_EDGE('',*,*,#9730,.T.);
#13241=ORIENTED_EDGE('',*,*,#9731,.T.);
#13242=ORIENTED_EDGE('',*,*,#9732,.T.);
#13243=ORIENTED_EDGE('',*,*,#9733,.T.);
#13244=ORIENTED_EDGE('',*,*,#9734,.T.);
#13245=ORIENTED_EDGE('',*,*,#9735,.T.);
#13246=ORIENTED_EDGE('',*,*,#9736,.T.);
#13247=ORIENTED_EDGE('',*,*,#9737,.T.);
#13248=ORIENTED_EDGE('',*,*,#9738,.T.);
#13249=ORIENTED_EDGE('',*,*,#9739,.T.);
#13250=ORIENTED_EDGE('',*,*,#9740,.T.);
#13251=ORIENTED_EDGE('',*,*,#9741,.T.);
#13252=ORIENTED_EDGE('',*,*,#9742,.T.);
#13253=ORIENTED_EDGE('',*,*,#9743,.T.);
#13254=ORIENTED_EDGE('',*,*,#9744,.T.);
#13255=ORIENTED_EDGE('',*,*,#9745,.T.);
#13256=ORIENTED_EDGE('',*,*,#9746,.T.);
#13257=ORIENTED_EDGE('',*,*,#9747,.T.);
#13258=ORIENTED_EDGE('',*,*,#9748,.T.);
#13259=ORIENTED_EDGE('',*,*,#9749,.T.);
#13260=ORIENTED_EDGE('',*,*,#9750,.T.);
#13261=ORIENTED_EDGE('',*,*,#9751,.T.);
#13262=ORIENTED_EDGE('',*,*,#9752,.T.);
#13263=ORIENTED_EDGE('',*,*,#9753,.T.);
#13264=ORIENTED_EDGE('',*,*,#9754,.T.);
#13265=ORIENTED_EDGE('',*,*,#9755,.T.);
#13266=ORIENTED_EDGE('',*,*,#9756,.T.);
#13267=ORIENTED_EDGE('',*,*,#9757,.T.);
#13268=ORIENTED_EDGE('',*,*,#9758,.T.);
#13269=ORIENTED_EDGE('',*,*,#9759,.T.);
#13270=ORIENTED_EDGE('',*,*,#9760,.T.);
#13271=ORIENTED_EDGE('',*,*,#9761,.T.);
#13272=ORIENTED_EDGE('',*,*,#9762,.T.);
#13273=ORIENTED_EDGE('',*,*,#9763,.T.);
#13274=ORIENTED_EDGE('',*,*,#9764,.T.);
#13275=ORIENTED_EDGE('',*,*,#9765,.T.);
#13276=ORIENTED_EDGE('',*,*,#9766,.T.);
#13277=ORIENTED_EDGE('',*,*,#9767,.T.);
#13278=ORIENTED_EDGE('',*,*,#9768,.T.);
#13279=ORIENTED_EDGE('',*,*,#9769,.T.);
#13280=ORIENTED_EDGE('',*,*,#9770,.T.);
#13281=ORIENTED_EDGE('',*,*,#9771,.T.);
#13282=ORIENTED_EDGE('',*,*,#9772,.T.);
#13283=ORIENTED_EDGE('',*,*,#9773,.T.);
#13284=ORIENTED_EDGE('',*,*,#9774,.T.);
#13285=ORIENTED_EDGE('',*,*,#9775,.T.);
#13286=ORIENTED_EDGE('',*,*,#9776,.T.);
#13287=ORIENTED_EDGE('',*,*,#9777,.T.);
#13288=ORIENTED_EDGE('',*,*,#9778,.T.);
#13289=ORIENTED_EDGE('',*,*,#9779,.T.);
#13290=ORIENTED_EDGE('',*,*,#9780,.T.);
#13291=ORIENTED_EDGE('',*,*,#9781,.T.);
#13292=ORIENTED_EDGE('',*,*,#9782,.T.);
#13293=ORIENTED_EDGE('',*,*,#9783,.T.);
#13294=ORIENTED_EDGE('',*,*,#9784,.T.);
#13295=ORIENTED_EDGE('',*,*,#9785,.T.);
#13296=ORIENTED_EDGE('',*,*,#9786,.T.);
#13297=ORIENTED_EDGE('',*,*,#9787,.T.);
#13298=ORIENTED_EDGE('',*,*,#9788,.T.);
#13299=ORIENTED_EDGE('',*,*,#9789,.T.);
#13300=ORIENTED_EDGE('',*,*,#9790,.T.);
#13301=ORIENTED_EDGE('',*,*,#9791,.T.);
#13302=ORIENTED_EDGE('',*,*,#9792,.T.);
#13303=ORIENTED_EDGE('',*,*,#9793,.T.);
#13304=ORIENTED_EDGE('',*,*,#9794,.T.);
#13305=ORIENTED_EDGE('',*,*,#9795,.T.);
#13306=ORIENTED_EDGE('',*,*,#9796,.T.);
#13307=ORIENTED_EDGE('',*,*,#9797,.T.);
#13308=ORIENTED_EDGE('',*,*,#9798,.T.);
#13309=ORIENTED_EDGE('',*,*,#9799,.T.);
#13310=ORIENTED_EDGE('',*,*,#9800,.T.);
#13311=ORIENTED_EDGE('',*,*,#9801,.T.);
#13312=ORIENTED_EDGE('',*,*,#9802,.T.);
#13313=ORIENTED_EDGE('',*,*,#9803,.T.);
#13314=ORIENTED_EDGE('',*,*,#9804,.T.);
#13315=ORIENTED_EDGE('',*,*,#9805,.T.);
#13316=ORIENTED_EDGE('',*,*,#9806,.T.);
#13317=ORIENTED_EDGE('',*,*,#9807,.T.);
#13318=ORIENTED_EDGE('',*,*,#9694,.F.);
#13319=ORIENTED_EDGE('',*,*,#9808,.F.);
#13320=ORIENTED_EDGE('',*,*,#9692,.F.);
#13321=ORIENTED_EDGE('',*,*,#9716,.T.);
#13322=ORIENTED_EDGE('',*,*,#9706,.T.);
#13323=ORIENTED_EDGE('',*,*,#9693,.F.);
#13324=ORIENTED_EDGE('',*,*,#9808,.T.);
#13325=ORIENTED_EDGE('',*,*,#9809,.F.);
#13326=ORIENTED_EDGE('',*,*,#9810,.F.);
#13327=ORIENTED_EDGE('',*,*,#9644,.F.);
#13328=ORIENTED_EDGE('',*,*,#9641,.F.);
#13329=ORIENTED_EDGE('',*,*,#9638,.F.);
#13330=ORIENTED_EDGE('',*,*,#9635,.F.);
#13331=ORIENTED_EDGE('',*,*,#9632,.F.);
#13332=ORIENTED_EDGE('',*,*,#9629,.F.);
#13333=ORIENTED_EDGE('',*,*,#9626,.F.);
#13334=ORIENTED_EDGE('',*,*,#9623,.F.);
#13335=ORIENTED_EDGE('',*,*,#9620,.F.);
#13336=ORIENTED_EDGE('',*,*,#9617,.F.);
#13337=ORIENTED_EDGE('',*,*,#9614,.F.);
#13338=ORIENTED_EDGE('',*,*,#9611,.F.);
#13339=ORIENTED_EDGE('',*,*,#9608,.F.);
#13340=ORIENTED_EDGE('',*,*,#9811,.F.);
#13341=ORIENTED_EDGE('',*,*,#9812,.T.);
#13342=ORIENTED_EDGE('',*,*,#9684,.T.);
#13343=ORIENTED_EDGE('',*,*,#9681,.T.);
#13344=ORIENTED_EDGE('',*,*,#9678,.T.);
#13345=ORIENTED_EDGE('',*,*,#9675,.T.);
#13346=ORIENTED_EDGE('',*,*,#9672,.T.);
#13347=ORIENTED_EDGE('',*,*,#9669,.T.);
#13348=ORIENTED_EDGE('',*,*,#9666,.T.);
#13349=ORIENTED_EDGE('',*,*,#9663,.T.);
#13350=ORIENTED_EDGE('',*,*,#9660,.T.);
#13351=ORIENTED_EDGE('',*,*,#9657,.T.);
#13352=ORIENTED_EDGE('',*,*,#9654,.T.);
#13353=ORIENTED_EDGE('',*,*,#9651,.T.);
#13354=ORIENTED_EDGE('',*,*,#9813,.T.);
#13355=ORIENTED_EDGE('',*,*,#9814,.T.);
#13356=ORIENTED_EDGE('',*,*,#9815,.T.);
#13357=ORIENTED_EDGE('',*,*,#9816,.T.);
#13358=ORIENTED_EDGE('',*,*,#9811,.T.);
#13359=ORIENTED_EDGE('',*,*,#9682,.T.);
#13360=ORIENTED_EDGE('',*,*,#9812,.F.);
#13361=ORIENTED_EDGE('',*,*,#9816,.F.);
#13362=ORIENTED_EDGE('',*,*,#9817,.T.);
#13363=ORIENTED_EDGE('',*,*,#9818,.F.);
#13364=ORIENTED_EDGE('',*,*,#9646,.F.);
#13365=ORIENTED_EDGE('',*,*,#9649,.F.);
#13366=ORIENTED_EDGE('',*,*,#9653,.F.);
#13367=ORIENTED_EDGE('',*,*,#9656,.F.);
#13368=ORIENTED_EDGE('',*,*,#9659,.F.);
#13369=ORIENTED_EDGE('',*,*,#9662,.F.);
#13370=ORIENTED_EDGE('',*,*,#9665,.F.);
#13371=ORIENTED_EDGE('',*,*,#9668,.F.);
#13372=ORIENTED_EDGE('',*,*,#9671,.F.);
#13373=ORIENTED_EDGE('',*,*,#9674,.F.);
#13374=ORIENTED_EDGE('',*,*,#9677,.F.);
#13375=ORIENTED_EDGE('',*,*,#9680,.F.);
#13376=ORIENTED_EDGE('',*,*,#9683,.F.);
#13377=ORIENTED_EDGE('',*,*,#9817,.F.);
#13378=ORIENTED_EDGE('',*,*,#9815,.F.);
#13379=ORIENTED_EDGE('',*,*,#9606,.F.);
#13380=ORIENTED_EDGE('',*,*,#9610,.F.);
#13381=ORIENTED_EDGE('',*,*,#9613,.F.);
#13382=ORIENTED_EDGE('',*,*,#9616,.F.);
#13383=ORIENTED_EDGE('',*,*,#9619,.F.);
#13384=ORIENTED_EDGE('',*,*,#9622,.F.);
#13385=ORIENTED_EDGE('',*,*,#9625,.F.);
#13386=ORIENTED_EDGE('',*,*,#9628,.F.);
#13387=ORIENTED_EDGE('',*,*,#9631,.F.);
#13388=ORIENTED_EDGE('',*,*,#9634,.F.);
#13389=ORIENTED_EDGE('',*,*,#9637,.F.);
#13390=ORIENTED_EDGE('',*,*,#9640,.F.);
#13391=ORIENTED_EDGE('',*,*,#9643,.F.);
#13392=ORIENTED_EDGE('',*,*,#9819,.F.);
#13393=ORIENTED_EDGE('',*,*,#9696,.F.);
#13394=ORIENTED_EDGE('',*,*,#9705,.F.);
#13395=ORIENTED_EDGE('',*,*,#9820,.T.);
#13396=ORIENTED_EDGE('',*,*,#9717,.F.);
#13397=ORIENTED_EDGE('',*,*,#9700,.F.);
#13398=ORIENTED_EDGE('',*,*,#9821,.F.);
#13399=ORIENTED_EDGE('',*,*,#9722,.F.);
#13400=ORIENTED_EDGE('',*,*,#9822,.F.);
#13401=ORIENTED_EDGE('',*,*,#9823,.F.);
#13402=ORIENTED_EDGE('',*,*,#9718,.F.);
#13403=ORIENTED_EDGE('',*,*,#9820,.F.);
#13404=ORIENTED_EDGE('',*,*,#9704,.F.);
#13405=ORIENTED_EDGE('',*,*,#9824,.F.);
#13406=ORIENTED_EDGE('',*,*,#9825,.F.);
#13407=ORIENTED_EDGE('',*,*,#9689,.F.);
#13408=ORIENTED_EDGE('',*,*,#9723,.F.);
#13409=ORIENTED_EDGE('',*,*,#9821,.T.);
#13410=ORIENTED_EDGE('',*,*,#9699,.F.);
#13411=ORIENTED_EDGE('',*,*,#9824,.T.);
#13412=ORIENTED_EDGE('',*,*,#9703,.F.);
#13413=ORIENTED_EDGE('',*,*,#9826,.F.);
#13414=ORIENTED_EDGE('',*,*,#9827,.T.);
#13415=ORIENTED_EDGE('',*,*,#9806,.F.);
#13416=ORIENTED_EDGE('',*,*,#9828,.T.);
#13417=ORIENTED_EDGE('',*,*,#9829,.F.);
#13418=ORIENTED_EDGE('',*,*,#9830,.F.);
#13419=ORIENTED_EDGE('',*,*,#9807,.F.);
#13420=ORIENTED_EDGE('',*,*,#9830,.T.);
#13421=ORIENTED_EDGE('',*,*,#9831,.T.);
#13422=ORIENTED_EDGE('',*,*,#9804,.F.);
#13423=ORIENTED_EDGE('',*,*,#9831,.F.);
#13424=ORIENTED_EDGE('',*,*,#9829,.T.);
#13425=ORIENTED_EDGE('',*,*,#9832,.T.);
#13426=ORIENTED_EDGE('',*,*,#9805,.F.);
#13427=ORIENTED_EDGE('',*,*,#9832,.F.);
#13428=ORIENTED_EDGE('',*,*,#9828,.F.);
#13429=ORIENTED_EDGE('',*,*,#9802,.F.);
#13430=ORIENTED_EDGE('',*,*,#9833,.T.);
#13431=ORIENTED_EDGE('',*,*,#9834,.F.);
#13432=ORIENTED_EDGE('',*,*,#9835,.F.);
#13433=ORIENTED_EDGE('',*,*,#9803,.F.);
#13434=ORIENTED_EDGE('',*,*,#9835,.T.);
#13435=ORIENTED_EDGE('',*,*,#9836,.T.);
#13436=ORIENTED_EDGE('',*,*,#9800,.F.);
#13437=ORIENTED_EDGE('',*,*,#9836,.F.);
#13438=ORIENTED_EDGE('',*,*,#9834,.T.);
#13439=ORIENTED_EDGE('',*,*,#9837,.T.);
#13440=ORIENTED_EDGE('',*,*,#9801,.F.);
#13441=ORIENTED_EDGE('',*,*,#9837,.F.);
#13442=ORIENTED_EDGE('',*,*,#9833,.F.);
#13443=ORIENTED_EDGE('',*,*,#9798,.F.);
#13444=ORIENTED_EDGE('',*,*,#9838,.T.);
#13445=ORIENTED_EDGE('',*,*,#9839,.F.);
#13446=ORIENTED_EDGE('',*,*,#9840,.F.);
#13447=ORIENTED_EDGE('',*,*,#9799,.F.);
#13448=ORIENTED_EDGE('',*,*,#9840,.T.);
#13449=ORIENTED_EDGE('',*,*,#9841,.T.);
#13450=ORIENTED_EDGE('',*,*,#9796,.F.);
#13451=ORIENTED_EDGE('',*,*,#9841,.F.);
#13452=ORIENTED_EDGE('',*,*,#9839,.T.);
#13453=ORIENTED_EDGE('',*,*,#9842,.T.);
#13454=ORIENTED_EDGE('',*,*,#9797,.F.);
#13455=ORIENTED_EDGE('',*,*,#9842,.F.);
#13456=ORIENTED_EDGE('',*,*,#9838,.F.);
#13457=ORIENTED_EDGE('',*,*,#9794,.F.);
#13458=ORIENTED_EDGE('',*,*,#9843,.T.);
#13459=ORIENTED_EDGE('',*,*,#9844,.F.);
#13460=ORIENTED_EDGE('',*,*,#9845,.F.);
#13461=ORIENTED_EDGE('',*,*,#9795,.F.);
#13462=ORIENTED_EDGE('',*,*,#9845,.T.);
#13463=ORIENTED_EDGE('',*,*,#9846,.T.);
#13464=ORIENTED_EDGE('',*,*,#9792,.F.);
#13465=ORIENTED_EDGE('',*,*,#9846,.F.);
#13466=ORIENTED_EDGE('',*,*,#9844,.T.);
#13467=ORIENTED_EDGE('',*,*,#9847,.T.);
#13468=ORIENTED_EDGE('',*,*,#9793,.F.);
#13469=ORIENTED_EDGE('',*,*,#9847,.F.);
#13470=ORIENTED_EDGE('',*,*,#9843,.F.);
#13471=ORIENTED_EDGE('',*,*,#9790,.F.);
#13472=ORIENTED_EDGE('',*,*,#9848,.T.);
#13473=ORIENTED_EDGE('',*,*,#9849,.F.);
#13474=ORIENTED_EDGE('',*,*,#9850,.F.);
#13475=ORIENTED_EDGE('',*,*,#9791,.F.);
#13476=ORIENTED_EDGE('',*,*,#9850,.T.);
#13477=ORIENTED_EDGE('',*,*,#9851,.T.);
#13478=ORIENTED_EDGE('',*,*,#9788,.F.);
#13479=ORIENTED_EDGE('',*,*,#9851,.F.);
#13480=ORIENTED_EDGE('',*,*,#9849,.T.);
#13481=ORIENTED_EDGE('',*,*,#9852,.T.);
#13482=ORIENTED_EDGE('',*,*,#9789,.F.);
#13483=ORIENTED_EDGE('',*,*,#9852,.F.);
#13484=ORIENTED_EDGE('',*,*,#9848,.F.);
#13485=ORIENTED_EDGE('',*,*,#9825,.T.);
#13486=ORIENTED_EDGE('',*,*,#9827,.F.);
#13487=ORIENTED_EDGE('',*,*,#9853,.F.);
#13488=ORIENTED_EDGE('',*,*,#9701,.F.);
#13489=ORIENTED_EDGE('',*,*,#9702,.F.);
#13490=ORIENTED_EDGE('',*,*,#9853,.T.);
#13491=ORIENTED_EDGE('',*,*,#9826,.T.);
#13492=ORIENTED_EDGE('',*,*,#9786,.F.);
#13493=ORIENTED_EDGE('',*,*,#9854,.T.);
#13494=ORIENTED_EDGE('',*,*,#9855,.F.);
#13495=ORIENTED_EDGE('',*,*,#9856,.F.);
#13496=ORIENTED_EDGE('',*,*,#9787,.F.);
#13497=ORIENTED_EDGE('',*,*,#9856,.T.);
#13498=ORIENTED_EDGE('',*,*,#9857,.T.);
#13499=ORIENTED_EDGE('',*,*,#9784,.F.);
#13500=ORIENTED_EDGE('',*,*,#9857,.F.);
#13501=ORIENTED_EDGE('',*,*,#9855,.T.);
#13502=ORIENTED_EDGE('',*,*,#9858,.T.);
#13503=ORIENTED_EDGE('',*,*,#9785,.F.);
#13504=ORIENTED_EDGE('',*,*,#9858,.F.);
#13505=ORIENTED_EDGE('',*,*,#9854,.F.);
#13506=ORIENTED_EDGE('',*,*,#9782,.F.);
#13507=ORIENTED_EDGE('',*,*,#9859,.T.);
#13508=ORIENTED_EDGE('',*,*,#9860,.F.);
#13509=ORIENTED_EDGE('',*,*,#9861,.F.);
#13510=ORIENTED_EDGE('',*,*,#9783,.F.);
#13511=ORIENTED_EDGE('',*,*,#9861,.T.);
#13512=ORIENTED_EDGE('',*,*,#9862,.T.);
#13513=ORIENTED_EDGE('',*,*,#9780,.F.);
#13514=ORIENTED_EDGE('',*,*,#9862,.F.);
#13515=ORIENTED_EDGE('',*,*,#9860,.T.);
#13516=ORIENTED_EDGE('',*,*,#9863,.T.);
#13517=ORIENTED_EDGE('',*,*,#9781,.F.);
#13518=ORIENTED_EDGE('',*,*,#9863,.F.);
#13519=ORIENTED_EDGE('',*,*,#9859,.F.);
#13520=ORIENTED_EDGE('',*,*,#9778,.F.);
#13521=ORIENTED_EDGE('',*,*,#9864,.T.);
#13522=ORIENTED_EDGE('',*,*,#9865,.F.);
#13523=ORIENTED_EDGE('',*,*,#9866,.F.);
#13524=ORIENTED_EDGE('',*,*,#9779,.F.);
#13525=ORIENTED_EDGE('',*,*,#9866,.T.);
#13526=ORIENTED_EDGE('',*,*,#9867,.T.);
#13527=ORIENTED_EDGE('',*,*,#9776,.F.);
#13528=ORIENTED_EDGE('',*,*,#9867,.F.);
#13529=ORIENTED_EDGE('',*,*,#9865,.T.);
#13530=ORIENTED_EDGE('',*,*,#9868,.T.);
#13531=ORIENTED_EDGE('',*,*,#9777,.F.);
#13532=ORIENTED_EDGE('',*,*,#9868,.F.);
#13533=ORIENTED_EDGE('',*,*,#9864,.F.);
#13534=ORIENTED_EDGE('',*,*,#9774,.F.);
#13535=ORIENTED_EDGE('',*,*,#9869,.T.);
#13536=ORIENTED_EDGE('',*,*,#9870,.F.);
#13537=ORIENTED_EDGE('',*,*,#9871,.F.);
#13538=ORIENTED_EDGE('',*,*,#9775,.F.);
#13539=ORIENTED_EDGE('',*,*,#9871,.T.);
#13540=ORIENTED_EDGE('',*,*,#9872,.T.);
#13541=ORIENTED_EDGE('',*,*,#9772,.F.);
#13542=ORIENTED_EDGE('',*,*,#9872,.F.);
#13543=ORIENTED_EDGE('',*,*,#9870,.T.);
#13544=ORIENTED_EDGE('',*,*,#9873,.T.);
#13545=ORIENTED_EDGE('',*,*,#9773,.F.);
#13546=ORIENTED_EDGE('',*,*,#9873,.F.);
#13547=ORIENTED_EDGE('',*,*,#9869,.F.);
#13548=ORIENTED_EDGE('',*,*,#9770,.F.);
#13549=ORIENTED_EDGE('',*,*,#9874,.T.);
#13550=ORIENTED_EDGE('',*,*,#9875,.F.);
#13551=ORIENTED_EDGE('',*,*,#9876,.F.);
#13552=ORIENTED_EDGE('',*,*,#9771,.F.);
#13553=ORIENTED_EDGE('',*,*,#9876,.T.);
#13554=ORIENTED_EDGE('',*,*,#9877,.T.);
#13555=ORIENTED_EDGE('',*,*,#9768,.F.);
#13556=ORIENTED_EDGE('',*,*,#9877,.F.);
#13557=ORIENTED_EDGE('',*,*,#9875,.T.);
#13558=ORIENTED_EDGE('',*,*,#9878,.T.);
#13559=ORIENTED_EDGE('',*,*,#9769,.F.);
#13560=ORIENTED_EDGE('',*,*,#9878,.F.);
#13561=ORIENTED_EDGE('',*,*,#9874,.F.);
#13562=ORIENTED_EDGE('',*,*,#9709,.F.);
#13563=ORIENTED_EDGE('',*,*,#9879,.T.);
#13564=ORIENTED_EDGE('',*,*,#9880,.F.);
#13565=ORIENTED_EDGE('',*,*,#9881,.F.);
#13566=ORIENTED_EDGE('',*,*,#9710,.F.);
#13567=ORIENTED_EDGE('',*,*,#9881,.T.);
#13568=ORIENTED_EDGE('',*,*,#9882,.T.);
#13569=ORIENTED_EDGE('',*,*,#9713,.F.);
#13570=ORIENTED_EDGE('',*,*,#9714,.F.);
#13571=ORIENTED_EDGE('',*,*,#9882,.F.);
#13572=ORIENTED_EDGE('',*,*,#9880,.T.);
#13573=ORIENTED_EDGE('',*,*,#9883,.T.);
#13574=ORIENTED_EDGE('',*,*,#9715,.F.);
#13575=ORIENTED_EDGE('',*,*,#9883,.F.);
#13576=ORIENTED_EDGE('',*,*,#9879,.F.);
#13577=ORIENTED_EDGE('',*,*,#9708,.F.);
#13578=ORIENTED_EDGE('',*,*,#9766,.F.);
#13579=ORIENTED_EDGE('',*,*,#9884,.T.);
#13580=ORIENTED_EDGE('',*,*,#9885,.F.);
#13581=ORIENTED_EDGE('',*,*,#9886,.F.);
#13582=ORIENTED_EDGE('',*,*,#9767,.F.);
#13583=ORIENTED_EDGE('',*,*,#9886,.T.);
#13584=ORIENTED_EDGE('',*,*,#9887,.T.);
#13585=ORIENTED_EDGE('',*,*,#9764,.F.);
#13586=ORIENTED_EDGE('',*,*,#9887,.F.);
#13587=ORIENTED_EDGE('',*,*,#9885,.T.);
#13588=ORIENTED_EDGE('',*,*,#9888,.T.);
#13589=ORIENTED_EDGE('',*,*,#9765,.F.);
#13590=ORIENTED_EDGE('',*,*,#9888,.F.);
#13591=ORIENTED_EDGE('',*,*,#9884,.F.);
#13592=ORIENTED_EDGE('',*,*,#9762,.F.);
#13593=ORIENTED_EDGE('',*,*,#9889,.T.);
#13594=ORIENTED_EDGE('',*,*,#9890,.F.);
#13595=ORIENTED_EDGE('',*,*,#9891,.F.);
#13596=ORIENTED_EDGE('',*,*,#9763,.F.);
#13597=ORIENTED_EDGE('',*,*,#9891,.T.);
#13598=ORIENTED_EDGE('',*,*,#9892,.T.);
#13599=ORIENTED_EDGE('',*,*,#9760,.F.);
#13600=ORIENTED_EDGE('',*,*,#9892,.F.);
#13601=ORIENTED_EDGE('',*,*,#9890,.T.);
#13602=ORIENTED_EDGE('',*,*,#9893,.T.);
#13603=ORIENTED_EDGE('',*,*,#9761,.F.);
#13604=ORIENTED_EDGE('',*,*,#9893,.F.);
#13605=ORIENTED_EDGE('',*,*,#9889,.F.);
#13606=ORIENTED_EDGE('',*,*,#9758,.F.);
#13607=ORIENTED_EDGE('',*,*,#9894,.T.);
#13608=ORIENTED_EDGE('',*,*,#9895,.F.);
#13609=ORIENTED_EDGE('',*,*,#9896,.F.);
#13610=ORIENTED_EDGE('',*,*,#9759,.F.);
#13611=ORIENTED_EDGE('',*,*,#9896,.T.);
#13612=ORIENTED_EDGE('',*,*,#9897,.T.);
#13613=ORIENTED_EDGE('',*,*,#9756,.F.);
#13614=ORIENTED_EDGE('',*,*,#9897,.F.);
#13615=ORIENTED_EDGE('',*,*,#9895,.T.);
#13616=ORIENTED_EDGE('',*,*,#9898,.T.);
#13617=ORIENTED_EDGE('',*,*,#9757,.F.);
#13618=ORIENTED_EDGE('',*,*,#9898,.F.);
#13619=ORIENTED_EDGE('',*,*,#9894,.F.);
#13620=ORIENTED_EDGE('',*,*,#9754,.F.);
#13621=ORIENTED_EDGE('',*,*,#9899,.T.);
#13622=ORIENTED_EDGE('',*,*,#9900,.F.);
#13623=ORIENTED_EDGE('',*,*,#9901,.F.);
#13624=ORIENTED_EDGE('',*,*,#9755,.F.);
#13625=ORIENTED_EDGE('',*,*,#9901,.T.);
#13626=ORIENTED_EDGE('',*,*,#9902,.T.);
#13627=ORIENTED_EDGE('',*,*,#9752,.F.);
#13628=ORIENTED_EDGE('',*,*,#9902,.F.);
#13629=ORIENTED_EDGE('',*,*,#9900,.T.);
#13630=ORIENTED_EDGE('',*,*,#9903,.T.);
#13631=ORIENTED_EDGE('',*,*,#9753,.F.);
#13632=ORIENTED_EDGE('',*,*,#9903,.F.);
#13633=ORIENTED_EDGE('',*,*,#9899,.F.);
#13634=ORIENTED_EDGE('',*,*,#9750,.F.);
#13635=ORIENTED_EDGE('',*,*,#9904,.T.);
#13636=ORIENTED_EDGE('',*,*,#9905,.F.);
#13637=ORIENTED_EDGE('',*,*,#9906,.F.);
#13638=ORIENTED_EDGE('',*,*,#9751,.F.);
#13639=ORIENTED_EDGE('',*,*,#9906,.T.);
#13640=ORIENTED_EDGE('',*,*,#9907,.T.);
#13641=ORIENTED_EDGE('',*,*,#9748,.F.);
#13642=ORIENTED_EDGE('',*,*,#9907,.F.);
#13643=ORIENTED_EDGE('',*,*,#9905,.T.);
#13644=ORIENTED_EDGE('',*,*,#9908,.T.);
#13645=ORIENTED_EDGE('',*,*,#9749,.F.);
#13646=ORIENTED_EDGE('',*,*,#9908,.F.);
#13647=ORIENTED_EDGE('',*,*,#9904,.F.);
#13648=ORIENTED_EDGE('',*,*,#9823,.T.);
#13649=ORIENTED_EDGE('',*,*,#9909,.F.);
#13650=ORIENTED_EDGE('',*,*,#9910,.F.);
#13651=ORIENTED_EDGE('',*,*,#9719,.F.);
#13652=ORIENTED_EDGE('',*,*,#9720,.F.);
#13653=ORIENTED_EDGE('',*,*,#9910,.T.);
#13654=ORIENTED_EDGE('',*,*,#9911,.T.);
#13655=ORIENTED_EDGE('',*,*,#9822,.T.);
#13656=ORIENTED_EDGE('',*,*,#9721,.F.);
#13657=ORIENTED_EDGE('',*,*,#9911,.F.);
#13658=ORIENTED_EDGE('',*,*,#9909,.T.);
#13659=ORIENTED_EDGE('',*,*,#9746,.F.);
#13660=ORIENTED_EDGE('',*,*,#9912,.T.);
#13661=ORIENTED_EDGE('',*,*,#9913,.F.);
#13662=ORIENTED_EDGE('',*,*,#9914,.F.);
#13663=ORIENTED_EDGE('',*,*,#9747,.F.);
#13664=ORIENTED_EDGE('',*,*,#9914,.T.);
#13665=ORIENTED_EDGE('',*,*,#9915,.T.);
#13666=ORIENTED_EDGE('',*,*,#9744,.F.);
#13667=ORIENTED_EDGE('',*,*,#9915,.F.);
#13668=ORIENTED_EDGE('',*,*,#9913,.T.);
#13669=ORIENTED_EDGE('',*,*,#9916,.T.);
#13670=ORIENTED_EDGE('',*,*,#9745,.F.);
#13671=ORIENTED_EDGE('',*,*,#9916,.F.);
#13672=ORIENTED_EDGE('',*,*,#9912,.F.);
#13673=ORIENTED_EDGE('',*,*,#9742,.F.);
#13674=ORIENTED_EDGE('',*,*,#9917,.T.);
#13675=ORIENTED_EDGE('',*,*,#9918,.F.);
#13676=ORIENTED_EDGE('',*,*,#9919,.F.);
#13677=ORIENTED_EDGE('',*,*,#9743,.F.);
#13678=ORIENTED_EDGE('',*,*,#9919,.T.);
#13679=ORIENTED_EDGE('',*,*,#9920,.T.);
#13680=ORIENTED_EDGE('',*,*,#9740,.F.);
#13681=ORIENTED_EDGE('',*,*,#9920,.F.);
#13682=ORIENTED_EDGE('',*,*,#9918,.T.);
#13683=ORIENTED_EDGE('',*,*,#9921,.T.);
#13684=ORIENTED_EDGE('',*,*,#9741,.F.);
#13685=ORIENTED_EDGE('',*,*,#9921,.F.);
#13686=ORIENTED_EDGE('',*,*,#9917,.F.);
#13687=ORIENTED_EDGE('',*,*,#9738,.F.);
#13688=ORIENTED_EDGE('',*,*,#9922,.T.);
#13689=ORIENTED_EDGE('',*,*,#9923,.F.);
#13690=ORIENTED_EDGE('',*,*,#9924,.F.);
#13691=ORIENTED_EDGE('',*,*,#9739,.F.);
#13692=ORIENTED_EDGE('',*,*,#9924,.T.);
#13693=ORIENTED_EDGE('',*,*,#9925,.T.);
#13694=ORIENTED_EDGE('',*,*,#9736,.F.);
#13695=ORIENTED_EDGE('',*,*,#9925,.F.);
#13696=ORIENTED_EDGE('',*,*,#9923,.T.);
#13697=ORIENTED_EDGE('',*,*,#9926,.T.);
#13698=ORIENTED_EDGE('',*,*,#9737,.F.);
#13699=ORIENTED_EDGE('',*,*,#9926,.F.);
#13700=ORIENTED_EDGE('',*,*,#9922,.F.);
#13701=ORIENTED_EDGE('',*,*,#9734,.F.);
#13702=ORIENTED_EDGE('',*,*,#9927,.T.);
#13703=ORIENTED_EDGE('',*,*,#9928,.F.);
#13704=ORIENTED_EDGE('',*,*,#9929,.F.);
#13705=ORIENTED_EDGE('',*,*,#9735,.F.);
#13706=ORIENTED_EDGE('',*,*,#9929,.T.);
#13707=ORIENTED_EDGE('',*,*,#9930,.T.);
#13708=ORIENTED_EDGE('',*,*,#9732,.F.);
#13709=ORIENTED_EDGE('',*,*,#9930,.F.);
#13710=ORIENTED_EDGE('',*,*,#9928,.T.);
#13711=ORIENTED_EDGE('',*,*,#9931,.T.);
#13712=ORIENTED_EDGE('',*,*,#9733,.F.);
#13713=ORIENTED_EDGE('',*,*,#9931,.F.);
#13714=ORIENTED_EDGE('',*,*,#9927,.F.);
#13715=ORIENTED_EDGE('',*,*,#9730,.F.);
#13716=ORIENTED_EDGE('',*,*,#9932,.T.);
#13717=ORIENTED_EDGE('',*,*,#9933,.F.);
#13718=ORIENTED_EDGE('',*,*,#9934,.F.);
#13719=ORIENTED_EDGE('',*,*,#9731,.F.);
#13720=ORIENTED_EDGE('',*,*,#9934,.T.);
#13721=ORIENTED_EDGE('',*,*,#9935,.T.);
#13722=ORIENTED_EDGE('',*,*,#9728,.F.);
#13723=ORIENTED_EDGE('',*,*,#9935,.F.);
#13724=ORIENTED_EDGE('',*,*,#9933,.T.);
#13725=ORIENTED_EDGE('',*,*,#9936,.T.);
#13726=ORIENTED_EDGE('',*,*,#9729,.F.);
#13727=ORIENTED_EDGE('',*,*,#9936,.F.);
#13728=ORIENTED_EDGE('',*,*,#9932,.F.);
#13729=ORIENTED_EDGE('',*,*,#9726,.F.);
#13730=ORIENTED_EDGE('',*,*,#9937,.T.);
#13731=ORIENTED_EDGE('',*,*,#9938,.F.);
#13732=ORIENTED_EDGE('',*,*,#9939,.F.);
#13733=ORIENTED_EDGE('',*,*,#9727,.F.);
#13734=ORIENTED_EDGE('',*,*,#9939,.T.);
#13735=ORIENTED_EDGE('',*,*,#9940,.T.);
#13736=ORIENTED_EDGE('',*,*,#9724,.F.);
#13737=ORIENTED_EDGE('',*,*,#9940,.F.);
#13738=ORIENTED_EDGE('',*,*,#9938,.T.);
#13739=ORIENTED_EDGE('',*,*,#9941,.T.);
#13740=ORIENTED_EDGE('',*,*,#9725,.F.);
#13741=ORIENTED_EDGE('',*,*,#9941,.F.);
#13742=ORIENTED_EDGE('',*,*,#9937,.F.);
#13743=ORIENTED_EDGE('',*,*,#9942,.F.);
#13744=ORIENTED_EDGE('',*,*,#9813,.F.);
#13745=ORIENTED_EDGE('',*,*,#9607,.F.);
#13746=ORIENTED_EDGE('',*,*,#9814,.F.);
#13747=ORIENTED_EDGE('',*,*,#9943,.T.);
#13748=ORIENTED_EDGE('',*,*,#9942,.T.);
#13749=ORIENTED_EDGE('',*,*,#9943,.F.);
#13750=ORIENTED_EDGE('',*,*,#9642,.T.);
#13751=ORIENTED_EDGE('',*,*,#9810,.T.);
#13752=ORIENTED_EDGE('',*,*,#9944,.F.);
#13753=ORIENTED_EDGE('',*,*,#9819,.T.);
#13754=ORIENTED_EDGE('',*,*,#9945,.F.);
#13755=ORIENTED_EDGE('',*,*,#9944,.T.);
#13756=ORIENTED_EDGE('',*,*,#9809,.T.);
#13757=ORIENTED_EDGE('',*,*,#9650,.T.);
#13758=ORIENTED_EDGE('',*,*,#9647,.T.);
#13759=ORIENTED_EDGE('',*,*,#9818,.T.);
#13760=ORIENTED_EDGE('',*,*,#9712,.F.);
#13761=ORIENTED_EDGE('',*,*,#9946,.T.);
#13762=ORIENTED_EDGE('',*,*,#9945,.T.);
#13763=ORIENTED_EDGE('',*,*,#9946,.F.);
#13764=ORIENTED_EDGE('',*,*,#9687,.F.);
#13765=ORIENTED_EDGE('',*,*,#9691,.F.);
#13766=ORIENTED_EDGE('',*,*,#9685,.F.);
#13767=ORIENTED_EDGE('',*,*,#9698,.T.);
#15507=CONICAL_SURFACE('',#17437,6.8,0.785398163397415);
#15508=CONICAL_SURFACE('',#17544,4.8,0.785398163397415);
#15509=CONICAL_SURFACE('',#17549,6.8,0.785398163397415);
#15510=CONICAL_SURFACE('',#17550,6.8,0.785398163397415);
#16006=ADVANCED_FACE('',(#2278),#1718,.T.);
#16007=ADVANCED_FACE('',(#2279),#1719,.T.);
#16008=ADVANCED_FACE('',(#2280),#1720,.T.);
#16009=ADVANCED_FACE('',(#2281),#1721,.T.);
#16010=ADVANCED_FACE('',(#2282),#1722,.T.);
#16011=ADVANCED_FACE('',(#2283),#1723,.T.);
#16012=ADVANCED_FACE('',(#2284),#1724,.T.);
#16013=ADVANCED_FACE('',(#2285),#1725,.T.);
#16014=ADVANCED_FACE('',(#2286),#1726,.T.);
#16015=ADVANCED_FACE('',(#2287),#1727,.T.);
#16016=ADVANCED_FACE('',(#2288),#1728,.T.);
#16017=ADVANCED_FACE('',(#2289),#1729,.T.);
#16018=ADVANCED_FACE('',(#2290),#1730,.T.);
#16019=ADVANCED_FACE('',(#2291),#1731,.T.);
#16020=ADVANCED_FACE('',(#2292),#1732,.T.);
#16021=ADVANCED_FACE('',(#2293),#1733,.T.);
#16022=ADVANCED_FACE('',(#2294),#1734,.T.);
#16023=ADVANCED_FACE('',(#2295),#1735,.T.);
#16024=ADVANCED_FACE('',(#2296),#1736,.T.);
#16025=ADVANCED_FACE('',(#2297),#1737,.T.);
#16026=ADVANCED_FACE('',(#2298),#1738,.T.);
#16027=ADVANCED_FACE('',(#2299),#1739,.T.);
#16028=ADVANCED_FACE('',(#2300),#1740,.T.);
#16029=ADVANCED_FACE('',(#2301),#1741,.T.);
#16030=ADVANCED_FACE('',(#2302),#1742,.T.);
#16031=ADVANCED_FACE('',(#2303),#1743,.T.);
#16032=ADVANCED_FACE('',(#2304),#1225,.T.);
#16033=ADVANCED_FACE('',(#2305),#1226,.T.);
#16034=ADVANCED_FACE('',(#2306),#1227,.T.);
#16035=ADVANCED_FACE('',(#2307,#979,#980,#981,#982,#983,#984,#985,#986,
#987,#988,#989,#990,#991,#992,#993,#994,#995,#996,#997,#998,#999),#1744,
 .T.);
#16036=ADVANCED_FACE('',(#2308),#15507,.T.);
#16037=ADVANCED_FACE('',(#2309),#1228,.T.);
#16038=ADVANCED_FACE('',(#2310),#905,.F.);
#16039=ADVANCED_FACE('',(#2311),#1229,.T.);
#16040=ADVANCED_FACE('',(#2312),#1745,.T.);
#16041=ADVANCED_FACE('',(#2313),#906,.F.);
#16042=ADVANCED_FACE('',(#2314),#1230,.F.);
#16043=ADVANCED_FACE('',(#2315),#1231,.F.);
#16044=ADVANCED_FACE('',(#2316),#1232,.F.);
#16045=ADVANCED_FACE('',(#2317),#1233,.F.);
#16046=ADVANCED_FACE('',(#2318),#1234,.F.);
#16047=ADVANCED_FACE('',(#2319),#1235,.T.);
#16048=ADVANCED_FACE('',(#2320),#1236,.F.);
#16049=ADVANCED_FACE('',(#2321),#1237,.F.);
#16050=ADVANCED_FACE('',(#2322),#1238,.F.);
#16051=ADVANCED_FACE('',(#2323),#1239,.T.);
#16052=ADVANCED_FACE('',(#2324),#1240,.F.);
#16053=ADVANCED_FACE('',(#2325),#1241,.F.);
#16054=ADVANCED_FACE('',(#2326),#1242,.F.);
#16055=ADVANCED_FACE('',(#2327),#1243,.T.);
#16056=ADVANCED_FACE('',(#2328),#1244,.F.);
#16057=ADVANCED_FACE('',(#2329),#1245,.F.);
#16058=ADVANCED_FACE('',(#2330),#1246,.F.);
#16059=ADVANCED_FACE('',(#2331),#1247,.T.);
#16060=ADVANCED_FACE('',(#2332),#1248,.F.);
#16061=ADVANCED_FACE('',(#2333),#1249,.F.);
#16062=ADVANCED_FACE('',(#2334),#1250,.F.);
#16063=ADVANCED_FACE('',(#2335),#1251,.T.);
#16064=ADVANCED_FACE('',(#2336),#1252,.F.);
#16065=ADVANCED_FACE('',(#2337),#1253,.F.);
#16066=ADVANCED_FACE('',(#2338),#1254,.F.);
#16067=ADVANCED_FACE('',(#2339),#1255,.T.);
#16068=ADVANCED_FACE('',(#2340),#1256,.F.);
#16069=ADVANCED_FACE('',(#2341),#1257,.T.);
#16070=ADVANCED_FACE('',(#2342),#1258,.F.);
#16071=ADVANCED_FACE('',(#2343),#1259,.F.);
#16072=ADVANCED_FACE('',(#2344),#1260,.F.);
#16073=ADVANCED_FACE('',(#2345),#1261,.T.);
#16074=ADVANCED_FACE('',(#2346),#1262,.F.);
#16075=ADVANCED_FACE('',(#2347),#1263,.F.);
#16076=ADVANCED_FACE('',(#2348),#1264,.F.);
#16077=ADVANCED_FACE('',(#2349),#1265,.T.);
#16078=ADVANCED_FACE('',(#2350),#1266,.F.);
#16079=ADVANCED_FACE('',(#2351),#1267,.F.);
#16080=ADVANCED_FACE('',(#2352),#1268,.F.);
#16081=ADVANCED_FACE('',(#2353),#1269,.T.);
#16082=ADVANCED_FACE('',(#2354),#1270,.F.);
#16083=ADVANCED_FACE('',(#2355),#1271,.F.);
#16084=ADVANCED_FACE('',(#2356),#1272,.F.);
#16085=ADVANCED_FACE('',(#2357),#1273,.T.);
#16086=ADVANCED_FACE('',(#2358),#1274,.F.);
#16087=ADVANCED_FACE('',(#2359),#1275,.F.);
#16088=ADVANCED_FACE('',(#2360),#1276,.F.);
#16089=ADVANCED_FACE('',(#2361),#1277,.T.);
#16090=ADVANCED_FACE('',(#2362),#1278,.F.);
#16091=ADVANCED_FACE('',(#2363),#1279,.F.);
#16092=ADVANCED_FACE('',(#2364),#1280,.F.);
#16093=ADVANCED_FACE('',(#2365),#1281,.T.);
#16094=ADVANCED_FACE('',(#2366),#1282,.F.);
#16095=ADVANCED_FACE('',(#2367),#1283,.F.);
#16096=ADVANCED_FACE('',(#2368),#1284,.F.);
#16097=ADVANCED_FACE('',(#2369),#1285,.T.);
#16098=ADVANCED_FACE('',(#2370),#1286,.F.);
#16099=ADVANCED_FACE('',(#2371),#1287,.F.);
#16100=ADVANCED_FACE('',(#2372),#1288,.F.);
#16101=ADVANCED_FACE('',(#2373),#1289,.T.);
#16102=ADVANCED_FACE('',(#2374),#1290,.F.);
#16103=ADVANCED_FACE('',(#2375),#1291,.F.);
#16104=ADVANCED_FACE('',(#2376),#1292,.F.);
#16105=ADVANCED_FACE('',(#2377),#1293,.T.);
#16106=ADVANCED_FACE('',(#2378),#1294,.F.);
#16107=ADVANCED_FACE('',(#2379),#1295,.F.);
#16108=ADVANCED_FACE('',(#2380),#1296,.F.);
#16109=ADVANCED_FACE('',(#2381),#1297,.T.);
#16110=ADVANCED_FACE('',(#2382),#1298,.F.);
#16111=ADVANCED_FACE('',(#2383),#1299,.F.);
#16112=ADVANCED_FACE('',(#2384),#1300,.F.);
#16113=ADVANCED_FACE('',(#2385),#1301,.T.);
#16114=ADVANCED_FACE('',(#2386),#1302,.F.);
#16115=ADVANCED_FACE('',(#2387),#1303,.F.);
#16116=ADVANCED_FACE('',(#2388),#1304,.T.);
#16117=ADVANCED_FACE('',(#2389),#1305,.F.);
#16118=ADVANCED_FACE('',(#2390),#1306,.F.);
#16119=ADVANCED_FACE('',(#2391),#1307,.F.);
#16120=ADVANCED_FACE('',(#2392),#1308,.T.);
#16121=ADVANCED_FACE('',(#2393),#1309,.F.);
#16122=ADVANCED_FACE('',(#2394),#1310,.F.);
#16123=ADVANCED_FACE('',(#2395),#1311,.F.);
#16124=ADVANCED_FACE('',(#2396),#1312,.T.);
#16125=ADVANCED_FACE('',(#2397),#1313,.F.);
#16126=ADVANCED_FACE('',(#2398),#1314,.F.);
#16127=ADVANCED_FACE('',(#2399),#1315,.F.);
#16128=ADVANCED_FACE('',(#2400),#1316,.T.);
#16129=ADVANCED_FACE('',(#2401),#1317,.F.);
#16130=ADVANCED_FACE('',(#2402),#1318,.F.);
#16131=ADVANCED_FACE('',(#2403),#1319,.F.);
#16132=ADVANCED_FACE('',(#2404),#1320,.T.);
#16133=ADVANCED_FACE('',(#2405),#1321,.F.);
#16134=ADVANCED_FACE('',(#2406),#1322,.F.);
#16135=ADVANCED_FACE('',(#2407),#1323,.F.);
#16136=ADVANCED_FACE('',(#2408),#1324,.T.);
#16137=ADVANCED_FACE('',(#2409),#1325,.F.);
#16138=ADVANCED_FACE('',(#2410),#1326,.F.);
#16139=ADVANCED_FACE('',(#2411),#1327,.T.);
#16140=ADVANCED_FACE('',(#2412),#15508,.T.);
#16141=ADVANCED_FACE('',(#2413),#1746,.T.);
#16142=ADVANCED_FACE('',(#2414,#1000),#1328,.T.);
#16143=ADVANCED_FACE('',(#2415),#15509,.T.);
#16144=ADVANCED_FACE('',(#2416),#15510,.T.);
#16527=CLOSED_SHELL('',(#16006,#16007,#16008,#16009,#16010,#16011,#16012,
#16013,#16014,#16015,#16016,#16017,#16018,#16019,#16020,#16021,#16022,#16023,
#16024,#16025,#16026,#16027,#16028,#16029,#16030,#16031,#16032,#16033,#16034,
#16035,#16036,#16037,#16038,#16039,#16040,#16041,#16042,#16043,#16044,#16045,
#16046,#16047,#16048,#16049,#16050,#16051,#16052,#16053,#16054,#16055,#16056,
#16057,#16058,#16059,#16060,#16061,#16062,#16063,#16064,#16065,#16066,#16067,
#16068,#16069,#16070,#16071,#16072,#16073,#16074,#16075,#16076,#16077,#16078,
#16079,#16080,#16081,#16082,#16083,#16084,#16085,#16086,#16087,#16088,#16089,
#16090,#16091,#16092,#16093,#16094,#16095,#16096,#16097,#16098,#16099,#16100,
#16101,#16102,#16103,#16104,#16105,#16106,#16107,#16108,#16109,#16110,#16111,
#16112,#16113,#16114,#16115,#16116,#16117,#16118,#16119,#16120,#16121,#16122,
#16123,#16124,#16125,#16126,#16127,#16128,#16129,#16130,#16131,#16132,#16133,
#16134,#16135,#16136,#16137,#16138,#16139,#16140,#16141,#16142,#16143,#16144));
#17342=AXIS2_PLACEMENT_3D('',#36658,#19858,#19859);
#17343=AXIS2_PLACEMENT_3D('',#36659,#19860,#19861);
#17344=AXIS2_PLACEMENT_3D('',#36681,#19863,#19864);
#17345=AXIS2_PLACEMENT_3D('',#36692,#19865,#19866);
#17346=AXIS2_PLACEMENT_3D('',#36776,#19868,#19869);
#17347=AXIS2_PLACEMENT_3D('',#36866,#19871,#19872);
#17348=AXIS2_PLACEMENT_3D('',#36956,#19874,#19875);
#17349=AXIS2_PLACEMENT_3D('',#37040,#19877,#19878);
#17350=AXIS2_PLACEMENT_3D('',#37130,#19880,#19881);
#17351=AXIS2_PLACEMENT_3D('',#37217,#19883,#19884);
#17352=AXIS2_PLACEMENT_3D('',#37304,#19886,#19887);
#17353=AXIS2_PLACEMENT_3D('',#37394,#19889,#19890);
#17354=AXIS2_PLACEMENT_3D('',#37478,#19892,#19893);
#17355=AXIS2_PLACEMENT_3D('',#37568,#19895,#19896);
#17356=AXIS2_PLACEMENT_3D('',#37658,#19898,#19899);
#17357=AXIS2_PLACEMENT_3D('',#37742,#19901,#19902);
#17358=AXIS2_PLACEMENT_3D('',#37751,#19904,#19905);
#17359=AXIS2_PLACEMENT_3D('',#37752,#19906,#19907);
#17360=AXIS2_PLACEMENT_3D('',#37773,#19909,#19910);
#17361=AXIS2_PLACEMENT_3D('',#37788,#19911,#19912);
#17362=AXIS2_PLACEMENT_3D('',#37825,#19914,#19915);
#17363=AXIS2_PLACEMENT_3D('',#37863,#19917,#19918);
#17364=AXIS2_PLACEMENT_3D('',#37900,#19920,#19921);
#17365=AXIS2_PLACEMENT_3D('',#37937,#19923,#19924);
#17366=AXIS2_PLACEMENT_3D('',#37975,#19926,#19927);
#17367=AXIS2_PLACEMENT_3D('',#38011,#19929,#19930);
#17368=AXIS2_PLACEMENT_3D('',#38049,#19932,#19933);
#17369=AXIS2_PLACEMENT_3D('',#38086,#19935,#19936);
#17370=AXIS2_PLACEMENT_3D('',#38123,#19938,#19939);
#17371=AXIS2_PLACEMENT_3D('',#38161,#19941,#19942);
#17372=AXIS2_PLACEMENT_3D('',#38198,#19944,#19945);
#17373=AXIS2_PLACEMENT_3D('',#38211,#19947,#19948);
#17374=AXIS2_PLACEMENT_3D('',#38214,#19950,#19951);
#17375=AXIS2_PLACEMENT_3D('',#38215,#19952,#19953);
#17376=AXIS2_PLACEMENT_3D('',#38216,#19954,#19955);
#17377=AXIS2_PLACEMENT_3D('',#38217,#19956,#19957);
#17378=AXIS2_PLACEMENT_3D('',#38230,#19959,#19960);
#17379=AXIS2_PLACEMENT_3D('',#38233,#19962,#19963);
#17380=AXIS2_PLACEMENT_3D('',#38234,#19964,#19965);
#17381=AXIS2_PLACEMENT_3D('',#38235,#19966,#19967);
#17382=AXIS2_PLACEMENT_3D('',#38239,#19969,#19970);
#17383=AXIS2_PLACEMENT_3D('',#38243,#19972,#19973);
#17384=AXIS2_PLACEMENT_3D('',#38247,#19975,#19976);
#17385=AXIS2_PLACEMENT_3D('',#38250,#19978,#19979);
#17386=AXIS2_PLACEMENT_3D('',#38254,#19981,#19982);
#17387=AXIS2_PLACEMENT_3D('',#38258,#19984,#19985);
#17388=AXIS2_PLACEMENT_3D('',#38261,#19987,#19988);
#17389=AXIS2_PLACEMENT_3D('',#38263,#19989,#19990);
#17390=AXIS2_PLACEMENT_3D('',#38266,#19992,#19993);
#17391=AXIS2_PLACEMENT_3D('',#38267,#19994,#19995);
#17392=AXIS2_PLACEMENT_3D('',#38271,#19997,#19998);
#17393=AXIS2_PLACEMENT_3D('',#38275,#20000,#20001);
#17394=AXIS2_PLACEMENT_3D('',#38279,#20003,#20004);
#17395=AXIS2_PLACEMENT_3D('',#38285,#20007,#20008);
#17396=AXIS2_PLACEMENT_3D('',#38288,#20010,#20011);
#17397=AXIS2_PLACEMENT_3D('',#38293,#20013,#20014);
#17398=AXIS2_PLACEMENT_3D('',#38296,#20016,#20017);
#17399=AXIS2_PLACEMENT_3D('',#38301,#20019,#20020);
#17400=AXIS2_PLACEMENT_3D('',#38304,#20022,#20023);
#17401=AXIS2_PLACEMENT_3D('',#38309,#20025,#20026);
#17402=AXIS2_PLACEMENT_3D('',#38312,#20028,#20029);
#17403=AXIS2_PLACEMENT_3D('',#38317,#20031,#20032);
#17404=AXIS2_PLACEMENT_3D('',#38320,#20034,#20035);
#17405=AXIS2_PLACEMENT_3D('',#38325,#20037,#20038);
#17406=AXIS2_PLACEMENT_3D('',#38328,#20040,#20041);
#17407=AXIS2_PLACEMENT_3D('',#38333,#20043,#20044);
#17408=AXIS2_PLACEMENT_3D('',#38336,#20046,#20047);
#17409=AXIS2_PLACEMENT_3D('',#38341,#20049,#20050);
#17410=AXIS2_PLACEMENT_3D('',#38344,#20052,#20053);
#17411=AXIS2_PLACEMENT_3D('',#38349,#20055,#20056);
#17412=AXIS2_PLACEMENT_3D('',#38352,#20058,#20059);
#17413=AXIS2_PLACEMENT_3D('',#38357,#20061,#20062);
#17414=AXIS2_PLACEMENT_3D('',#38360,#20064,#20065);
#17415=AXIS2_PLACEMENT_3D('',#38365,#20067,#20068);
#17416=AXIS2_PLACEMENT_3D('',#38368,#20070,#20071);
#17417=AXIS2_PLACEMENT_3D('',#38373,#20073,#20074);
#17418=AXIS2_PLACEMENT_3D('',#38376,#20076,#20077);
#17419=AXIS2_PLACEMENT_3D('',#38381,#20079,#20080);
#17420=AXIS2_PLACEMENT_3D('',#38384,#20082,#20083);
#17421=AXIS2_PLACEMENT_3D('',#38389,#20085,#20086);
#17422=AXIS2_PLACEMENT_3D('',#38392,#20088,#20089);
#17423=AXIS2_PLACEMENT_3D('',#38397,#20091,#20092);
#17424=AXIS2_PLACEMENT_3D('',#38400,#20094,#20095);
#17425=AXIS2_PLACEMENT_3D('',#38405,#20097,#20098);
#17426=AXIS2_PLACEMENT_3D('',#38408,#20100,#20101);
#17427=AXIS2_PLACEMENT_3D('',#38413,#20103,#20104);
#17428=AXIS2_PLACEMENT_3D('',#38416,#20106,#20107);
#17429=AXIS2_PLACEMENT_3D('',#38421,#20109,#20110);
#17430=AXIS2_PLACEMENT_3D('',#38424,#20112,#20113);
#17431=AXIS2_PLACEMENT_3D('',#38429,#20115,#20116);
#17432=AXIS2_PLACEMENT_3D('',#38432,#20118,#20119);
#17433=AXIS2_PLACEMENT_3D('',#38437,#20121,#20122);
#17434=AXIS2_PLACEMENT_3D('',#38440,#20124,#20125);
#17435=AXIS2_PLACEMENT_3D('',#38445,#20127,#20128);
#17436=AXIS2_PLACEMENT_3D('',#38448,#20130,#20131);
#17437=AXIS2_PLACEMENT_3D('',#38449,#20132,#20133);
#17438=AXIS2_PLACEMENT_3D('',#38450,#20134,#20135);
#17439=AXIS2_PLACEMENT_3D('',#38451,#20136,#20137);
#17440=AXIS2_PLACEMENT_3D('',#39361,#20138,#20139);
#17441=AXIS2_PLACEMENT_3D('',#39363,#20140,#20141);
#17442=AXIS2_PLACEMENT_3D('',#39364,#20142,#20143);
#17443=AXIS2_PLACEMENT_3D('',#39466,#20144,#20145);
#17444=AXIS2_PLACEMENT_3D('',#39467,#20146,#20147);
#17445=AXIS2_PLACEMENT_3D('',#40268,#20148,#20149);
#17446=AXIS2_PLACEMENT_3D('',#40270,#20151,#20152);
#17447=AXIS2_PLACEMENT_3D('',#40278,#20158,#20159);
#17448=AXIS2_PLACEMENT_3D('',#40279,#20160,#20161);
#17449=AXIS2_PLACEMENT_3D('',#40283,#20164,#20165);
#17450=AXIS2_PLACEMENT_3D('',#40289,#20169,#20170);
#17451=AXIS2_PLACEMENT_3D('',#40291,#20172,#20173);
#17452=AXIS2_PLACEMENT_3D('',#40293,#20175,#20176);
#17453=AXIS2_PLACEMENT_3D('',#40294,#20177,#20178);
#17454=AXIS2_PLACEMENT_3D('',#40300,#20182,#20183);
#17455=AXIS2_PLACEMENT_3D('',#40302,#20185,#20186);
#17456=AXIS2_PLACEMENT_3D('',#40304,#20188,#20189);
#17457=AXIS2_PLACEMENT_3D('',#40305,#20190,#20191);
#17458=AXIS2_PLACEMENT_3D('',#40311,#20195,#20196);
#17459=AXIS2_PLACEMENT_3D('',#40313,#20198,#20199);
#17460=AXIS2_PLACEMENT_3D('',#40315,#20201,#20202);
#17461=AXIS2_PLACEMENT_3D('',#40316,#20203,#20204);
#17462=AXIS2_PLACEMENT_3D('',#40322,#20208,#20209);
#17463=AXIS2_PLACEMENT_3D('',#40324,#20211,#20212);
#17464=AXIS2_PLACEMENT_3D('',#40326,#20214,#20215);
#17465=AXIS2_PLACEMENT_3D('',#40327,#20216,#20217);
#17466=AXIS2_PLACEMENT_3D('',#40333,#20221,#20222);
#17467=AXIS2_PLACEMENT_3D('',#40335,#20224,#20225);
#17468=AXIS2_PLACEMENT_3D('',#40337,#20227,#20228);
#17469=AXIS2_PLACEMENT_3D('',#40338,#20229,#20230);
#17470=AXIS2_PLACEMENT_3D('',#40340,#20232,#20233);
#17471=AXIS2_PLACEMENT_3D('',#40341,#20234,#20235);
#17472=AXIS2_PLACEMENT_3D('',#40347,#20239,#20240);
#17473=AXIS2_PLACEMENT_3D('',#40349,#20242,#20243);
#17474=AXIS2_PLACEMENT_3D('',#40351,#20245,#20246);
#17475=AXIS2_PLACEMENT_3D('',#40352,#20247,#20248);
#17476=AXIS2_PLACEMENT_3D('',#40358,#20252,#20253);
#17477=AXIS2_PLACEMENT_3D('',#40360,#20255,#20256);
#17478=AXIS2_PLACEMENT_3D('',#40362,#20258,#20259);
#17479=AXIS2_PLACEMENT_3D('',#40363,#20260,#20261);
#17480=AXIS2_PLACEMENT_3D('',#40369,#20265,#20266);
#17481=AXIS2_PLACEMENT_3D('',#40371,#20268,#20269);
#17482=AXIS2_PLACEMENT_3D('',#40373,#20271,#20272);
#17483=AXIS2_PLACEMENT_3D('',#40374,#20273,#20274);
#17484=AXIS2_PLACEMENT_3D('',#40380,#20278,#20279);
#17485=AXIS2_PLACEMENT_3D('',#40382,#20281,#20282);
#17486=AXIS2_PLACEMENT_3D('',#40384,#20284,#20285);
#17487=AXIS2_PLACEMENT_3D('',#40385,#20286,#20287);
#17488=AXIS2_PLACEMENT_3D('',#40391,#20291,#20292);
#17489=AXIS2_PLACEMENT_3D('',#40393,#20294,#20295);
#17490=AXIS2_PLACEMENT_3D('',#40395,#20297,#20298);
#17491=AXIS2_PLACEMENT_3D('',#40396,#20299,#20300);
#17492=AXIS2_PLACEMENT_3D('',#40402,#20304,#20305);
#17493=AXIS2_PLACEMENT_3D('',#40404,#20307,#20308);
#17494=AXIS2_PLACEMENT_3D('',#40406,#20310,#20311);
#17495=AXIS2_PLACEMENT_3D('',#40407,#20312,#20313);
#17496=AXIS2_PLACEMENT_3D('',#40413,#20317,#20318);
#17497=AXIS2_PLACEMENT_3D('',#40415,#20320,#20321);
#17498=AXIS2_PLACEMENT_3D('',#40417,#20323,#20324);
#17499=AXIS2_PLACEMENT_3D('',#40418,#20325,#20326);
#17500=AXIS2_PLACEMENT_3D('',#40424,#20330,#20331);
#17501=AXIS2_PLACEMENT_3D('',#40426,#20333,#20334);
#17502=AXIS2_PLACEMENT_3D('',#40428,#20336,#20337);
#17503=AXIS2_PLACEMENT_3D('',#40429,#20338,#20339);
#17504=AXIS2_PLACEMENT_3D('',#40435,#20343,#20344);
#17505=AXIS2_PLACEMENT_3D('',#40437,#20346,#20347);
#17506=AXIS2_PLACEMENT_3D('',#40439,#20349,#20350);
#17507=AXIS2_PLACEMENT_3D('',#40440,#20351,#20352);
#17508=AXIS2_PLACEMENT_3D('',#40446,#20356,#20357);
#17509=AXIS2_PLACEMENT_3D('',#40448,#20359,#20360);
#17510=AXIS2_PLACEMENT_3D('',#40450,#20362,#20363);
#17511=AXIS2_PLACEMENT_3D('',#40451,#20364,#20365);
#17512=AXIS2_PLACEMENT_3D('',#40457,#20369,#20370);
#17513=AXIS2_PLACEMENT_3D('',#40459,#20372,#20373);
#17514=AXIS2_PLACEMENT_3D('',#40461,#20375,#20376);
#17515=AXIS2_PLACEMENT_3D('',#40462,#20377,#20378);
#17516=AXIS2_PLACEMENT_3D('',#40466,#20381,#20382);
#17517=AXIS2_PLACEMENT_3D('',#40468,#20384,#20385);
#17518=AXIS2_PLACEMENT_3D('',#40469,#20386,#20387);
#17519=AXIS2_PLACEMENT_3D('',#40475,#20391,#20392);
#17520=AXIS2_PLACEMENT_3D('',#40477,#20394,#20395);
#17521=AXIS2_PLACEMENT_3D('',#40479,#20397,#20398);
#17522=AXIS2_PLACEMENT_3D('',#40480,#20399,#20400);
#17523=AXIS2_PLACEMENT_3D('',#40486,#20404,#20405);
#17524=AXIS2_PLACEMENT_3D('',#40488,#20407,#20408);
#17525=AXIS2_PLACEMENT_3D('',#40490,#20410,#20411);
#17526=AXIS2_PLACEMENT_3D('',#40491,#20412,#20413);
#17527=AXIS2_PLACEMENT_3D('',#40497,#20417,#20418);
#17528=AXIS2_PLACEMENT_3D('',#40499,#20420,#20421);
#17529=AXIS2_PLACEMENT_3D('',#40501,#20423,#20424);
#17530=AXIS2_PLACEMENT_3D('',#40502,#20425,#20426);
#17531=AXIS2_PLACEMENT_3D('',#40508,#20430,#20431);
#17532=AXIS2_PLACEMENT_3D('',#40510,#20433,#20434);
#17533=AXIS2_PLACEMENT_3D('',#40512,#20436,#20437);
#17534=AXIS2_PLACEMENT_3D('',#40513,#20438,#20439);
#17535=AXIS2_PLACEMENT_3D('',#40519,#20443,#20444);
#17536=AXIS2_PLACEMENT_3D('',#40521,#20446,#20447);
#17537=AXIS2_PLACEMENT_3D('',#40523,#20449,#20450);
#17538=AXIS2_PLACEMENT_3D('',#40524,#20451,#20452);
#17539=AXIS2_PLACEMENT_3D('',#40530,#20456,#20457);
#17540=AXIS2_PLACEMENT_3D('',#40532,#20459,#20460);
#17541=AXIS2_PLACEMENT_3D('',#40534,#20462,#20463);
#17542=AXIS2_PLACEMENT_3D('',#40535,#20464,#20465);
#17543=AXIS2_PLACEMENT_3D('',#40537,#20466,#20467);
#17544=AXIS2_PLACEMENT_3D('',#40538,#20468,#20469);
#17545=AXIS2_PLACEMENT_3D('',#40540,#20471,#20472);
#17546=AXIS2_PLACEMENT_3D('',#40541,#20473,#20474);
#17547=AXIS2_PLACEMENT_3D('',#40542,#20475,#20476);
#17548=AXIS2_PLACEMENT_3D('',#40544,#20477,#20478);
#17549=AXIS2_PLACEMENT_3D('',#40545,#20479,#20480);
#17550=AXIS2_PLACEMENT_3D('',#40547,#20482,#20483);
#19858=DIRECTION('axis',(0.,0.,1.));
#19859=DIRECTION('refdir',(1.,0.,0.));
#19860=DIRECTION('center_axis',(1.,0.,0.));
#19861=DIRECTION('ref_axis',(0.,1.,0.));
#19862=DIRECTION('',(-1.,0.,0.));
#19863=DIRECTION('center_axis',(1.,0.,0.));
#19864=DIRECTION('ref_axis',(0.,1.,0.));
#19865=DIRECTION('center_axis',(1.,0.,0.));
#19866=DIRECTION('ref_axis',(0.,1.,0.));
#19867=DIRECTION('',(-1.,0.,0.));
#19868=DIRECTION('center_axis',(1.,0.,0.));
#19869=DIRECTION('ref_axis',(0.,1.,0.));
#19870=DIRECTION('',(-1.,0.,0.));
#19871=DIRECTION('center_axis',(1.,0.,0.));
#19872=DIRECTION('ref_axis',(0.,1.,0.));
#19873=DIRECTION('',(-1.,0.,0.));
#19874=DIRECTION('center_axis',(1.,0.,0.));
#19875=DIRECTION('ref_axis',(0.,1.,0.));
#19876=DIRECTION('',(-1.,0.,0.));
#19877=DIRECTION('center_axis',(1.,0.,0.));
#19878=DIRECTION('ref_axis',(0.,1.,0.));
#19879=DIRECTION('',(-1.,0.,0.));
#19880=DIRECTION('center_axis',(1.,0.,0.));
#19881=DIRECTION('ref_axis',(0.,1.,0.));
#19882=DIRECTION('',(-1.,0.,0.));
#19883=DIRECTION('center_axis',(1.,0.,0.));
#19884=DIRECTION('ref_axis',(0.,1.,0.));
#19885=DIRECTION('',(-1.,0.,0.));
#19886=DIRECTION('center_axis',(1.,0.,0.));
#19887=DIRECTION('ref_axis',(0.,1.,0.));
#19888=DIRECTION('',(-1.,0.,0.));
#19889=DIRECTION('center_axis',(1.,0.,0.));
#19890=DIRECTION('ref_axis',(0.,1.,0.));
#19891=DIRECTION('',(-1.,0.,0.));
#19892=DIRECTION('center_axis',(1.,0.,0.));
#19893=DIRECTION('ref_axis',(0.,1.,0.));
#19894=DIRECTION('',(-1.,0.,0.));
#19895=DIRECTION('center_axis',(1.,0.,0.));
#19896=DIRECTION('ref_axis',(0.,1.,0.));
#19897=DIRECTION('',(-1.,0.,0.));
#19898=DIRECTION('center_axis',(1.,0.,0.));
#19899=DIRECTION('ref_axis',(0.,1.,0.));
#19900=DIRECTION('',(-1.,0.,0.));
#19901=DIRECTION('center_axis',(1.,0.,0.));
#19902=DIRECTION('ref_axis',(0.,1.,7.05550968452284E-14));
#19903=DIRECTION('',(1.,0.,0.));
#19904=DIRECTION('center_axis',(1.,0.,0.));
#19905=DIRECTION('ref_axis',(0.,1.,7.05550968452284E-14));
#19906=DIRECTION('center_axis',(1.,0.,0.));
#19907=DIRECTION('ref_axis',(0.,1.,7.05550968452284E-14));
#19908=DIRECTION('',(1.,0.,0.));
#19909=DIRECTION('center_axis',(1.,0.,0.));
#19910=DIRECTION('ref_axis',(0.,1.,7.05550968452284E-14));
#19911=DIRECTION('center_axis',(1.,0.,0.));
#19912=DIRECTION('ref_axis',(0.,1.,7.05550968452284E-14));
#19913=DIRECTION('',(1.,0.,0.));
#19914=DIRECTION('center_axis',(1.,0.,0.));
#19915=DIRECTION('ref_axis',(0.,1.,7.05550968452284E-14));
#19916=DIRECTION('',(1.,0.,0.));
#19917=DIRECTION('center_axis',(1.,0.,0.));
#19918=DIRECTION('ref_axis',(0.,1.,7.05550968452284E-14));
#19919=DIRECTION('',(1.,0.,0.));
#19920=DIRECTION('center_axis',(1.,0.,0.));
#19921=DIRECTION('ref_axis',(0.,1.,7.05550968452284E-14));
#19922=DIRECTION('',(1.,0.,0.));
#19923=DIRECTION('center_axis',(1.,0.,0.));
#19924=DIRECTION('ref_axis',(0.,1.,7.05550968452284E-14));
#19925=DIRECTION('',(1.,0.,0.));
#19926=DIRECTION('center_axis',(1.,0.,0.));
#19927=DIRECTION('ref_axis',(0.,1.,7.05550968452284E-14));
#19928=DIRECTION('',(1.,0.,0.));
#19929=DIRECTION('center_axis',(1.,0.,0.));
#19930=DIRECTION('ref_axis',(0.,1.,7.05550968452284E-14));
#19931=DIRECTION('',(1.,0.,0.));
#19932=DIRECTION('center_axis',(1.,0.,0.));
#19933=DIRECTION('ref_axis',(0.,1.,7.05550968452284E-14));
#19934=DIRECTION('',(1.,0.,0.));
#19935=DIRECTION('center_axis',(1.,0.,0.));
#19936=DIRECTION('ref_axis',(0.,1.,7.05550968452284E-14));
#19937=DIRECTION('',(1.,0.,0.));
#19938=DIRECTION('center_axis',(1.,0.,0.));
#19939=DIRECTION('ref_axis',(0.,1.,7.05550968452284E-14));
#19940=DIRECTION('',(1.,0.,0.));
#19941=DIRECTION('center_axis',(1.,0.,0.));
#19942=DIRECTION('ref_axis',(0.,1.,7.05550968452284E-14));
#19943=DIRECTION('',(1.,0.,0.));
#19944=DIRECTION('center_axis',(0.707106781186543,-0.707106781186553,0.));
#19945=DIRECTION('ref_axis',(0.,0.,-1.));
#19946=DIRECTION('',(0.,0.,1.));
#19947=DIRECTION('center_axis',(0.707106781186543,-0.707106781186553,0.));
#19948=DIRECTION('ref_axis',(0.707106781186553,0.707106781186543,0.));
#19949=DIRECTION('',(0.,0.,-1.));
#19950=DIRECTION('center_axis',(0.707106781186543,-0.707106781186553,0.));
#19951=DIRECTION('ref_axis',(0.707106781186553,0.707106781186543,0.));
#19952=DIRECTION('center_axis',(1.,0.,0.));
#19953=DIRECTION('ref_axis',(0.,0.,-1.));
#19954=DIRECTION('center_axis',(1.,0.,0.));
#19955=DIRECTION('ref_axis',(0.,0.,-1.));
#19956=DIRECTION('center_axis',(0.707106781186543,0.707106781186553,0.));
#19957=DIRECTION('ref_axis',(0.,0.,-1.));
#19958=DIRECTION('',(0.,0.,-1.));
#19959=DIRECTION('center_axis',(0.707106781186543,0.707106781186553,0.));
#19960=DIRECTION('ref_axis',(-0.707106781186553,0.707106781186543,0.));
#19961=DIRECTION('',(0.,0.,1.));
#19962=DIRECTION('center_axis',(0.707106781186543,0.707106781186553,0.));
#19963=DIRECTION('ref_axis',(-0.707106781186553,0.707106781186543,0.));
#19964=DIRECTION('center_axis',(1.,0.,0.));
#19965=DIRECTION('ref_axis',(0.,1.,0.));
#19966=DIRECTION('center_axis',(1.,0.,0.));
#19967=DIRECTION('ref_axis',(0.,0.,-1.));
#19968=DIRECTION('',(-1.,0.,0.));
#19969=DIRECTION('center_axis',(-1.,0.,0.));
#19970=DIRECTION('ref_axis',(0.,1.,0.));
#19971=DIRECTION('',(-1.,0.,0.));
#19972=DIRECTION('center_axis',(-1.,0.,0.));
#19973=DIRECTION('ref_axis',(0.,1.,0.));
#19974=DIRECTION('',(1.,0.,0.));
#19975=DIRECTION('center_axis',(-1.,0.,0.));
#19976=DIRECTION('ref_axis',(0.,1.,0.));
#19977=DIRECTION('',(1.,0.,0.));
#19978=DIRECTION('center_axis',(1.,0.,0.));
#19979=DIRECTION('ref_axis',(0.,0.,-1.));
#19980=DIRECTION('',(-1.,0.,0.));
#19981=DIRECTION('center_axis',(1.,0.,0.));
#19982=DIRECTION('ref_axis',(0.,1.,0.));
#19983=DIRECTION('',(-1.,0.,0.));
#19984=DIRECTION('center_axis',(-1.,0.,0.));
#19985=DIRECTION('ref_axis',(0.,1.,0.));
#19986=DIRECTION('',(-1.,0.,0.));
#19987=DIRECTION('center_axis',(1.,0.,0.));
#19988=DIRECTION('ref_axis',(0.,0.,-1.));
#19989=DIRECTION('center_axis',(-1.,0.,0.));
#19990=DIRECTION('ref_axis',(0.,1.,0.));
#19991=DIRECTION('',(1.,0.,0.));
#19992=DIRECTION('center_axis',(1.,0.,0.));
#19993=DIRECTION('ref_axis',(0.,1.,0.));
#19994=DIRECTION('center_axis',(1.,0.,0.));
#19995=DIRECTION('ref_axis',(0.,0.,-1.));
#19996=DIRECTION('',(-1.,0.,0.));
#19997=DIRECTION('center_axis',(-1.,0.,0.));
#19998=DIRECTION('ref_axis',(0.,1.,0.));
#19999=DIRECTION('',(-1.,0.,0.));
#20000=DIRECTION('center_axis',(-1.,0.,0.));
#20001=DIRECTION('ref_axis',(0.,1.,0.));
#20002=DIRECTION('',(1.,0.,0.));
#20003=DIRECTION('center_axis',(-1.,0.,0.));
#20004=DIRECTION('ref_axis',(0.,1.,0.));
#20005=DIRECTION('',(1.,0.,0.));
#20006=DIRECTION('',(1.,0.,0.));
#20007=DIRECTION('center_axis',(1.,0.,0.));
#20008=DIRECTION('ref_axis',(0.,1.,0.));
#20009=DIRECTION('',(-1.,0.,0.));
#20010=DIRECTION('center_axis',(-1.,0.,0.));
#20011=DIRECTION('ref_axis',(0.,1.,0.));
#20012=DIRECTION('',(1.,0.,0.));
#20013=DIRECTION('center_axis',(1.,0.,0.));
#20014=DIRECTION('ref_axis',(0.,1.,0.));
#20015=DIRECTION('',(-1.,0.,0.));
#20016=DIRECTION('center_axis',(-1.,0.,0.));
#20017=DIRECTION('ref_axis',(0.,1.,0.));
#20018=DIRECTION('',(1.,0.,0.));
#20019=DIRECTION('center_axis',(1.,0.,0.));
#20020=DIRECTION('ref_axis',(0.,1.,0.));
#20021=DIRECTION('',(-1.,0.,0.));
#20022=DIRECTION('center_axis',(-1.,0.,0.));
#20023=DIRECTION('ref_axis',(0.,1.,0.));
#20024=DIRECTION('',(1.,0.,0.));
#20025=DIRECTION('center_axis',(1.,0.,0.));
#20026=DIRECTION('ref_axis',(0.,1.,0.));
#20027=DIRECTION('',(-1.,0.,0.));
#20028=DIRECTION('center_axis',(-1.,0.,0.));
#20029=DIRECTION('ref_axis',(0.,1.,0.));
#20030=DIRECTION('',(1.,0.,0.));
#20031=DIRECTION('center_axis',(1.,0.,0.));
#20032=DIRECTION('ref_axis',(0.,1.,0.));
#20033=DIRECTION('',(-1.,0.,0.));
#20034=DIRECTION('center_axis',(-1.,0.,0.));
#20035=DIRECTION('ref_axis',(0.,1.,0.));
#20036=DIRECTION('',(1.,0.,0.));
#20037=DIRECTION('center_axis',(1.,0.,0.));
#20038=DIRECTION('ref_axis',(0.,1.,0.));
#20039=DIRECTION('',(-1.,0.,0.));
#20040=DIRECTION('center_axis',(-1.,0.,0.));
#20041=DIRECTION('ref_axis',(0.,1.,0.));
#20042=DIRECTION('',(1.,0.,0.));
#20043=DIRECTION('center_axis',(1.,0.,0.));
#20044=DIRECTION('ref_axis',(0.,1.,0.));
#20045=DIRECTION('',(-1.,0.,0.));
#20046=DIRECTION('center_axis',(-1.,0.,0.));
#20047=DIRECTION('ref_axis',(0.,1.,0.));
#20048=DIRECTION('',(1.,0.,0.));
#20049=DIRECTION('center_axis',(1.,0.,0.));
#20050=DIRECTION('ref_axis',(0.,1.,0.));
#20051=DIRECTION('',(-1.,0.,0.));
#20052=DIRECTION('center_axis',(-1.,0.,0.));
#20053=DIRECTION('ref_axis',(0.,1.,0.));
#20054=DIRECTION('',(1.,0.,0.));
#20055=DIRECTION('center_axis',(1.,0.,0.));
#20056=DIRECTION('ref_axis',(0.,1.,0.));
#20057=DIRECTION('',(-1.,0.,0.));
#20058=DIRECTION('center_axis',(-1.,0.,0.));
#20059=DIRECTION('ref_axis',(0.,1.,0.));
#20060=DIRECTION('',(1.,0.,0.));
#20061=DIRECTION('center_axis',(1.,0.,0.));
#20062=DIRECTION('ref_axis',(0.,1.,0.));
#20063=DIRECTION('',(-1.,0.,0.));
#20064=DIRECTION('center_axis',(-1.,0.,0.));
#20065=DIRECTION('ref_axis',(0.,1.,0.));
#20066=DIRECTION('',(1.,0.,0.));
#20067=DIRECTION('center_axis',(1.,0.,0.));
#20068=DIRECTION('ref_axis',(0.,1.,0.));
#20069=DIRECTION('',(-1.,0.,0.));
#20070=DIRECTION('center_axis',(-1.,0.,0.));
#20071=DIRECTION('ref_axis',(0.,1.,0.));
#20072=DIRECTION('',(1.,0.,0.));
#20073=DIRECTION('center_axis',(1.,0.,0.));
#20074=DIRECTION('ref_axis',(0.,1.,0.));
#20075=DIRECTION('',(-1.,0.,0.));
#20076=DIRECTION('center_axis',(-1.,0.,0.));
#20077=DIRECTION('ref_axis',(0.,1.,0.));
#20078=DIRECTION('',(1.,0.,0.));
#20079=DIRECTION('center_axis',(1.,0.,0.));
#20080=DIRECTION('ref_axis',(0.,1.,0.));
#20081=DIRECTION('',(-1.,0.,0.));
#20082=DIRECTION('center_axis',(-1.,0.,0.));
#20083=DIRECTION('ref_axis',(0.,1.,0.));
#20084=DIRECTION('',(1.,0.,0.));
#20085=DIRECTION('center_axis',(1.,0.,0.));
#20086=DIRECTION('ref_axis',(0.,1.,0.));
#20087=DIRECTION('',(-1.,0.,0.));
#20088=DIRECTION('center_axis',(-1.,0.,0.));
#20089=DIRECTION('ref_axis',(0.,1.,0.));
#20090=DIRECTION('',(1.,0.,0.));
#20091=DIRECTION('center_axis',(1.,0.,0.));
#20092=DIRECTION('ref_axis',(0.,1.,0.));
#20093=DIRECTION('',(-1.,0.,0.));
#20094=DIRECTION('center_axis',(-1.,0.,0.));
#20095=DIRECTION('ref_axis',(0.,1.,0.));
#20096=DIRECTION('',(1.,0.,0.));
#20097=DIRECTION('center_axis',(1.,0.,0.));
#20098=DIRECTION('ref_axis',(0.,1.,0.));
#20099=DIRECTION('',(-1.,0.,0.));
#20100=DIRECTION('center_axis',(-1.,0.,0.));
#20101=DIRECTION('ref_axis',(0.,1.,0.));
#20102=DIRECTION('',(1.,0.,0.));
#20103=DIRECTION('center_axis',(1.,0.,0.));
#20104=DIRECTION('ref_axis',(0.,1.,0.));
#20105=DIRECTION('',(-1.,0.,0.));
#20106=DIRECTION('center_axis',(-1.,0.,0.));
#20107=DIRECTION('ref_axis',(0.,1.,0.));
#20108=DIRECTION('',(1.,0.,0.));
#20109=DIRECTION('center_axis',(1.,0.,0.));
#20110=DIRECTION('ref_axis',(0.,1.,0.));
#20111=DIRECTION('',(-1.,0.,0.));
#20112=DIRECTION('center_axis',(-1.,0.,0.));
#20113=DIRECTION('ref_axis',(0.,1.,0.));
#20114=DIRECTION('',(1.,0.,0.));
#20115=DIRECTION('center_axis',(1.,0.,0.));
#20116=DIRECTION('ref_axis',(0.,1.,0.));
#20117=DIRECTION('',(-1.,0.,0.));
#20118=DIRECTION('center_axis',(-1.,0.,0.));
#20119=DIRECTION('ref_axis',(0.,1.,0.));
#20120=DIRECTION('',(1.,0.,0.));
#20121=DIRECTION('center_axis',(1.,0.,0.));
#20122=DIRECTION('ref_axis',(0.,1.,0.));
#20123=DIRECTION('',(-1.,0.,0.));
#20124=DIRECTION('center_axis',(-1.,0.,0.));
#20125=DIRECTION('ref_axis',(0.,1.,0.));
#20126=DIRECTION('',(1.,0.,0.));
#20127=DIRECTION('center_axis',(1.,0.,0.));
#20128=DIRECTION('ref_axis',(0.,1.,0.));
#20129=DIRECTION('',(-1.,0.,0.));
#20130=DIRECTION('center_axis',(-1.,0.,0.));
#20131=DIRECTION('ref_axis',(0.,1.,0.));
#20132=DIRECTION('center_axis',(-1.,0.,0.));
#20133=DIRECTION('ref_axis',(0.,-1.,-1.22464679914735E-16));
#20134=DIRECTION('center_axis',(1.,0.,0.));
#20135=DIRECTION('ref_axis',(0.,0.,-1.));
#20136=DIRECTION('center_axis',(1.,0.,0.));
#20137=DIRECTION('ref_axis',(0.,0.,-1.));
#20138=DIRECTION('center_axis',(1.,0.,0.));
#20139=DIRECTION('ref_axis',(0.,0.,-1.));
#20140=DIRECTION('center_axis',(1.,0.,0.));
#20141=DIRECTION('ref_axis',(0.,1.,0.));
#20142=DIRECTION('center_axis',(1.,0.,0.));
#20143=DIRECTION('ref_axis',(0.,1.,0.));
#20144=DIRECTION('center_axis',(-1.,0.,0.));
#20145=DIRECTION('ref_axis',(0.,1.,7.05550968452284E-14));
#20146=DIRECTION('center_axis',(1.,0.,0.));
#20147=DIRECTION('ref_axis',(0.,0.888987169455759,0.457932104730644));
#20148=DIRECTION('center_axis',(0.,-1.,0.));
#20149=DIRECTION('ref_axis',(0.,0.,1.));
#20150=DIRECTION('',(0.,0.,1.));
#20151=DIRECTION('center_axis',(-1.,0.,0.));
#20152=DIRECTION('ref_axis',(0.,0.,1.));
#20153=DIRECTION('',(0.,0.,-1.));
#20154=DIRECTION('',(0.,0.707106781186547,0.707106781186548));
#20155=DIRECTION('',(0.,0.707106781186547,-0.707106781186548));
#20156=DIRECTION('',(0.,-0.707106781186547,-0.707106781186548));
#20157=DIRECTION('',(0.,-0.707106781186547,0.707106781186548));
#20158=DIRECTION('center_axis',(0.,1.,0.));
#20159=DIRECTION('ref_axis',(0.,0.,-1.));
#20160=DIRECTION('center_axis',(0.,-0.707106781186548,0.707106781186547));
#20161=DIRECTION('ref_axis',(0.,-0.707106781186547,-0.707106781186548));
#20162=DIRECTION('',(0.,-0.707106781186547,-0.707106781186548));
#20163=DIRECTION('',(1.,0.,0.));
#20164=DIRECTION('center_axis',(0.,-0.499999999999999,0.866025403784439));
#20165=DIRECTION('ref_axis',(0.,-0.866025403784439,-0.499999999999999));
#20166=DIRECTION('',(0.,-0.866025403784439,-0.499999999999999));
#20167=DIRECTION('',(1.,0.,0.));
#20168=DIRECTION('',(0.,-0.866025403784439,-0.499999999999999));
#20169=DIRECTION('center_axis',(1.,0.,0.));
#20170=DIRECTION('ref_axis',(0.,-0.258819045102522,-0.965925826289068));
#20171=DIRECTION('',(0.,0.5,-0.866025403784439));
#20172=DIRECTION('center_axis',(0.,-0.866025403784439,-0.5));
#20173=DIRECTION('ref_axis',(0.,0.5,-0.866025403784439));
#20174=DIRECTION('',(0.,0.5,-0.866025403784439));
#20175=DIRECTION('center_axis',(1.,0.,0.));
#20176=DIRECTION('ref_axis',(0.,-0.258819045102522,-0.965925826289068));
#20177=DIRECTION('center_axis',(0.,-0.25881904510252,0.965925826289069));
#20178=DIRECTION('ref_axis',(0.,-0.965925826289069,-0.25881904510252));
#20179=DIRECTION('',(0.,-0.965925826289069,-0.25881904510252));
#20180=DIRECTION('',(1.,0.,0.));
#20181=DIRECTION('',(0.,-0.965925826289069,-0.25881904510252));
#20182=DIRECTION('center_axis',(1.,0.,0.));
#20183=DIRECTION('ref_axis',(0.,-0.5,-0.866025403784438));
#20184=DIRECTION('',(0.,0.258819045102521,-0.965925826289068));
#20185=DIRECTION('center_axis',(0.,-0.965925826289068,-0.258819045102521));
#20186=DIRECTION('ref_axis',(0.,0.258819045102521,-0.965925826289068));
#20187=DIRECTION('',(0.,0.258819045102521,-0.965925826289068));
#20188=DIRECTION('center_axis',(1.,0.,0.));
#20189=DIRECTION('ref_axis',(0.,-0.5,-0.866025403784438));
#20190=DIRECTION('center_axis',(0.,6.66133814775094E-16,1.));
#20191=DIRECTION('ref_axis',(0.,-1.,6.66133814775094E-16));
#20192=DIRECTION('',(0.,-1.,6.66133814775094E-16));
#20193=DIRECTION('',(1.,0.,0.));
#20194=DIRECTION('',(0.,-1.,6.66133814775094E-16));
#20195=DIRECTION('center_axis',(1.,0.,0.));
#20196=DIRECTION('ref_axis',(0.,-0.707106781186548,-0.707106781186547));
#20197=DIRECTION('',(0.,2.22044604925031E-16,-1.));
#20198=DIRECTION('center_axis',(0.,-1.,-2.22044604925031E-16));
#20199=DIRECTION('ref_axis',(0.,2.22044604925031E-16,-1.));
#20200=DIRECTION('',(0.,2.22044604925031E-16,-1.));
#20201=DIRECTION('center_axis',(1.,0.,0.));
#20202=DIRECTION('ref_axis',(0.,-0.707106781186548,-0.707106781186547));
#20203=DIRECTION('center_axis',(0.,0.258819045102522,0.965925826289068));
#20204=DIRECTION('ref_axis',(0.,-0.965925826289068,0.258819045102522));
#20205=DIRECTION('',(0.,-0.965925826289068,0.258819045102522));
#20206=DIRECTION('',(1.,0.,0.));
#20207=DIRECTION('',(0.,-0.965925826289068,0.258819045102522));
#20208=DIRECTION('center_axis',(1.,0.,0.));
#20209=DIRECTION('ref_axis',(0.,-0.866025403784439,-0.499999999999999));
#20210=DIRECTION('',(0.,-0.258819045102521,-0.965925826289068));
#20211=DIRECTION('center_axis',(0.,-0.965925826289068,0.258819045102521));
#20212=DIRECTION('ref_axis',(0.,-0.258819045102521,-0.965925826289068));
#20213=DIRECTION('',(0.,-0.258819045102521,-0.965925826289068));
#20214=DIRECTION('center_axis',(1.,0.,0.));
#20215=DIRECTION('ref_axis',(0.,-0.866025403784439,-0.499999999999999));
#20216=DIRECTION('center_axis',(0.,0.500000000000001,0.866025403784438));
#20217=DIRECTION('ref_axis',(0.,-0.866025403784438,0.500000000000001));
#20218=DIRECTION('',(0.,-0.866025403784438,0.500000000000001));
#20219=DIRECTION('',(1.,0.,0.));
#20220=DIRECTION('',(0.,-0.866025403784438,0.500000000000001));
#20221=DIRECTION('center_axis',(1.,0.,0.));
#20222=DIRECTION('ref_axis',(0.,-0.965925826289068,-0.25881904510252));
#20223=DIRECTION('',(0.,-0.5,-0.866025403784439));
#20224=DIRECTION('center_axis',(0.,-0.866025403784439,0.5));
#20225=DIRECTION('ref_axis',(0.,-0.5,-0.866025403784439));
#20226=DIRECTION('',(0.,-0.5,-0.866025403784439));
#20227=DIRECTION('center_axis',(1.,0.,0.));
#20228=DIRECTION('ref_axis',(0.,-0.965925826289068,-0.25881904510252));
#20229=DIRECTION('center_axis',(0.,0.707106781186548,0.707106781186547));
#20230=DIRECTION('ref_axis',(0.,-0.707106781186547,0.707106781186548));
#20231=DIRECTION('',(0.,-0.707106781186547,0.707106781186548));
#20232=DIRECTION('center_axis',(1.,0.,0.));
#20233=DIRECTION('ref_axis',(0.,-1.,1.83697019872103E-16));
#20234=DIRECTION('center_axis',(0.,0.866025403784439,0.499999999999999));
#20235=DIRECTION('ref_axis',(0.,-0.499999999999999,0.866025403784439));
#20236=DIRECTION('',(0.,-0.499999999999999,0.866025403784439));
#20237=DIRECTION('',(1.,0.,0.));
#20238=DIRECTION('',(0.,-0.499999999999999,0.866025403784439));
#20239=DIRECTION('center_axis',(1.,0.,0.));
#20240=DIRECTION('ref_axis',(0.,-0.965925826289068,0.258819045102522));
#20241=DIRECTION('',(0.,-0.866025403784439,-0.5));
#20242=DIRECTION('center_axis',(0.,-0.5,0.866025403784439));
#20243=DIRECTION('ref_axis',(0.,-0.866025403784439,-0.5));
#20244=DIRECTION('',(0.,-0.866025403784439,-0.5));
#20245=DIRECTION('center_axis',(1.,0.,0.));
#20246=DIRECTION('ref_axis',(0.,-0.965925826289068,0.258819045102522));
#20247=DIRECTION('center_axis',(0.,0.965925826289069,0.25881904510252));
#20248=DIRECTION('ref_axis',(0.,-0.25881904510252,0.965925826289069));
#20249=DIRECTION('',(0.,-0.25881904510252,0.965925826289069));
#20250=DIRECTION('',(1.,0.,0.));
#20251=DIRECTION('',(0.,-0.25881904510252,0.965925826289069));
#20252=DIRECTION('center_axis',(1.,0.,0.));
#20253=DIRECTION('ref_axis',(0.,-0.866025403784438,0.5));
#20254=DIRECTION('',(0.,-0.965925826289068,-0.258819045102521));
#20255=DIRECTION('center_axis',(0.,-0.258819045102521,0.965925826289068));
#20256=DIRECTION('ref_axis',(0.,-0.965925826289068,-0.258819045102521));
#20257=DIRECTION('',(0.,-0.965925826289068,-0.258819045102521));
#20258=DIRECTION('center_axis',(1.,0.,0.));
#20259=DIRECTION('ref_axis',(0.,-0.866025403784438,0.5));
#20260=DIRECTION('center_axis',(0.,1.,-1.0547118733939E-15));
#20261=DIRECTION('ref_axis',(0.,1.0547118733939E-15,1.));
#20262=DIRECTION('',(0.,1.0547118733939E-15,1.));
#20263=DIRECTION('',(1.,0.,0.));
#20264=DIRECTION('',(0.,1.0547118733939E-15,1.));
#20265=DIRECTION('center_axis',(1.,0.,0.));
#20266=DIRECTION('ref_axis',(0.,-0.707106781186547,0.707106781186548));
#20267=DIRECTION('',(0.,-1.,1.11022302462516E-16));
#20268=DIRECTION('center_axis',(0.,1.11022302462516E-16,1.));
#20269=DIRECTION('ref_axis',(0.,-1.,1.11022302462516E-16));
#20270=DIRECTION('',(0.,-1.,1.11022302462516E-16));
#20271=DIRECTION('center_axis',(1.,0.,0.));
#20272=DIRECTION('ref_axis',(0.,-0.707106781186547,0.707106781186548));
#20273=DIRECTION('center_axis',(0.,0.965925826289068,-0.258819045102522));
#20274=DIRECTION('ref_axis',(0.,0.258819045102522,0.965925826289068));
#20275=DIRECTION('',(0.,0.258819045102522,0.965925826289068));
#20276=DIRECTION('',(1.,0.,0.));
#20277=DIRECTION('',(0.,0.258819045102522,0.965925826289068));
#20278=DIRECTION('center_axis',(1.,0.,0.));
#20279=DIRECTION('ref_axis',(0.,-0.5,0.866025403784439));
#20280=DIRECTION('',(0.,-0.965925826289068,0.258819045102521));
#20281=DIRECTION('center_axis',(0.,0.258819045102521,0.965925826289068));
#20282=DIRECTION('ref_axis',(0.,-0.965925826289068,0.258819045102521));
#20283=DIRECTION('',(0.,-0.965925826289068,0.258819045102521));
#20284=DIRECTION('center_axis',(1.,0.,0.));
#20285=DIRECTION('ref_axis',(0.,-0.5,0.866025403784439));
#20286=DIRECTION('center_axis',(0.,0.866025403784438,-0.500000000000001));
#20287=DIRECTION('ref_axis',(0.,0.500000000000001,0.866025403784438));
#20288=DIRECTION('',(0.,0.500000000000001,0.866025403784438));
#20289=DIRECTION('',(1.,0.,0.));
#20290=DIRECTION('',(0.,0.500000000000001,0.866025403784438));
#20291=DIRECTION('center_axis',(1.,0.,0.));
#20292=DIRECTION('ref_axis',(0.,-0.25881904510252,0.965925826289068));
#20293=DIRECTION('',(0.,-0.866025403784439,0.5));
#20294=DIRECTION('center_axis',(0.,0.5,0.866025403784439));
#20295=DIRECTION('ref_axis',(0.,-0.866025403784439,0.5));
#20296=DIRECTION('',(0.,-0.866025403784439,0.5));
#20297=DIRECTION('center_axis',(1.,0.,0.));
#20298=DIRECTION('ref_axis',(0.,-0.25881904510252,0.965925826289068));
#20299=DIRECTION('center_axis',(0.,0.707106781186547,-0.707106781186548));
#20300=DIRECTION('ref_axis',(0.,0.707106781186548,0.707106781186547));
#20301=DIRECTION('',(0.,0.707106781186548,0.707106781186547));
#20302=DIRECTION('',(1.,0.,0.));
#20303=DIRECTION('',(0.,0.707106781186548,0.707106781186547));
#20304=DIRECTION('center_axis',(1.,0.,0.));
#20305=DIRECTION('ref_axis',(0.,1.22464679914735E-16,1.));
#20306=DIRECTION('',(0.,-0.707106781186548,0.707106781186547));
#20307=DIRECTION('center_axis',(0.,0.707106781186547,0.707106781186548));
#20308=DIRECTION('ref_axis',(0.,-0.707106781186548,0.707106781186547));
#20309=DIRECTION('',(0.,-0.707106781186548,0.707106781186547));
#20310=DIRECTION('center_axis',(1.,0.,0.));
#20311=DIRECTION('ref_axis',(0.,1.22464679914735E-16,1.));
#20312=DIRECTION('center_axis',(0.,0.499999999999999,-0.866025403784439));
#20313=DIRECTION('ref_axis',(0.,0.866025403784439,0.499999999999999));
#20314=DIRECTION('',(0.,0.866025403784439,0.499999999999999));
#20315=DIRECTION('',(1.,0.,0.));
#20316=DIRECTION('',(0.,0.866025403784439,0.499999999999999));
#20317=DIRECTION('center_axis',(1.,0.,0.));
#20318=DIRECTION('ref_axis',(0.,0.258819045102521,0.965925826289068));
#20319=DIRECTION('',(0.,-0.5,0.866025403784439));
#20320=DIRECTION('center_axis',(0.,0.866025403784439,0.5));
#20321=DIRECTION('ref_axis',(0.,-0.5,0.866025403784439));
#20322=DIRECTION('',(0.,-0.5,0.866025403784439));
#20323=DIRECTION('center_axis',(1.,0.,0.));
#20324=DIRECTION('ref_axis',(0.,0.258819045102521,0.965925826289068));
#20325=DIRECTION('center_axis',(0.,0.25881904510252,-0.965925826289069));
#20326=DIRECTION('ref_axis',(0.,0.965925826289068,0.25881904510252));
#20327=DIRECTION('',(0.,0.965925826289068,0.25881904510252));
#20328=DIRECTION('',(1.,0.,0.));
#20329=DIRECTION('',(0.,0.965925826289068,0.25881904510252));
#20330=DIRECTION('center_axis',(1.,0.,0.));
#20331=DIRECTION('ref_axis',(0.,0.5,0.866025403784438));
#20332=DIRECTION('',(0.,-0.258819045102521,0.965925826289068));
#20333=DIRECTION('center_axis',(0.,0.965925826289068,0.258819045102521));
#20334=DIRECTION('ref_axis',(0.,-0.258819045102521,0.965925826289068));
#20335=DIRECTION('',(0.,-0.258819045102521,0.965925826289068));
#20336=DIRECTION('center_axis',(1.,0.,0.));
#20337=DIRECTION('ref_axis',(0.,0.5,0.866025403784438));
#20338=DIRECTION('center_axis',(0.,-5.55111512312578E-16,-1.));
#20339=DIRECTION('ref_axis',(0.,1.,-5.55111512312578E-16));
#20340=DIRECTION('',(0.,1.,-5.55111512312578E-16));
#20341=DIRECTION('',(1.,0.,0.));
#20342=DIRECTION('',(0.,1.,-5.55111512312578E-16));
#20343=DIRECTION('center_axis',(1.,0.,0.));
#20344=DIRECTION('ref_axis',(0.,0.707106781186548,0.707106781186547));
#20345=DIRECTION('',(0.,-3.88578058618805E-16,1.));
#20346=DIRECTION('center_axis',(0.,1.,3.88578058618805E-16));
#20347=DIRECTION('ref_axis',(0.,-3.88578058618805E-16,1.));
#20348=DIRECTION('',(0.,-3.88578058618805E-16,1.));
#20349=DIRECTION('center_axis',(1.,0.,0.));
#20350=DIRECTION('ref_axis',(0.,0.707106781186548,0.707106781186547));
#20351=DIRECTION('center_axis',(0.,-0.258819045102522,-0.965925826289068));
#20352=DIRECTION('ref_axis',(0.,0.965925826289068,-0.258819045102522));
#20353=DIRECTION('',(0.,0.965925826289068,-0.258819045102522));
#20354=DIRECTION('',(1.,0.,0.));
#20355=DIRECTION('',(0.,0.965925826289068,-0.258819045102522));
#20356=DIRECTION('center_axis',(1.,0.,0.));
#20357=DIRECTION('ref_axis',(0.,0.866025403784439,0.5));
#20358=DIRECTION('',(0.,0.25881904510252,0.965925826289068));
#20359=DIRECTION('center_axis',(0.,0.965925826289068,-0.258819045102521));
#20360=DIRECTION('ref_axis',(0.,0.25881904510252,0.965925826289068));
#20361=DIRECTION('',(0.,0.25881904510252,0.965925826289068));
#20362=DIRECTION('center_axis',(1.,0.,0.));
#20363=DIRECTION('ref_axis',(0.,0.866025403784439,0.5));
#20364=DIRECTION('center_axis',(0.,-0.500000000000001,-0.866025403784438));
#20365=DIRECTION('ref_axis',(0.,0.866025403784438,-0.500000000000001));
#20366=DIRECTION('',(0.,0.866025403784438,-0.500000000000001));
#20367=DIRECTION('',(1.,0.,0.));
#20368=DIRECTION('',(0.,0.866025403784438,-0.500000000000001));
#20369=DIRECTION('center_axis',(1.,0.,0.));
#20370=DIRECTION('ref_axis',(0.,0.965925826289068,0.258819045102521));
#20371=DIRECTION('',(0.,0.5,0.866025403784439));
#20372=DIRECTION('center_axis',(0.,0.866025403784439,-0.5));
#20373=DIRECTION('ref_axis',(0.,0.5,0.866025403784439));
#20374=DIRECTION('',(0.,0.5,0.866025403784439));
#20375=DIRECTION('center_axis',(1.,0.,0.));
#20376=DIRECTION('ref_axis',(0.,0.965925826289068,0.258819045102521));
#20377=DIRECTION('center_axis',(0.,-0.707106781186548,-0.707106781186547));
#20378=DIRECTION('ref_axis',(0.,0.707106781186547,-0.707106781186548));
#20379=DIRECTION('',(1.,0.,0.));
#20380=DIRECTION('',(0.,0.707106781186547,-0.707106781186548));
#20381=DIRECTION('center_axis',(1.,0.,0.));
#20382=DIRECTION('ref_axis',(0.,1.,-6.12323399573677E-17));
#20383=DIRECTION('',(0.,0.707106781186547,0.707106781186548));
#20384=DIRECTION('center_axis',(0.,0.707106781186548,-0.707106781186547));
#20385=DIRECTION('ref_axis',(0.,0.707106781186547,0.707106781186548));
#20386=DIRECTION('center_axis',(0.,-0.866025403784439,-0.499999999999999));
#20387=DIRECTION('ref_axis',(0.,0.499999999999999,-0.866025403784439));
#20388=DIRECTION('',(0.,0.499999999999999,-0.866025403784439));
#20389=DIRECTION('',(1.,0.,0.));
#20390=DIRECTION('',(0.,0.499999999999999,-0.866025403784439));
#20391=DIRECTION('center_axis',(1.,0.,0.));
#20392=DIRECTION('ref_axis',(0.,0.965925826289068,-0.258819045102521));
#20393=DIRECTION('',(0.,0.866025403784439,0.5));
#20394=DIRECTION('center_axis',(0.,0.5,-0.866025403784439));
#20395=DIRECTION('ref_axis',(0.,0.866025403784439,0.5));
#20396=DIRECTION('',(0.,0.866025403784439,0.5));
#20397=DIRECTION('center_axis',(1.,0.,0.));
#20398=DIRECTION('ref_axis',(0.,0.965925826289068,-0.258819045102521));
#20399=DIRECTION('center_axis',(0.,-0.965925826289068,-0.25881904510252));
#20400=DIRECTION('ref_axis',(0.,0.25881904510252,-0.965925826289068));
#20401=DIRECTION('',(0.,0.25881904510252,-0.965925826289068));
#20402=DIRECTION('',(1.,0.,0.));
#20403=DIRECTION('',(0.,0.25881904510252,-0.965925826289068));
#20404=DIRECTION('center_axis',(1.,0.,0.));
#20405=DIRECTION('ref_axis',(0.,0.866025403784439,-0.5));
#20406=DIRECTION('',(0.,0.965925826289068,0.258819045102521));
#20407=DIRECTION('center_axis',(0.,0.258819045102521,-0.965925826289068));
#20408=DIRECTION('ref_axis',(0.,0.965925826289068,0.258819045102521));
#20409=DIRECTION('',(0.,0.965925826289068,0.258819045102521));
#20410=DIRECTION('center_axis',(1.,0.,0.));
#20411=DIRECTION('ref_axis',(0.,0.866025403784439,-0.5));
#20412=DIRECTION('center_axis',(0.,-1.,4.9960036108132E-16));
#20413=DIRECTION('ref_axis',(0.,-4.9960036108132E-16,-1.));
#20414=DIRECTION('',(0.,-4.9960036108132E-16,-1.));
#20415=DIRECTION('',(1.,0.,0.));
#20416=DIRECTION('',(0.,-4.9960036108132E-16,-1.));
#20417=DIRECTION('center_axis',(1.,0.,0.));
#20418=DIRECTION('ref_axis',(0.,0.707106781186548,-0.707106781186548));
#20419=DIRECTION('',(0.,1.,4.9960036108132E-16));
#20420=DIRECTION('center_axis',(0.,4.9960036108132E-16,-1.));
#20421=DIRECTION('ref_axis',(0.,1.,4.9960036108132E-16));
#20422=DIRECTION('',(0.,1.,4.9960036108132E-16));
#20423=DIRECTION('center_axis',(1.,0.,0.));
#20424=DIRECTION('ref_axis',(0.,0.707106781186548,-0.707106781186548));
#20425=DIRECTION('center_axis',(0.,-0.965925826289068,0.258819045102521));
#20426=DIRECTION('ref_axis',(0.,-0.258819045102521,-0.965925826289068));
#20427=DIRECTION('',(0.,-0.258819045102521,-0.965925826289068));
#20428=DIRECTION('',(1.,0.,0.));
#20429=DIRECTION('',(0.,-0.258819045102521,-0.965925826289068));
#20430=DIRECTION('center_axis',(1.,0.,0.));
#20431=DIRECTION('ref_axis',(0.,0.5,-0.866025403784439));
#20432=DIRECTION('',(0.,0.965925826289068,-0.25881904510252));
#20433=DIRECTION('center_axis',(0.,-0.25881904510252,-0.965925826289068));
#20434=DIRECTION('ref_axis',(0.,0.965925826289068,-0.25881904510252));
#20435=DIRECTION('',(0.,0.965925826289068,-0.25881904510252));
#20436=DIRECTION('center_axis',(1.,0.,0.));
#20437=DIRECTION('ref_axis',(0.,0.5,-0.866025403784439));
#20438=DIRECTION('center_axis',(0.,-0.866025403784438,0.5));
#20439=DIRECTION('ref_axis',(0.,-0.5,-0.866025403784438));
#20440=DIRECTION('',(0.,-0.5,-0.866025403784438));
#20441=DIRECTION('',(1.,0.,0.));
#20442=DIRECTION('',(0.,-0.5,-0.866025403784438));
#20443=DIRECTION('center_axis',(1.,0.,0.));
#20444=DIRECTION('ref_axis',(0.,0.258819045102521,-0.965925826289068));
#20445=DIRECTION('',(0.,0.866025403784439,-0.5));
#20446=DIRECTION('center_axis',(0.,-0.5,-0.866025403784439));
#20447=DIRECTION('ref_axis',(0.,0.866025403784439,-0.5));
#20448=DIRECTION('',(0.,0.866025403784439,-0.5));
#20449=DIRECTION('center_axis',(1.,0.,0.));
#20450=DIRECTION('ref_axis',(0.,0.258819045102521,-0.965925826289068));
#20451=DIRECTION('center_axis',(0.,-0.707106781186547,0.707106781186548));
#20452=DIRECTION('ref_axis',(0.,-0.707106781186548,-0.707106781186547));
#20453=DIRECTION('',(0.,-0.707106781186548,-0.707106781186547));
#20454=DIRECTION('',(1.,0.,0.));
#20455=DIRECTION('',(0.,-0.707106781186548,-0.707106781186547));
#20456=DIRECTION('center_axis',(1.,0.,0.));
#20457=DIRECTION('ref_axis',(0.,0.,-1.));
#20458=DIRECTION('',(0.,0.707106781186548,-0.707106781186547));
#20459=DIRECTION('center_axis',(0.,-0.707106781186547,-0.707106781186548));
#20460=DIRECTION('ref_axis',(0.,0.707106781186548,-0.707106781186547));
#20461=DIRECTION('',(0.,0.707106781186548,-0.707106781186547));
#20462=DIRECTION('center_axis',(1.,0.,0.));
#20463=DIRECTION('ref_axis',(0.,0.,-1.));
#20464=DIRECTION('center_axis',(-1.,0.,0.));
#20465=DIRECTION('ref_axis',(0.,0.,1.));
#20466=DIRECTION('center_axis',(1.,0.,0.));
#20467=DIRECTION('ref_axis',(0.,0.,-1.));
#20468=DIRECTION('center_axis',(1.,0.,0.));
#20469=DIRECTION('ref_axis',(0.,1.,0.));
#20470=DIRECTION('',(-0.707106781186571,0.707106781186524,8.65956056235465E-17));
#20471=DIRECTION('center_axis',(1.,0.,0.));
#20472=DIRECTION('ref_axis',(0.,1.,0.));
#20473=DIRECTION('center_axis',(1.,0.,0.));
#20474=DIRECTION('ref_axis',(0.,1.,0.));
#20475=DIRECTION('center_axis',(-1.,0.,0.));
#20476=DIRECTION('ref_axis',(0.,0.,1.));
#20477=DIRECTION('center_axis',(1.,0.,0.));
#20478=DIRECTION('ref_axis',(0.,0.,-1.));
#20479=DIRECTION('center_axis',(1.,0.,0.));
#20480=DIRECTION('ref_axis',(0.,1.,0.));
#20481=DIRECTION('',(-0.707106781186571,0.707106781186524,8.65956056235465E-17));
#20482=DIRECTION('center_axis',(-1.,0.,0.));
#20483=DIRECTION('ref_axis',(0.,1.,0.));
#36658=CARTESIAN_POINT('',(0.,0.,0.));
#36659=CARTESIAN_POINT('Origin',(215.7,0.,0.));
#36660=CARTESIAN_POINT('',(209.664320454657,-4.9420180477033,0.000126580456323855));
#36661=CARTESIAN_POINT('',(209.519679545343,-4.94198289688221,9.21666299965981E-5));
#36662=CARTESIAN_POINT('',(215.7,-4.942,-6.05220448138622E-16));
#36663=CARTESIAN_POINT('',(209.342,2.16926434203831,4.44056974845354));
#36664=CARTESIAN_POINT('Ctrl Pts',(209.664320454657,-4.9420180477033,0.000126580456323855));
#36665=CARTESIAN_POINT('Ctrl Pts',(209.658355941445,-4.9422072805368,0.185328915025629));
#36666=CARTESIAN_POINT('Ctrl Pts',(209.652391428234,-4.93199568223875,0.370510473892667));
#36667=CARTESIAN_POINT('Ctrl Pts',(209.646426915022,-4.91122249414261,0.554499541264965));
#36668=CARTESIAN_POINT('Ctrl Pts',(209.620030391337,-4.81928876339832,1.36876075631831));
#36669=CARTESIAN_POINT('Ctrl Pts',(209.593633867651,-4.52049682480743,2.15966595601887));
#36670=CARTESIAN_POINT('Ctrl Pts',(209.567237343965,-4.05107496711084,2.83131889085814));
#36671=CARTESIAN_POINT('Ctrl Pts',(209.540840820279,-3.58165310941424,3.50297182569741));
#36672=CARTESIAN_POINT('Ctrl Pts',(209.514444296593,-2.94160133261193,4.05537249567538));
#36673=CARTESIAN_POINT('Ctrl Pts',(209.488047772907,-2.20852840820168,4.42153669317007));
#36674=CARTESIAN_POINT('Ctrl Pts',(209.461651249221,-1.47545548379142,4.78770089066475));
#36675=CARTESIAN_POINT('Ctrl Pts',(209.435254725536,-0.649361411773217,
4.96762861567614));
#36676=CARTESIAN_POINT('Ctrl Pts',(209.40885820185,0.16959176212969,4.93951348019594));
#36677=CARTESIAN_POINT('Ctrl Pts',(209.386572134567,0.861017866287247,4.9157764226786));
#36678=CARTESIAN_POINT('Ctrl Pts',(209.364286067283,1.54735387132166,4.74374446378248));
#36679=CARTESIAN_POINT('Ctrl Pts',(209.342,2.1693573297895,4.44063731407458));
#36680=CARTESIAN_POINT('',(209.342,-2.16917135428513,4.44050218283347));
#36681=CARTESIAN_POINT('Origin',(209.342,0.,0.));
#36682=CARTESIAN_POINT('Ctrl Pts',(209.342,-2.16917135428514,4.44050218283347));
#36683=CARTESIAN_POINT('Ctrl Pts',(209.368396523686,-2.90564751248118,4.08073589521655));
#36684=CARTESIAN_POINT('Ctrl Pts',(209.394793047372,-3.55049743892233,3.53432461158655));
#36685=CARTESIAN_POINT('Ctrl Pts',(209.421189571058,-4.02583336624512,2.86696358887512));
#36686=CARTESIAN_POINT('Ctrl Pts',(209.447586094743,-4.50116929356792,2.19960256616367));
#36687=CARTESIAN_POINT('Ctrl Pts',(209.473982618429,-4.80699122177235,1.41129180437078));
#36688=CARTESIAN_POINT('Ctrl Pts',(209.500379142115,-4.90613404925993,0.597858302054359));
#36689=CARTESIAN_POINT('Ctrl Pts',(209.506812609858,-4.93029754101932,0.399604991874226));
#36690=CARTESIAN_POINT('Ctrl Pts',(209.5132460776,-4.94218400193112,0.199859355380918));
#36691=CARTESIAN_POINT('Ctrl Pts',(209.519679545343,-4.94198289688221,9.21666299965981E-5));
#36692=CARTESIAN_POINT('Origin',(215.7,0.,0.));
#36693=CARTESIAN_POINT('',(210.664320454657,-4.94221937800576,-0.000104761278833521));
#36694=CARTESIAN_POINT('',(210.519679545343,-4.94226008201731,-9.58615277245487E-5));
#36695=CARTESIAN_POINT('',(215.7,-4.942,-6.05220448138622E-16));
#36696=CARTESIAN_POINT('Ctrl Pts',(210.664320454657,-4.94221937800576,-0.000104761278833521));
#36697=CARTESIAN_POINT('Ctrl Pts',(210.641780892342,-4.941563040604,0.699682317088681));
#36698=CARTESIAN_POINT('Ctrl Pts',(210.619241330028,-4.79143840278129,1.39974202050533));
#36699=CARTESIAN_POINT('Ctrl Pts',(210.596701767713,-4.50302543707184,2.03723795764061));
#36700=CARTESIAN_POINT('Ctrl Pts',(210.570305244027,-4.16525935384578,2.78382195822132));
#36701=CARTESIAN_POINT('Ctrl Pts',(210.543908720341,-3.63782790166743,3.44459842901169));
#36702=CARTESIAN_POINT('Ctrl Pts',(210.517512196655,-2.98468296975735,3.93944718870812));
#36703=CARTESIAN_POINT('Ctrl Pts',(210.491115672969,-2.33153803784727,4.43429594840454));
#36704=CARTESIAN_POINT('Ctrl Pts',(210.464719149284,-1.55267962620546,4.76321699700701));
#36705=CARTESIAN_POINT('Ctrl Pts',(210.438322625598,-0.742545536773605,
4.88632814185778));
#36706=CARTESIAN_POINT('Ctrl Pts',(210.411926101912,0.0675885526582515,
5.00943928670855));
#36707=CARTESIAN_POINT('Ctrl Pts',(210.385529578226,0.908998319880143,4.92674052780762));
#36708=CARTESIAN_POINT('Ctrl Pts',(210.35913305454,1.67966151371283,4.64825922034747));
#36709=CARTESIAN_POINT('Ctrl Pts',(210.332736530854,2.45032470754551,4.36977791288732));
#36710=CARTESIAN_POINT('Ctrl Pts',(210.306340007169,3.15024132798898,3.89551405686796));
#36711=CARTESIAN_POINT('Ctrl Pts',(210.279943483483,3.69454538824977,3.28297288476245));
#36712=CARTESIAN_POINT('Ctrl Pts',(210.253546959797,4.23884944851057,2.67043171265694));
#36713=CARTESIAN_POINT('Ctrl Pts',(210.227150436111,4.62754094858869,1.91961322446529));
#36714=CARTESIAN_POINT('Ctrl Pts',(210.200753912425,4.81349043727808,1.12155534276936));
#36715=CARTESIAN_POINT('Ctrl Pts',(210.174357388739,4.99943992596747,0.323497461073427));
#36716=CARTESIAN_POINT('Ctrl Pts',(210.147960865053,4.98264740326812,-0.521799814126788));
#36717=CARTESIAN_POINT('Ctrl Pts',(210.121564341368,4.76514898523828,-1.31184287638444));
#36718=CARTESIAN_POINT('Ctrl Pts',(210.095167817682,4.54765056720844,-2.10188593864209));
#36719=CARTESIAN_POINT('Ctrl Pts',(210.068771293996,4.12944625384811,-2.83667478795718));
#36720=CARTESIAN_POINT('Ctrl Pts',(210.04237477031,3.5612439805398,-3.42711510149462));
#36721=CARTESIAN_POINT('Ctrl Pts',(210.015978246624,2.99304170723149,-4.01755541503206));
#36722=CARTESIAN_POINT('Ctrl Pts',(209.989581722938,2.27484147397519,-4.46364719279186));
#36723=CARTESIAN_POINT('Ctrl Pts',(209.963185199253,1.49372616717388,-4.71130116034573));
#36724=CARTESIAN_POINT('Ctrl Pts',(209.936788675567,0.712610860372571,-4.95895512789961));
#36725=CARTESIAN_POINT('Ctrl Pts',(209.910392151881,-0.13141951997376,-5.00817128524755));
#36726=CARTESIAN_POINT('Ctrl Pts',(209.883995628195,-0.936024934326331,
-4.85298198583465));
#36727=CARTESIAN_POINT('Ctrl Pts',(209.857599104509,-1.7406303486789,-4.69779268642175));
#36728=CARTESIAN_POINT('Ctrl Pts',(209.831202580823,-2.50581079703771,-4.33819793024801));
#36729=CARTESIAN_POINT('Ctrl Pts',(209.804806057137,-3.1387870254314,-3.81779937891553));
#36730=CARTESIAN_POINT('Ctrl Pts',(209.778409533452,-3.7717632538251,-3.29740082758306));
#36731=CARTESIAN_POINT('Ctrl Pts',(209.752013009766,-4.27253526225367,-2.61619848109185));
#36732=CARTESIAN_POINT('Ctrl Pts',(209.72561648608,-4.58038350501912,-1.85678869264318));
#36733=CARTESIAN_POINT('Ctrl Pts',(209.705184475606,-4.81867088693121,-1.26897383730318));
#36734=CARTESIAN_POINT('Ctrl Pts',(209.684752465131,-4.9413698125332,-0.634301730049446));
#36735=CARTESIAN_POINT('Ctrl Pts',(209.664320454657,-4.9420180477033,0.000126580456323855));
#36736=CARTESIAN_POINT('Ctrl Pts',(209.519679545343,-4.94198289688221,9.21666299965981E-5));
#36737=CARTESIAN_POINT('Ctrl Pts',(209.539642601286,-4.94135886774234,-0.619785592014529));
#36738=CARTESIAN_POINT('Ctrl Pts',(209.559605657229,-4.82434832763514,-1.23987086903581));
#36739=CARTESIAN_POINT('Ctrl Pts',(209.579568713173,-4.59661203239717,-1.81622046758434));
#36740=CARTESIAN_POINT('Ctrl Pts',(209.605965236859,-4.2954834612761,-2.57830949206667));
#36741=CARTESIAN_POINT('Ctrl Pts',(209.632361760544,-3.80076259226322,-3.26393129819136));
#36742=CARTESIAN_POINT('Ctrl Pts',(209.65875828423,-3.17241385187217,-3.78990976178524));
#36743=CARTESIAN_POINT('Ctrl Pts',(209.685154807916,-2.54406511148113,-4.31588822537912));
#36744=CARTESIAN_POINT('Ctrl Pts',(209.711551331602,-1.7820884997119,-4.68222334644218));
#36745=CARTESIAN_POINT('Ctrl Pts',(209.737947855288,-0.978885076945217,
-4.8445163738841));
#36746=CARTESIAN_POINT('Ctrl Pts',(209.764344378974,-0.175681654178535,
-5.00680940132602));
#36747=CARTESIAN_POINT('Ctrl Pts',(209.790740902659,0.668748579585601,-4.96506033514679));
#36748=CARTESIAN_POINT('Ctrl Pts',(209.817137426345,1.45202191277295,-4.72432184612485));
#36749=CARTESIAN_POINT('Ctrl Pts',(209.843533950031,2.2352952459603,-4.48358335710292));
#36750=CARTESIAN_POINT('Ctrl Pts',(209.869930473717,2.95741167857085,-4.04385544523827));
#36751=CARTESIAN_POINT('Ctrl Pts',(209.896326997403,3.53081120871917,-3.45846025712288));
#36752=CARTESIAN_POINT('Ctrl Pts',(209.922723521089,4.10421073886749,-2.87306506900749));
#36753=CARTESIAN_POINT('Ctrl Pts',(209.949120044775,4.52889336655357,-2.14200260464136));
#36754=CARTESIAN_POINT('Ctrl Pts',(209.97551656846,4.75336671917514,-1.35391323544134));
#36755=CARTESIAN_POINT('Ctrl Pts',(210.001913092146,4.97784007179672,-0.565823866241315));
#36756=CARTESIAN_POINT('Ctrl Pts',(210.028309615832,5.00210414935379,0.279292407792593));
#36757=CARTESIAN_POINT('Ctrl Pts',(210.054706139518,4.82321639471094,1.07896292800015));
#36758=CARTESIAN_POINT('Ctrl Pts',(210.081102663204,4.64432864006809,1.8786334482077));
#36759=CARTESIAN_POINT('Ctrl Pts',(210.10749918689,4.26228905322531,2.63285821458891));
#36760=CARTESIAN_POINT('Ctrl Pts',(210.133895710575,3.72342076754685,3.25018675848713));
#36761=CARTESIAN_POINT('Ctrl Pts',(210.160292234261,3.18455248186838,3.86751530238536));
#36762=CARTESIAN_POINT('Ctrl Pts',(210.186688757947,2.48885549735423,4.34794762380061));
#36763=CARTESIAN_POINT('Ctrl Pts',(210.213085281633,1.72068405168742,4.63323033259046));
#36764=CARTESIAN_POINT('Ctrl Pts',(210.239481805319,0.952512606020613,4.91851304138032));
#36765=CARTESIAN_POINT('Ctrl Pts',(210.265878329005,0.11186669920115,5.00864613754478));
#36766=CARTESIAN_POINT('Ctrl Pts',(210.292274852691,-0.699323984278334,
4.8927009452202));
#36767=CARTESIAN_POINT('Ctrl Pts',(210.318671376376,-1.51051466775782,4.77675575289561));
#36768=CARTESIAN_POINT('Ctrl Pts',(210.345067900062,-2.29225012789733,4.45473227208197));
#36769=CARTESIAN_POINT('Ctrl Pts',(210.371464423748,-2.94974374088599,3.96567630539273));
#36770=CARTESIAN_POINT('Ctrl Pts',(210.397860947434,-3.60723735387464,3.4766203387035));
#36771=CARTESIAN_POINT('Ctrl Pts',(210.42425747112,-4.14048911971245,2.82053188613866));
#36772=CARTESIAN_POINT('Ctrl Pts',(210.450653994806,-4.48484141537169,2.07696272260168));
#36773=CARTESIAN_POINT('Ctrl Pts',(210.473662511651,-4.78499592396769,1.42883102810752));
#36774=CARTESIAN_POINT('Ctrl Pts',(210.496671028497,-4.94162974142002,0.714233863442395));
#36775=CARTESIAN_POINT('Ctrl Pts',(210.519679545343,-4.94226008201731,-9.58615277245487E-5));
#36776=CARTESIAN_POINT('Origin',(215.7,0.,0.));
#36777=CARTESIAN_POINT('',(211.664320454657,-4.9415897287205,1.37434265569392E-5));
#36778=CARTESIAN_POINT('',(211.519679545343,-4.94158749800685,3.21734411369081E-7));
#36779=CARTESIAN_POINT('',(215.7,-4.942,-6.05220448138622E-16));
#36780=CARTESIAN_POINT('Ctrl Pts',(211.664320454657,-4.9415897287205,1.37434265569392E-5));
#36781=CARTESIAN_POINT('Ctrl Pts',(211.651602366925,-4.94162817182109,0.395017559605729));
#36782=CARTESIAN_POINT('Ctrl Pts',(211.638884279193,-4.89482715788202,0.790012419678822));
#36783=CARTESIAN_POINT('Ctrl Pts',(211.626166191461,-4.80108290976675,1.17353290387558));
#36784=CARTESIAN_POINT('Ctrl Pts',(211.599769667775,-4.60651574543051,1.96953366739189));
#36785=CARTESIAN_POINT('Ctrl Pts',(211.573373144089,-4.20972916787737,2.7161057624864));
#36786=CARTESIAN_POINT('Ctrl Pts',(211.546976620403,-3.65883417083036,3.32272615382265));
#36787=CARTESIAN_POINT('Ctrl Pts',(211.520580096718,-3.10793917378334,3.92934654515892));
#36788=CARTESIAN_POINT('Ctrl Pts',(211.494183573032,-2.40293575724243,4.39601523273692));
#36789=CARTESIAN_POINT('Ctrl Pts',(211.467787049346,-1.62930668919103,4.66614790758825));
#36790=CARTESIAN_POINT('Ctrl Pts',(211.44139052566,-0.855677621139631,4.9362805824396));
#36791=CARTESIAN_POINT('Ctrl Pts',(211.414994001974,-0.0134229015777539,
5.00987724456428));
#36792=CARTESIAN_POINT('Ctrl Pts',(211.388597478288,0.795332766144239,4.87801418345934));
#36793=CARTESIAN_POINT('Ctrl Pts',(211.362200954603,1.60408843386621,4.7461511223544));
#36794=CARTESIAN_POINT('Ctrl Pts',(211.335804430917,2.37934504974831,4.40882833801985));
#36795=CARTESIAN_POINT('Ctrl Pts',(211.309407907231,3.02710153540114,3.90694674615674));
#36796=CARTESIAN_POINT('Ctrl Pts',(211.283011383545,3.67485802105398,3.40506515429362));
#36797=CARTESIAN_POINT('Ctrl Pts',(211.256614859859,4.19511437647758,2.73862475490193));
#36798=CARTESIAN_POINT('Ctrl Pts',(211.230218336173,4.52478870408222,1.98843248976257));
#36799=CARTESIAN_POINT('Ctrl Pts',(211.203821812487,4.85446303168686,1.23824022462321));
#36800=CARTESIAN_POINT('Ctrl Pts',(211.177425288802,4.99355533147254,0.404296093736161));
#36801=CARTESIAN_POINT('Ctrl Pts',(211.151028765116,4.92520044433258,-0.412282871435125));
#36802=CARTESIAN_POINT('Ctrl Pts',(211.12463224143,4.85684555719262,-1.22886183660641));
#36803=CARTESIAN_POINT('Ctrl Pts',(211.098235717744,4.58104348312702,-2.02807563606193));
#36804=CARTESIAN_POINT('Ctrl Pts',(211.071839194058,4.13123565540155,-2.7130183453989));
#36805=CARTESIAN_POINT('Ctrl Pts',(211.045442670372,3.68142782767608,-3.39796105473587));
#36806=CARTESIAN_POINT('Ctrl Pts',(211.019046146687,3.05761424629074,-3.9686326739543));
#36807=CARTESIAN_POINT('Ctrl Pts',(210.992649623001,2.33543328460936,-4.35583837579821));
#36808=CARTESIAN_POINT('Ctrl Pts',(210.966253099315,1.61325232292797,-4.74304407764211));
#36809=CARTESIAN_POINT('Ctrl Pts',(210.939856575629,0.792703980950555,-4.94678386211149));
#36810=CARTESIAN_POINT('Ctrl Pts',(210.913460051943,-0.0267189702393086,
-4.942353961378));
#36811=CARTESIAN_POINT('Ctrl Pts',(210.887063528257,-0.846141921429158,
-4.93792406064451));
#36812=CARTESIAN_POINT('Ctrl Pts',(210.860667004571,-1.66443948183145,-4.72532447470816));
#36813=CARTESIAN_POINT('Ctrl Pts',(210.834270480886,-2.38239179114626,-4.33033323618878));
#36814=CARTESIAN_POINT('Ctrl Pts',(210.8078739572,-3.10034410046108,-3.9353419976694));
#36815=CARTESIAN_POINT('Ctrl Pts',(210.781477433514,-3.71795115868842,-3.35795910656698));
#36816=CARTESIAN_POINT('Ctrl Pts',(210.755080909828,-4.16032714312371,-2.66819314238538));
#36817=CARTESIAN_POINT('Ctrl Pts',(210.728684386142,-4.60270312755899,-1.97842717820379));
#36818=CARTESIAN_POINT('Ctrl Pts',(210.702287862456,-4.86984803820222,-1.17627814094302));
#36819=CARTESIAN_POINT('Ctrl Pts',(210.67589133877,-4.92937013638695,-0.359007857127102));
#36820=CARTESIAN_POINT('Ctrl Pts',(210.672034377399,-4.93806728288102,-0.239591378199565));
#36821=CARTESIAN_POINT('Ctrl Pts',(210.668177416028,-4.9423316902135,-0.1198520612323));
#36822=CARTESIAN_POINT('Ctrl Pts',(210.664320454657,-4.94221937800576,-0.000104761278833521));
#36823=CARTESIAN_POINT('Ctrl Pts',(210.519679545343,-4.94226008201731,-9.58615277245487E-5));
#36824=CARTESIAN_POINT('Ctrl Pts',(210.523067552183,-4.94235289974518,-0.10528099842556));
#36825=CARTESIAN_POINT('Ctrl Pts',(210.526455559023,-4.93906315687572,-0.210460336536133));
#36826=CARTESIAN_POINT('Ctrl Pts',(210.529843565863,-4.93235099880689,-0.315420813356548));
#36827=CARTESIAN_POINT('Ctrl Pts',(210.556240089549,-4.88005546110216,-1.13318531126868));
#36828=CARTESIAN_POINT('Ctrl Pts',(210.582636613235,-4.62001156021202,-1.93766443258382));
#36829=CARTESIAN_POINT('Ctrl Pts',(210.609033136921,-4.18375002366602,-2.63131381930358));
#36830=CARTESIAN_POINT('Ctrl Pts',(210.635429660607,-3.74748848712002,-3.32496320602334));
#36831=CARTESIAN_POINT('Ctrl Pts',(210.661826184293,-3.13500931491815,-3.90778285814772));
#36832=CARTESIAN_POINT('Ctrl Pts',(210.688222707978,-2.4205765667749,-4.30910498280575));
#36833=CARTESIAN_POINT('Ctrl Pts',(210.714619231664,-1.70614381863165,-4.71042710746378));
#36834=CARTESIAN_POINT('Ctrl Pts',(210.74101575535,-0.889757494547013,-4.93025170465545));
#36835=CARTESIAN_POINT('Ctrl Pts',(210.767412279036,-0.0704057138513457,
-4.94192469669601));
#36836=CARTESIAN_POINT('Ctrl Pts',(210.793808802722,0.748946066844314,-4.95359768873657));
#36837=CARTESIAN_POINT('Ctrl Pts',(210.820205326408,1.57126330415101,-4.75711907562602));
#36838=CARTESIAN_POINT('Ctrl Pts',(210.846601850093,2.29683874538686,-4.37631219733406));
#36839=CARTESIAN_POINT('Ctrl Pts',(210.872998373779,3.02241418662272,-3.99550531904209));
#36840=CARTESIAN_POINT('Ctrl Pts',(210.899394897465,3.65124783178774,-3.43037017556871));
#36841=CARTESIAN_POINT('Ctrl Pts',(210.925791421151,4.10709261705286,-2.74943028756545));
#36842=CARTESIAN_POINT('Ctrl Pts',(210.952187944837,4.56293740231798,-2.06849039956218));
#36843=CARTESIAN_POINT('Ctrl Pts',(210.978584468523,4.8457933276832,-1.27174576702903));
#36844=CARTESIAN_POINT('Ctrl Pts',(211.004980992209,4.92136366930947,-0.455802924132807));
#36845=CARTESIAN_POINT('Ctrl Pts',(211.031377515894,4.99693401093573,0.360139918763401));
#36846=CARTESIAN_POINT('Ctrl Pts',(211.05777403958,4.86521876882306,1.19528097202268));
#36847=CARTESIAN_POINT('Ctrl Pts',(211.084170563266,4.54218862231425,1.94835807552615));
#36848=CARTESIAN_POINT('Ctrl Pts',(211.110567086952,4.21915847580543,2.70143517902964));
#36849=CARTESIAN_POINT('Ctrl Pts',(211.136963610638,3.70481342490047,3.37244833277733));
#36850=CARTESIAN_POINT('Ctrl Pts',(211.163360134324,3.06151861224838,3.88003614133731));
#36851=CARTESIAN_POINT('Ctrl Pts',(211.189756658009,2.4182237995963,4.38762394989728));
#36852=CARTESIAN_POINT('Ctrl Pts',(211.216153181695,1.64597922519708,4.73178641326956));
#36853=CARTESIAN_POINT('Ctrl Pts',(211.242549705381,0.838420752701002,4.87079329397425));
#36854=CARTESIAN_POINT('Ctrl Pts',(211.268946229067,0.0308622802049217,
5.00980017467893));
#36855=CARTESIAN_POINT('Ctrl Pts',(211.295342752753,-0.812010090388028,
4.94365147271603));
#36856=CARTESIAN_POINT('Ctrl Pts',(211.321739276439,-1.58799676457591,4.68036782175277));
#36857=CARTESIAN_POINT('Ctrl Pts',(211.348135800125,-2.3639834387638,4.4170841707895));
#36858=CARTESIAN_POINT('Ctrl Pts',(211.37453232381,-3.07308441654662,3.95666557082588));
#36859=CARTESIAN_POINT('Ctrl Pts',(211.400928847496,-3.62932009422403,3.35493849792489));
#36860=CARTESIAN_POINT('Ctrl Pts',(211.427325371182,-4.18555577190144,2.7532114250239));
#36861=CARTESIAN_POINT('Ctrl Pts',(211.453721894868,-4.58892614947342,2.01017587918554));
#36862=CARTESIAN_POINT('Ctrl Pts',(211.480118418554,-4.79052193715797,1.21592608361099));
#36863=CARTESIAN_POINT('Ctrl Pts',(211.493305460817,-4.891234144716,0.81913877379881));
#36864=CARTESIAN_POINT('Ctrl Pts',(211.50649250308,-4.94158843063211,0.409569660407683));
#36865=CARTESIAN_POINT('Ctrl Pts',(211.519679545343,-4.94158749800685,3.21734411369081E-7));
#36866=CARTESIAN_POINT('Origin',(215.7,0.,0.));
#36867=CARTESIAN_POINT('',(212.664320454657,-4.94229966671163,8.50863313224884E-5));
#36868=CARTESIAN_POINT('',(212.519679545343,-4.94226196377334,9.54014550954459E-5));
#36869=CARTESIAN_POINT('',(215.7,-4.942,-6.05220448138622E-16));
#36870=CARTESIAN_POINT('Ctrl Pts',(212.664320454657,-4.94229966671163,8.50863313224884E-5));
#36871=CARTESIAN_POINT('Ctrl Pts',(212.661423841508,-4.94237235712893,0.0900121728263076));
#36872=CARTESIAN_POINT('Ctrl Pts',(212.658527228358,-4.93996817019507,0.179935373971945));
#36873=CARTESIAN_POINT('Ctrl Pts',(212.655630615209,-4.93506096691248,0.269721774778861));
#36874=CARTESIAN_POINT('Ctrl Pts',(212.629234091523,-4.89034215186677,1.08793557601746));
#36875=CARTESIAN_POINT('Ctrl Pts',(212.602837567838,-4.63776082920043,1.89478881963755));
#36876=CARTESIAN_POINT('Ctrl Pts',(212.576441044152,-4.20794287971893,2.59244928666999));
#36877=CARTESIAN_POINT('Ctrl Pts',(212.550044520466,-3.77812493023742,3.29010975370243));
#36878=CARTESIAN_POINT('Ctrl Pts',(212.52364799678,-3.17107035394075,3.87857744414721));
#36879=CARTESIAN_POINT('Ctrl Pts',(212.497251473094,-2.46038546858754,4.28649972925419));
#36880=CARTESIAN_POINT('Ctrl Pts',(212.470854949408,-1.74970058323433,4.69442201436117));
#36881=CARTESIAN_POINT('Ctrl Pts',(212.444458425722,-0.935385388824589,
4.92179889413036));
#36882=CARTESIAN_POINT('Ctrl Pts',(212.418061902037,-0.116176877542877,
4.94106056591673));
#36883=CARTESIAN_POINT('Ctrl Pts',(212.391665378351,0.703031633738836,4.9603222377031));
#36884=CARTESIAN_POINT('Ctrl Pts',(212.365268854665,1.52713346189252,4.77146870150665));
#36885=CARTESIAN_POINT('Ctrl Pts',(212.338872330979,2.25620497007056,4.39739874425346));
#36886=CARTESIAN_POINT('Ctrl Pts',(212.312475807293,2.9852764782486,4.02332878700027));
#36887=CARTESIAN_POINT('Ctrl Pts',(212.286079283607,3.61931766645099,3.46404240869033));
#36888=CARTESIAN_POINT('Ctrl Pts',(212.259682759921,4.08145004797628,2.78735395829224));
#36889=CARTESIAN_POINT('Ctrl Pts',(212.233286236236,4.54358242950156,2.11066550789415));
#36890=CARTESIAN_POINT('Ctrl Pts',(212.20688971255,4.83380600434973,1.31657498540791));
#36891=CARTESIAN_POINT('Ctrl Pts',(212.180493188864,4.91693070970694,0.501367109884335));
#36892=CARTESIAN_POINT('Ctrl Pts',(212.154096665178,5.00005541506415,-0.313840765639247));
#36893=CARTESIAN_POINT('Ctrl Pts',(212.127700141492,4.87608125093039,-1.15016599420016));
#36894=CARTESIAN_POINT('Ctrl Pts',(212.101303617806,4.56004027879635,-1.90620283251492));
#36895=CARTESIAN_POINT('Ctrl Pts',(212.07490709412,4.2439993066623,-2.66223967082967));
#36896=CARTESIAN_POINT('Ctrl Pts',(212.048510570435,3.73589152652797,-3.33798811889825));
#36897=CARTESIAN_POINT('Ctrl Pts',(212.022114046749,3.09732580220978,-3.85151261946505));
#36898=CARTESIAN_POINT('Ctrl Pts',(211.995717523063,2.45876007789159,-4.36503712003185));
#36899=CARTESIAN_POINT('Ctrl Pts',(211.969320999377,1.68973640938953,-4.71633767309686));
#36900=CARTESIAN_POINT('Ctrl Pts',(211.942924475691,0.883500120465094,-4.86281853661754));
#36901=CARTESIAN_POINT('Ctrl Pts',(211.916527952005,0.0772638315406597,
-5.00929940013821));
#36902=CARTESIAN_POINT('Ctrl Pts',(211.89013142832,-0.766185077806151,-4.95096057411454));
#36903=CARTESIAN_POINT('Ctrl Pts',(211.863734904634,-1.54457710684397,-4.69487573253505));
#36904=CARTESIAN_POINT('Ctrl Pts',(211.837338380948,-2.32296913588178,-4.43879089095556));
#36905=CARTESIAN_POINT('Ctrl Pts',(211.810941857262,-3.03630428461059,-3.98496003382025));
#36906=CARTESIAN_POINT('Ctrl Pts',(211.784545333576,-3.59808954947537,-3.38841086305795));
#36907=CARTESIAN_POINT('Ctrl Pts',(211.75814880989,-4.15987481434016,-2.79186169229563));
#36908=CARTESIAN_POINT('Ctrl Pts',(211.731752286205,-4.5701101953409,-2.0525942079063));
#36909=CARTESIAN_POINT('Ctrl Pts',(211.705355762519,-4.77905401028161,-1.26024574974258));
#36910=CARTESIAN_POINT('Ctrl Pts',(211.691677326565,-4.88732677470474,-0.849658061487058));
#36911=CARTESIAN_POINT('Ctrl Pts',(211.677998890611,-4.941548382765,-0.424816979164754));
#36912=CARTESIAN_POINT('Ctrl Pts',(211.664320454657,-4.9415897287205,1.37434265569392E-5));
#36913=CARTESIAN_POINT('Ctrl Pts',(211.519679545343,-4.94158749800685,3.21734411369081E-7));
#36914=CARTESIAN_POINT('Ctrl Pts',(211.532889026766,-4.94158656379464,-0.410265942875176));
#36915=CARTESIAN_POINT('Ctrl Pts',(211.546098508189,-4.89105889568341,-0.820532433534242));
#36916=CARTESIAN_POINT('Ctrl Pts',(211.559307989611,-4.79000721059605,-1.21795221319883));
#36917=CARTESIAN_POINT('Ctrl Pts',(211.585704513297,-4.58807549855246,-2.01211666912335));
#36918=CARTESIAN_POINT('Ctrl Pts',(211.612101036983,-4.18439087666816,-2.75498153566165));
#36919=CARTESIAN_POINT('Ctrl Pts',(211.638497560669,-3.62790073734079,-3.3564732847439));
#36920=CARTESIAN_POINT('Ctrl Pts',(211.664894084355,-3.07141059801342,-3.95796503382616));
#36921=CARTESIAN_POINT('Ctrl Pts',(211.691290608041,-2.36211494124297,-4.41808366545237));
#36922=CARTESIAN_POINT('Ctrl Pts',(211.717687131727,-1.58601697586039,-4.68103907519265));
#36923=CARTESIAN_POINT('Ctrl Pts',(211.744083655412,-0.809919010477825,
-4.94399448493293));
#36924=CARTESIAN_POINT('Ctrl Pts',(211.770480179098,0.0329812635168701,
-5.00978667278729));
#36925=CARTESIAN_POINT('Ctrl Pts',(211.796876702784,0.840480868287655,-4.87043823297658));
#36926=CARTESIAN_POINT('Ctrl Pts',(211.82327322647,1.64798047305844,-4.73108979316587));
#36927=CARTESIAN_POINT('Ctrl Pts',(211.849669750156,2.42007940860532,-4.38660072569009));
#36928=CARTESIAN_POINT('Ctrl Pts',(211.876066273842,3.06315947022311,-3.87874086930026));
#36929=CARTESIAN_POINT('Ctrl Pts',(211.902462797527,3.7062395318409,-3.37088101291043));
#36930=CARTESIAN_POINT('Ctrl Pts',(211.928859321213,4.22030071952961,-2.69965036760654));
#36931=CARTESIAN_POINT('Ctrl Pts',(211.955255844899,4.54301230948639,-1.94643669998611));
#36932=CARTESIAN_POINT('Ctrl Pts',(211.981652368585,4.86572389944316,-1.19322303236568));
#36933=CARTESIAN_POINT('Ctrl Pts',(212.008048892271,4.99708589166801,-0.358026342428714));
#36934=CARTESIAN_POINT('Ctrl Pts',(212.034445415957,4.92117043894809,0.457884463616269));
#36935=CARTESIAN_POINT('Ctrl Pts',(212.060841939643,4.84525498622817,1.27379526966126));
#36936=CARTESIAN_POINT('Ctrl Pts',(212.087238463328,4.56206208856348,2.07042019181425));
#36937=CARTESIAN_POINT('Ctrl Pts',(212.113634987014,4.10592932815241,2.75116721109706));
#36938=CARTESIAN_POINT('Ctrl Pts',(212.1400315107,3.64979656774134,3.43191423037987));
#36939=CARTESIAN_POINT('Ctrl Pts',(212.166428034386,3.02072394458389,3.9967833467925));
#36940=CARTESIAN_POINT('Ctrl Pts',(212.192824558072,2.29498749909123,4.37728329563128));
#36941=CARTESIAN_POINT('Ctrl Pts',(212.219221081758,1.56925105359856,4.75778324447007));
#36942=CARTESIAN_POINT('Ctrl Pts',(212.245617605443,0.746850785770678,4.95391402573501));
#36943=CARTESIAN_POINT('Ctrl Pts',(212.272014129129,-0.072495984398216,
4.94189447514248));
#36944=CARTESIAN_POINT('Ctrl Pts',(212.298410652815,-0.89184275456711,4.92987492454996));
#36945=CARTESIAN_POINT('Ctrl Pts',(212.324807176501,-1.70813602707702,4.70970504209997));
#36946=CARTESIAN_POINT('Ctrl Pts',(212.351203700187,-2.42239896467692,4.30808077072957));
#36947=CARTESIAN_POINT('Ctrl Pts',(212.377600223873,-3.13666190227682,3.90645649935917));
#36948=CARTESIAN_POINT('Ctrl Pts',(212.403996747559,-3.74889450496672,3.32337783906836));
#36949=CARTESIAN_POINT('Ctrl Pts',(212.430393271244,-4.18486261118127,2.62954399026423));
#36950=CARTESIAN_POINT('Ctrl Pts',(212.45678979493,-4.62083071739583,1.93571014146011));
#36951=CARTESIAN_POINT('Ctrl Pts',(212.483186318616,-4.88053432713503,1.13112110414268));
#36952=CARTESIAN_POINT('Ctrl Pts',(212.509582842302,-4.93248397113545,0.313334558722124));
#36953=CARTESIAN_POINT('Ctrl Pts',(212.512948409982,-4.93910757221779,0.209066436166142));
#36954=CARTESIAN_POINT('Ctrl Pts',(212.516313977663,-4.94235385099752,0.104583770228035));
#36955=CARTESIAN_POINT('Ctrl Pts',(212.519679545343,-4.94226196377334,9.54014550954459E-5));
#36956=CARTESIAN_POINT('Origin',(215.7,0.,0.));
#36957=CARTESIAN_POINT('',(213.664320454657,-4.94192591391644,-0.000125637169695325));
#36958=CARTESIAN_POINT('',(213.519679545343,-4.94197050942031,-0.000126753746856371));
#36959=CARTESIAN_POINT('',(215.7,-4.942,-6.05220448138622E-16));
#36960=CARTESIAN_POINT('Ctrl Pts',(213.664320454657,-4.94192591391644,-0.000125637169695325));
#36961=CARTESIAN_POINT('Ctrl Pts',(213.644848792405,-4.94133232753319,0.604515633599268));
#36962=CARTESIAN_POINT('Ctrl Pts',(213.625377130152,-4.8301532058668,1.20936919881882));
#36963=CARTESIAN_POINT('Ctrl Pts',(213.6059054679,-4.61324303097403,1.77357416537976));
#36964=CARTESIAN_POINT('Ctrl Pts',(213.579508944214,-4.31919137297763,2.53843181186435));
#36965=CARTESIAN_POINT('Ctrl Pts',(213.553112420528,-3.8308320314266,3.2285873268173));
#36966=CARTESIAN_POINT('Ctrl Pts',(213.526715896842,-3.2073793410417,3.76035827356807));
#36967=CARTESIAN_POINT('Ctrl Pts',(213.500319373156,-2.58392665065679,4.29212922031885));
#36968=CARTESIAN_POINT('Ctrl Pts',(213.473922849471,-1.82538061143801,4.66551559886746));
#36969=CARTESIAN_POINT('Ctrl Pts',(213.447526325785,-1.02371611819283,4.83524372625467));
#36970=CARTESIAN_POINT('Ctrl Pts',(213.421129802099,-0.222051624947664,
5.00497185364188));
#36971=CARTESIAN_POINT('Ctrl Pts',(213.394733278413,0.62273132232389,4.97104172986771));
#36972=CARTESIAN_POINT('Ctrl Pts',(213.368336754727,1.40820146870356,4.73756743555953));
#36973=CARTESIAN_POINT('Ctrl Pts',(213.341940231041,2.19367161508324,4.50409314125135));
#36974=CARTESIAN_POINT('Ctrl Pts',(213.315543707355,2.91982896057103,4.07107467640918));
#36975=CARTESIAN_POINT('Ctrl Pts',(213.28914718367,3.49862579018089,3.49101620781315));
#36976=CARTESIAN_POINT('Ctrl Pts',(213.262750659984,4.07742261979076,2.91095773921712));
#36977=CARTESIAN_POINT('Ctrl Pts',(213.236354136298,4.5088589335227,2.18385926686723));
#36978=CARTESIAN_POINT('Ctrl Pts',(213.209957612612,4.74062240289565,1.39788261885495));
#36979=CARTESIAN_POINT('Ctrl Pts',(213.183561088926,4.9723858722686,0.611905970842695));
#36980=CARTESIAN_POINT('Ctrl Pts',(213.15716456524,5.00447649728257,-0.232948852831949));
#36981=CARTESIAN_POINT('Ctrl Pts',(213.130768041555,4.83300323941469,-1.03424188212432));
#36982=CARTESIAN_POINT('Ctrl Pts',(213.104371517869,4.66152998154681,-1.83553491141671));
#36983=CARTESIAN_POINT('Ctrl Pts',(213.077974994183,4.28649284079707,-2.59326614632683));
#36984=CARTESIAN_POINT('Ctrl Pts',(213.051578470497,3.75336565762595,-3.21555948834523));
#36985=CARTESIAN_POINT('Ctrl Pts',(213.025181946811,3.22023847445484,-3.83785283036363));
#36986=CARTESIAN_POINT('Ctrl Pts',(212.998785423125,2.52902124886233,-4.32470827949033));
#36987=CARTESIAN_POINT('Ctrl Pts',(212.972388899439,1.7635251515962,-4.61709385031543));
#36988=CARTESIAN_POINT('Ctrl Pts',(212.945992375754,0.998029054330063,-4.90947942114053));
#36989=CARTESIAN_POINT('Ctrl Pts',(212.919595852068,0.158254085390298,-5.00739511366405));
#36990=CARTESIAN_POINT('Ctrl Pts',(212.893199328382,-0.653975725517873,
-4.89896849687425));
#36991=CARTESIAN_POINT('Ctrl Pts',(212.866802804696,-1.46620553642604,-4.79054188008444));
#36992=CARTESIAN_POINT('Ctrl Pts',(212.84040628101,-2.25089018930262,-4.47577295398131));
#36993=CARTESIAN_POINT('Ctrl Pts',(212.814009757324,-2.91288544151243,-3.99282794364569));
#36994=CARTESIAN_POINT('Ctrl Pts',(212.787613233638,-3.57488069372224,-3.50988293331007));
#36995=CARTESIAN_POINT('Ctrl Pts',(212.761216709953,-4.1141865452653,-2.85876183874197));
#36996=CARTESIAN_POINT('Ctrl Pts',(212.734820186267,-4.46541131732428,-2.11841411202937));
#36997=CARTESIAN_POINT('Ctrl Pts',(212.71132027573,-4.77809456379463,-1.45930818009766));
#36998=CARTESIAN_POINT('Ctrl Pts',(212.687820365194,-4.94170993718427,-0.729483681936857));
#36999=CARTESIAN_POINT('Ctrl Pts',(212.664320454657,-4.94229966671163,8.50863313224884E-5));
#37000=CARTESIAN_POINT('Ctrl Pts',(212.519679545343,-4.94226196377334,9.54014550954459E-5));
#37001=CARTESIAN_POINT('Ctrl Pts',(212.542710501349,-4.94163316922262,-0.714930190902053));
#37002=CARTESIAN_POINT('Ctrl Pts',(212.565741457354,-4.78468413781976,-1.4302228366333));
#37003=CARTESIAN_POINT('Ctrl Pts',(212.588772413359,-4.48396252385269,-2.07885948440059));
#37004=CARTESIAN_POINT('Ctrl Pts',(212.615168937045,-4.1392957543079,-2.82228292857908));
#37005=CARTESIAN_POINT('Ctrl Pts',(212.641565460731,-3.6057665369567,-3.4781457634124));
#37006=CARTESIAN_POINT('Ctrl Pts',(212.667961984417,-2.94806612467695,-3.96692359338189));
#37007=CARTESIAN_POINT('Ctrl Pts',(212.694358508103,-2.29036571239719,-4.45570142335139));
#37008=CARTESIAN_POINT('Ctrl Pts',(212.720755031789,-1.50849410518888,-4.77739424845707));
#37009=CARTESIAN_POINT('Ctrl Pts',(212.747151555475,-0.697254459495896,
-4.89299631002423));
#37010=CARTESIAN_POINT('Ctrl Pts',(212.77354807916,0.113985186197088,-5.00859837159139));
#37011=CARTESIAN_POINT('Ctrl Pts',(212.799944602846,0.954592870374744,-4.91810966962003));
#37012=CARTESIAN_POINT('Ctrl Pts',(212.826341126532,1.72264359530558,-4.63250210089001));
#37013=CARTESIAN_POINT('Ctrl Pts',(212.852737650218,2.4906943202364,-4.34689453215999));
#37014=CARTESIAN_POINT('Ctrl Pts',(212.879134173904,3.18618808592041,-3.86616809667132));
#37015=CARTESIAN_POINT('Ctrl Pts',(212.90553069759,3.72479518442856,-3.2486116273349));
#37016=CARTESIAN_POINT('Ctrl Pts',(212.931927221275,4.26340228293672,-2.63105515799846));
#37017=CARTESIAN_POINT('Ctrl Pts',(212.958323744961,4.645122714269,-1.87666865481429));
#37018=CARTESIAN_POINT('Ctrl Pts',(212.984720268647,4.82367227851871,-1.07692266233362));
#37019=CARTESIAN_POINT('Ctrl Pts',(213.011116792333,5.00222184276842,-0.277176669852958));
#37020=CARTESIAN_POINT('Ctrl Pts',(213.037513316019,4.97760053993555,0.567928811924184));
#37021=CARTESIAN_POINT('Ctrl Pts',(213.063909839705,4.7527937415348,1.35592342026579));
#37022=CARTESIAN_POINT('Ctrl Pts',(213.090306363391,4.52798694313405,2.1439180286074));
#37023=CARTESIAN_POINT('Ctrl Pts',(213.116702887077,4.10299464916542,2.87480176351348));
#37024=CARTESIAN_POINT('Ctrl Pts',(213.143099410762,3.52934784062516,3.45995382788155));
#37025=CARTESIAN_POINT('Ctrl Pts',(213.169495934448,2.95570103208489,4.04510589224962));
#37026=CARTESIAN_POINT('Ctrl Pts',(213.195892458134,2.23339970897298,4.48452628607969));
#37027=CARTESIAN_POINT('Ctrl Pts',(213.22228898182,1.45002403752555,4.7249345986792));
#37028=CARTESIAN_POINT('Ctrl Pts',(213.248685505506,0.666648366078123,4.96534291127871));
#37029=CARTESIAN_POINT('Ctrl Pts',(213.275082029192,-0.177801653704833,
5.00673914264765));
#37030=CARTESIAN_POINT('Ctrl Pts',(213.301478552878,-0.980935134884255,
4.84410393492411));
#37031=CARTESIAN_POINT('Ctrl Pts',(213.327875076563,-1.78406861606368,4.68146872720057));
#37032=CARTESIAN_POINT('Ctrl Pts',(213.354271600249,-2.54588555863957,4.31480208038455));
#37033=CARTESIAN_POINT('Ctrl Pts',(213.380668123935,-3.17401446565158,3.78856289944251));
#37034=CARTESIAN_POINT('Ctrl Pts',(213.407064647621,-3.80214337266358,3.26232371850047));
#37035=CARTESIAN_POINT('Ctrl Pts',(213.433461171307,-4.2965842441117,2.57651200343242));
#37036=CARTESIAN_POINT('Ctrl Pts',(213.459857694993,-4.59738535025415,1.81428349837234));
#37037=CARTESIAN_POINT('Ctrl Pts',(213.479798311776,-4.82461828656924,1.238476369306));
#37038=CARTESIAN_POINT('Ctrl Pts',(213.49973892856,-4.94134715880491,0.619060605181198));
#37039=CARTESIAN_POINT('Ctrl Pts',(213.519679545343,-4.94197050942031,-0.000126753746856371));
#37040=CARTESIAN_POINT('Origin',(215.7,0.,0.));
#37041=CARTESIAN_POINT('',(214.664320454657,-4.94170537201422,9.14365381503302E-5));
#37042=CARTESIAN_POINT('',(214.519679545343,-4.9416771233585,8.15223711883949E-5));
#37043=CARTESIAN_POINT('',(215.7,-4.942,-6.05220448138622E-16));
#37044=CARTESIAN_POINT('Ctrl Pts',(214.664320454657,-4.94170537201422,9.14365381503302E-5));
#37045=CARTESIAN_POINT('Ctrl Pts',(214.654670266987,-4.94190534123349,0.299791017841205));
#37046=CARTESIAN_POINT('Ctrl Pts',(214.645020079318,-4.91507622987908,0.59945521995453));
#37047=CARTESIAN_POINT('Ctrl Pts',(214.635369891648,-4.86088328872289,0.894086257778003));
#37048=CARTESIAN_POINT('Ctrl Pts',(214.608973367962,-4.71264728505111,1.70000169017262));
#37049=CARTESIAN_POINT('Ctrl Pts',(214.582576844276,-4.35967310358994,2.4682586188898));
#37050=CARTESIAN_POINT('Ctrl Pts',(214.55618032059,-3.84475941644516,3.10570468856735));
#37051=CARTESIAN_POINT('Ctrl Pts',(214.529783796904,-3.32984572930037,3.74315075824491));
#37052=CARTESIAN_POINT('Ctrl Pts',(214.503387273219,-2.65299253647195,4.24978596888284));
#37053=CARTESIAN_POINT('Ctrl Pts',(214.476990749533,-1.8962693472472,4.56418000802155));
#37054=CARTESIAN_POINT('Ctrl Pts',(214.450594225847,-1.13954615802247,4.87857404716025));
#37055=CARTESIAN_POINT('Ctrl Pts',(214.424197702161,-0.302952972401405,
5.00072691479974));
#37056=CARTESIAN_POINT('Ctrl Pts',(214.397801178475,0.512071976119432,4.91582738450061));
#37057=CARTESIAN_POINT('Ctrl Pts',(214.371404654789,1.32709692464027,4.83092785420148));
#37058=CARTESIAN_POINT('Ctrl Pts',(214.345008131104,2.12055363606088,4.53897592596373));
#37059=CARTESIAN_POINT('Ctrl Pts',(214.318611607418,2.79623424191442,4.07537122815557));
#37060=CARTESIAN_POINT('Ctrl Pts',(214.292215083732,3.47191484776796,3.61176653034741));
#37061=CARTESIAN_POINT('Ctrl Pts',(214.265818560046,4.02981934805443,2.97650906296882));
#37062=CARTESIAN_POINT('Ctrl Pts',(214.23942203636,4.40230094867901,2.24662478847556));
#37063=CARTESIAN_POINT('Ctrl Pts',(214.213025512674,4.77478254930359,1.5167405139823));
#37064=CARTESIAN_POINT('Ctrl Pts',(214.186628988988,4.96184125026628,0.692229432374359));
#37065=CARTESIAN_POINT('Ctrl Pts',(214.160232465303,4.94079589122303,-0.126935196878605));
#37066=CARTESIAN_POINT('Ctrl Pts',(214.133835941617,4.91975053217978,-0.946099826131545));
#37067=CARTESIAN_POINT('Ctrl Pts',(214.107439417931,4.69060111313059,-1.75991800302951));
#37068=CARTESIAN_POINT('Ctrl Pts',(214.081042894245,4.28113235988322,-2.46971299953935));
#37069=CARTESIAN_POINT('Ctrl Pts',(214.054646370559,3.87166360663584,-3.17950799604922));
#37070=CARTESIAN_POINT('Ctrl Pts',(214.028249846873,3.28187551919026,-3.78527981217096));
#37071=CARTESIAN_POINT('Ctrl Pts',(214.001853323188,2.58328082650013,-4.2135776668254));
#37072=CARTESIAN_POINT('Ctrl Pts',(213.975456799502,1.88468613381001,-4.64187552147983));
#37073=CARTESIAN_POINT('Ctrl Pts',(213.949060275816,1.07728483587533,-4.89269941466696));
#37074=CARTESIAN_POINT('Ctrl Pts',(213.92266375213,0.258975604108923,-4.93563655665704));
#37075=CARTESIAN_POINT('Ctrl Pts',(213.896267228444,-0.559333627657485,
-4.97857369864712));
#37076=CARTESIAN_POINT('Ctrl Pts',(213.869870704758,-1.38855079325563,-4.81362408944015));
#37077=CARTESIAN_POINT('Ctrl Pts',(213.843474181072,-2.12813201316436,-4.46078812739161));
#37078=CARTESIAN_POINT('Ctrl Pts',(213.817077657387,-2.86771323307308,-4.10795216534308));
#37079=CARTESIAN_POINT('Ctrl Pts',(213.790681133701,-3.51765850729239,-3.56722985045298));
#37080=CARTESIAN_POINT('Ctrl Pts',(213.764284610015,-3.99916095379242,-2.90418460993702));
#37081=CARTESIAN_POINT('Ctrl Pts',(213.737888086329,-4.48066340029245,-2.24113936942106));
#37082=CARTESIAN_POINT('Ctrl Pts',(213.711491562643,-4.7937230190732,-1.45577120327923));
#37083=CARTESIAN_POINT('Ctrl Pts',(213.685095038957,-4.9003808412427,-0.643307231200192));
#37084=CARTESIAN_POINT('Ctrl Pts',(213.678170177524,-4.92836144384437,-0.430165512491651));
#37085=CARTESIAN_POINT('Ctrl Pts',(213.67124531609,-4.94213701574224,-0.215159000154365));
#37086=CARTESIAN_POINT('Ctrl Pts',(213.664320454657,-4.94192591391644,-0.000125637169695325));
#37087=CARTESIAN_POINT('Ctrl Pts',(213.519679545343,-4.94197050942031,-0.000126753746856371));
#37088=CARTESIAN_POINT('Ctrl Pts',(213.526135452245,-4.94217232331525,-0.200592766796161));
#37089=CARTESIAN_POINT('Ctrl Pts',(213.532591359148,-4.93020414732645,-0.401034838788269));
#37090=CARTESIAN_POINT('Ctrl Pts',(213.53904726605,-4.90587589242006,-0.599965331806195));
#37091=CARTESIAN_POINT('Ctrl Pts',(213.565443789736,-4.80640398760677,-1.41334036187257));
#37092=CARTESIAN_POINT('Ctrl Pts',(213.591840313422,-4.50029883714341,-2.20144512695319));
#37093=CARTESIAN_POINT('Ctrl Pts',(213.618236837108,-4.02467616975082,-2.86872069045377));
#37094=CARTESIAN_POINT('Ctrl Pts',(213.644633360794,-3.54905350235822,-3.53599625395434));
#37095=CARTESIAN_POINT('Ctrl Pts',(213.671029884479,-2.90391331803639,-4.08244261587486));
#37096=CARTESIAN_POINT('Ctrl Pts',(213.697426408165,-2.16747987414245,-4.44180229933583));
#37097=CARTESIAN_POINT('Ctrl Pts',(213.723822931851,-1.43104643024851,-4.8011619827968));
#37098=CARTESIAN_POINT('Ctrl Pts',(213.750219455537,-0.603319726782466,
-4.97343498779822));
#37099=CARTESIAN_POINT('Ctrl Pts',(213.776615979223,0.215337077601472,-4.93773294277928));
#37100=CARTESIAN_POINT('Ctrl Pts',(213.803012502909,1.03399388198541,-4.90203089776034));
#37101=CARTESIAN_POINT('Ctrl Pts',(213.829409026594,1.84358078728724,-4.65835380272105));
#37102=CARTESIAN_POINT('Ctrl Pts',(213.85580555028,2.54593411377918,-4.23624788692696));
#37103=CARTESIAN_POINT('Ctrl Pts',(213.882202073966,3.24828744027111,-3.81414197113286));
#37104=CARTESIAN_POINT('Ctrl Pts',(213.908598597652,3.84340718795315,-3.21360723458397));
#37105=CARTESIAN_POINT('Ctrl Pts',(213.934995121338,4.25913415572091,-2.50745945426226));
#37106=CARTESIAN_POINT('Ctrl Pts',(213.961391645024,4.67486112348867,-1.80131167394057));
#37107=CARTESIAN_POINT('Ctrl Pts',(213.98778816871,4.91119531134216,-0.989550849846085));
#37108=CARTESIAN_POINT('Ctrl Pts',(214.014184692395,4.93948082900791,-0.170604252763584));
#37109=CARTESIAN_POINT('Ctrl Pts',(214.040581216081,4.96776634667366,0.648342344318934));
#37110=CARTESIAN_POINT('Ctrl Pts',(214.066977739767,4.78800319415165,1.47447471438945));
#37111=CARTESIAN_POINT('Ctrl Pts',(214.093374263453,4.42198793511587,2.207623014214));
#37112=CARTESIAN_POINT('Ctrl Pts',(214.119770787139,4.05597267608009,2.94077131403855));
#37113=CARTESIAN_POINT('Ctrl Pts',(214.146167310825,3.50370531053053,3.58093554361713));
#37114=CARTESIAN_POINT('Ctrl Pts',(214.172563834511,2.83214912114986,4.05049478789539));
#37115=CARTESIAN_POINT('Ctrl Pts',(214.198960358196,2.1605929317692,4.52005403217365));
#37116=CARTESIAN_POINT('Ctrl Pts',(214.225356881882,1.36974791855743,4.8190082911516));
#37117=CARTESIAN_POINT('Ctrl Pts',(214.251753405568,0.555505277484793,4.91110889289621));
#37118=CARTESIAN_POINT('Ctrl Pts',(214.278149929254,-0.258737363587817,
5.0032094946408));
#37119=CARTESIAN_POINT('Ctrl Pts',(214.30454645294,-1.09637763252129,4.88845643915207));
#37120=CARTESIAN_POINT('Ctrl Pts',(214.330942976626,-1.85585033532817,4.58076371406123));
#37121=CARTESIAN_POINT('Ctrl Pts',(214.357339500311,-2.61532303813507,4.27307098897037));
#37122=CARTESIAN_POINT('Ctrl Pts',(214.383736023997,-3.29662817481538,3.77243859427741));
#37123=CARTESIAN_POINT('Ctrl Pts',(214.410132547683,-3.81715643091995,3.13956899161081));
#37124=CARTESIAN_POINT('Ctrl Pts',(214.436529071369,-4.33768468702453,2.5066993889442));
#37125=CARTESIAN_POINT('Ctrl Pts',(214.462925595055,-4.69743606255337,1.74159257830395));
#37126=CARTESIAN_POINT('Ctrl Pts',(214.489322118741,-4.85279014000988,0.937018958303713));
#37127=CARTESIAN_POINT('Ctrl Pts',(214.499441260941,-4.91234533068453,0.628584598965291));
#37128=CARTESIAN_POINT('Ctrl Pts',(214.509560403142,-4.94186265527411,0.314350266997381));
#37129=CARTESIAN_POINT('Ctrl Pts',(214.519679545343,-4.9416771233585,8.15223711883949E-5));
#37130=CARTESIAN_POINT('Origin',(215.7,0.,0.));
#37131=CARTESIAN_POINT('',(215.664320454657,-4.9424258920011,-5.59704580684751E-6));
#37132=CARTESIAN_POINT('',(215.519679545343,-4.94242455630813,9.71285613910342E-6));
#37133=CARTESIAN_POINT('',(215.7,-4.942,-6.05220448138622E-16));
#37134=CARTESIAN_POINT('Ctrl Pts',(215.664320454657,-4.94242563693782,-5.5936937812251E-6));
#37135=CARTESIAN_POINT('Ctrl Pts',(215.638095217884,-4.94237108343367,0.814112285436369));
#37136=CARTESIAN_POINT('Ctrl Pts',(215.611869981111,-4.7369973879704,1.62825668193243));
#37137=CARTESIAN_POINT('Ctrl Pts',(215.585644744339,-4.3507429111603,2.3449120887405));
#37138=CARTESIAN_POINT('Ctrl Pts',(215.559248220653,-3.96196566067396,3.06624824231987));
#37139=CARTESIAN_POINT('Ctrl Pts',(215.532851696967,-3.38993711145197,3.68881777271392));
#37140=CARTESIAN_POINT('Ctrl Pts',(215.506455173281,-2.70401662063462,4.1371331496901));
#37141=CARTESIAN_POINT('Ctrl Pts',(215.480058649595,-2.01809612981727,4.58544852666628));
#37142=CARTESIAN_POINT('Ctrl Pts',(215.453662125909,-1.21828369740459,4.85950975022456));
#37143=CARTESIAN_POINT('Ctrl Pts',(215.427265602223,-0.401557832984007,
4.92608646794818));
#37144=CARTESIAN_POINT('Ctrl Pts',(215.400869078538,0.41516803143658,4.9926631856718));
#37145=CARTESIAN_POINT('Ctrl Pts',(215.374472554852,1.24880732786508,4.85175539756075));
#37146=CARTESIAN_POINT('Ctrl Pts',(215.348076031166,1.99827998649403,4.52044839352363));
#37147=CARTESIAN_POINT('Ctrl Pts',(215.32167950748,2.74775264512299,4.18914138948651));
#37148=CARTESIAN_POINT('Ctrl Pts',(215.295282983794,3.4130586659524,3.66743516952332));
#37149=CARTESIAN_POINT('Ctrl Pts',(215.268886460108,3.91352865237769,3.01858742956897));
#37150=CARTESIAN_POINT('Ctrl Pts',(215.242489936422,4.41399863880298,2.36973968961461));
#37151=CARTESIAN_POINT('Ctrl Pts',(215.216093412737,4.74963259082415,1.59375042966909));
#37152=CARTESIAN_POINT('Ctrl Pts',(215.189696889051,4.87973436630227,0.784709562361485));
#37153=CARTESIAN_POINT('Ctrl Pts',(215.163300365365,5.00983614178038,-0.0243313049461004));
#37154=CARTESIAN_POINT('Ctrl Pts',(215.136903841679,4.93440574071546,-0.86642377961577));
#37155=CARTESIAN_POINT('Ctrl Pts',(215.110507317993,4.66258921732772,-1.63946283074435));
#37156=CARTESIAN_POINT('Ctrl Pts',(215.084110794307,4.39077269393997,-2.41250188187294));
#37157=CARTESIAN_POINT('Ctrl Pts',(215.057714270621,3.9225700482294,-3.11648750946044));
#37158=CARTESIAN_POINT('Ctrl Pts',(215.031317746936,3.31475158398952,-3.66606035402746));
#37159=CARTESIAN_POINT('Ctrl Pts',(215.00492122325,2.70693311974964,-4.21563319859447));
#37160=CARTESIAN_POINT('Ctrl Pts',(214.978524699564,1.95949883698045,-4.610793260141));
#37161=CARTESIAN_POINT('Ctrl Pts',(214.952128175878,1.16307631262376,-4.80362676255623));
#37162=CARTESIAN_POINT('Ctrl Pts',(214.925731652192,0.366653788267074,-4.99646026497147));
#37163=CARTESIAN_POINT('Ctrl Pts',(214.899335128506,-0.478756977677111,
-4.98696720825542));
#37164=CARTESIAN_POINT('Ctrl Pts',(214.872938604821,-1.27064860629358,-4.77629864039689));
#37165=CARTESIAN_POINT('Ctrl Pts',(214.846542081135,-2.06254023491004,-4.56563007253835));
#37166=CARTESIAN_POINT('Ctrl Pts',(214.820145557449,-2.80091272619879,-4.15378599353734));
#37167=CARTESIAN_POINT('Ctrl Pts',(214.793749033763,-3.39623725962183,-3.5907031427409));
#37168=CARTESIAN_POINT('Ctrl Pts',(214.767352510077,-3.99156179304486,-3.02762029194445));
#37169=CARTESIAN_POINT('Ctrl Pts',(214.740955986391,-4.44383836860219,-2.31329866935258));
#37170=CARTESIAN_POINT('Ctrl Pts',(214.714559462706,-4.69822774343964,-1.5343508900206));
#37171=CARTESIAN_POINT('Ctrl Pts',(214.697813126689,-4.85961603837852,-1.04017516419425));
#37172=CARTESIAN_POINT('Ctrl Pts',(214.681066790673,-4.94135835785724,-0.519988593426523));
#37173=CARTESIAN_POINT('Ctrl Pts',(214.664320454657,-4.94170537201422,9.14365381503302E-5));
#37174=CARTESIAN_POINT('Ctrl Pts',(214.519679545343,-4.9416771233585,8.15223711883949E-5));
#37175=CARTESIAN_POINT('Ctrl Pts',(214.535956926828,-4.94137868168151,-0.505442774410793));
#37176=CARTESIAN_POINT('Ctrl Pts',(214.552234308313,-4.8642238638634,-1.01105611421827));
#37177=CARTESIAN_POINT('Ctrl Pts',(214.568511689798,-4.71160704544237,-1.49276110631793));
#37178=CARTESIAN_POINT('Ctrl Pts',(214.594908213484,-4.46411309403417,-2.27392712157909));
#37179=CARTESIAN_POINT('Ctrl Pts',(214.62130473717,-4.01816841183361,-2.99221872274118));
#37180=CARTESIAN_POINT('Ctrl Pts',(214.647701260856,-3.42784448971234,-3.56054192863199));
#37181=CARTESIAN_POINT('Ctrl Pts',(214.674097784542,-2.83752056759108,-4.12886513452279));
#37182=CARTESIAN_POINT('Ctrl Pts',(214.700494308228,-2.10281740554911,-4.54721994514231));
#37183=CARTESIAN_POINT('Ctrl Pts',(214.726890831913,-1.31281891220868,-4.76488018474178));
#37184=CARTESIAN_POINT('Ctrl Pts',(214.753287355599,-0.52282041886825,-4.98254042434126));
#37185=CARTESIAN_POINT('Ctrl Pts',(214.779683879285,0.322473405770636,-4.99950609292068));
#37186=CARTESIAN_POINT('Ctrl Pts',(214.806080402971,1.12056936210911,-4.81372007660396));
#37187=CARTESIAN_POINT('Ctrl Pts',(214.832476926657,1.91866531844758,-4.62793406028724));
#37188=CARTESIAN_POINT('Ctrl Pts',(214.858873450343,2.66956340648564,-4.23939635907438));
#37189=CARTESIAN_POINT('Ctrl Pts',(214.885269974028,3.28221605746981,-3.69521777751799));
#37190=CARTESIAN_POINT('Ctrl Pts',(214.911666497714,3.89486870845398,-3.15103919596161));
#37191=CARTESIAN_POINT('Ctrl Pts',(214.9380630214,4.36927592238426,-2.45121973406169));
#37192=CARTESIAN_POINT('Ctrl Pts',(214.964459545086,4.64791508185686,-1.68061359718562));
#37193=CARTESIAN_POINT('Ctrl Pts',(214.990856068772,4.92655424132946,-0.910007460309548));
#37194=CARTESIAN_POINT('Ctrl Pts',(215.017252592458,5.00942534634437,-0.0686146484573258));
#37195=CARTESIAN_POINT('Ctrl Pts',(215.043649116144,4.88648014567853,0.741544642679851));
#37196=CARTESIAN_POINT('Ctrl Pts',(215.070045639829,4.7635349450127,1.55170393381702));
#37197=CARTESIAN_POINT('Ctrl Pts',(215.096442163515,4.43477343866612,2.33062970423914));
#37198=CARTESIAN_POINT('Ctrl Pts',(215.122838687201,3.94005847398043,2.98387598482455));
#37199=CARTESIAN_POINT('Ctrl Pts',(215.149235210887,3.44534350929474,3.63712226540996));
#37200=CARTESIAN_POINT('Ctrl Pts',(215.175631734573,2.78467508626995,4.16468905615867));
#37201=CARTESIAN_POINT('Ctrl Pts',(215.202028258259,2.03816028551635,4.50260805775292));
#37202=CARTESIAN_POINT('Ctrl Pts',(215.228424781945,1.29164548476275,4.84052705934719));
#37203=CARTESIAN_POINT('Ctrl Pts',(215.25482130563,0.459284306280347,4.98879827178699));
#37204=CARTESIAN_POINT('Ctrl Pts',(215.281217829316,-0.357998153925342,
4.92944357843598));
#37205=CARTESIAN_POINT('Ctrl Pts',(215.307614353002,-1.17528061413103,4.87008888508496));
#37206=CARTESIAN_POINT('Ctrl Pts',(215.334010876688,-1.97748435606,4.60310828594313));
#37207=CARTESIAN_POINT('Ctrl Pts',(215.360407400374,-2.66734092010225,4.16087359663157));
#37208=CARTESIAN_POINT('Ctrl Pts',(215.38680392406,-3.35719748414449,3.71863890732002));
#37209=CARTESIAN_POINT('Ctrl Pts',(215.413200447745,-3.9347068703,3.10115012783875));
#37210=CARTESIAN_POINT('Ctrl Pts',(215.439596971431,-4.32984516136964,2.38327873941794));
#37211=CARTESIAN_POINT('Ctrl Pts',(215.465993495117,-4.72498345243928,1.66540735099713));
#37212=CARTESIAN_POINT('Ctrl Pts',(215.492390018803,-4.93775064842305,0.847153353636784));
#37213=CARTESIAN_POINT('Ctrl Pts',(215.518786542489,-4.9423483937073,0.0277313255456686));
#37214=CARTESIAN_POINT('Ctrl Pts',(215.519084210107,-4.94240024143936,0.0184908889552883));
#37215=CARTESIAN_POINT('Ctrl Pts',(215.519381877725,-4.94242561717416,0.0092503038315561));
#37216=CARTESIAN_POINT('Ctrl Pts',(215.519679545343,-4.94242455630813,9.71285613910342E-6));
#37217=CARTESIAN_POINT('Origin',(215.7,0.,0.));
#37218=CARTESIAN_POINT('',(216.664320454657,-4.94168438867978,-8.42883428375796E-5));
#37219=CARTESIAN_POINT('',(216.519679545343,-4.94171357522401,-9.3938055576132E-5));
#37220=CARTESIAN_POINT('',(215.7,-4.942,-6.05220448138622E-16));
#37221=CARTESIAN_POINT('Ctrl Pts',(216.664320454657,-4.94168438867978,-8.42883428375796E-5));
#37222=CARTESIAN_POINT('Ctrl Pts',(216.647916692467,-4.94137282101751,0.509362846945846));
#37223=CARTESIAN_POINT('Ctrl Pts',(216.631512930277,-4.86299534936484,1.018903668412));
#37224=CARTESIAN_POINT('Ctrl Pts',(216.615109168087,-4.70803758557245,1.50398094262197));
#37225=CARTESIAN_POINT('Ctrl Pts',(216.588712644401,-4.45868342919959,2.28455515540122));
#37226=CARTESIAN_POINT('Ctrl Pts',(216.562316120715,-4.01102888604924,3.00178237971507));
#37227=CARTESIAN_POINT('Ctrl Pts',(216.535919597029,-3.41935277031013,3.56869769175051));
#37228=CARTESIAN_POINT('Ctrl Pts',(216.509523073343,-2.82767665457099,4.13561300378596));
#37229=CARTESIAN_POINT('Ctrl Pts',(216.483126549657,-2.09197896624308,4.55221640354299));
#37230=CARTESIAN_POINT('Ctrl Pts',(216.456730025972,-1.30146420181781,4.76799407658186));
#37231=CARTESIAN_POINT('Ctrl Pts',(216.430333502286,-0.510949437392535,
4.98377174962073));
#37232=CARTESIAN_POINT('Ctrl Pts',(216.4039369786,0.33438240313007,4.99872369594143));
#37233=CARTESIAN_POINT('Ctrl Pts',(216.377540454914,1.13203351066578,4.81103696864436));
#37234=CARTESIAN_POINT('Ctrl Pts',(216.351143931228,1.92968461820145,4.62335024134729));
#37235=CARTESIAN_POINT('Ctrl Pts',(216.324747407542,2.67965499275022,4.23302484043244));
#37236=CARTESIAN_POINT('Ctrl Pts',(216.298350883857,3.29100955227154,3.68738833184009));
#37237=CARTESIAN_POINT('Ctrl Pts',(216.271954360171,3.90236411179289,3.14175182324771));
#37238=CARTESIAN_POINT('Ctrl Pts',(216.245557836485,4.37510285628678,2.44080420697781));
#37239=CARTESIAN_POINT('Ctrl Pts',(216.219161312799,4.65190547288072,1.66953647888129));
#37240=CARTESIAN_POINT('Ctrl Pts',(216.192764789113,4.92870808947466,0.898268750784777));
#37241=CARTESIAN_POINT('Ctrl Pts',(216.166368265427,5.00957457816861,0.0566809108616259));
#37242=CARTESIAN_POINT('Ctrl Pts',(216.139971741741,4.8846997506068,-0.753183197737967));
#37243=CARTESIAN_POINT('Ctrl Pts',(216.113575218056,4.75982492304499,-1.56304730633755));
#37244=CARTESIAN_POINT('Ctrl Pts',(216.08717869437,4.42920877922744,-2.34118768361358));
#37245=CARTESIAN_POINT('Ctrl Pts',(216.060782170684,3.93293904419266,-2.993253590593));
#37246=CARTESIAN_POINT('Ctrl Pts',(216.034385646998,3.43666930915788,-3.64531949757242));
#37247=CARTESIAN_POINT('Ctrl Pts',(216.007989123312,2.77474598290587,-4.17131093425521));
#37248=CARTESIAN_POINT('Ctrl Pts',(215.981592599626,2.02742830502788,-4.50745061547042));
#37249=CARTESIAN_POINT('Ctrl Pts',(215.95519607594,1.2801106271499,-4.84359029668564));
#37250=CARTESIAN_POINT('Ctrl Pts',(215.928799552255,0.447398597645939,-4.98987822243327));
#37251=CARTESIAN_POINT('Ctrl Pts',(215.902403028569,-0.369740146242837,
-4.92857675269335));
#37252=CARTESIAN_POINT('Ctrl Pts',(215.876006504883,-1.18687889013161,-4.86727528295342));
#37253=CARTESIAN_POINT('Ctrl Pts',(215.849609981197,-1.98844434840521,-4.59838441772594));
#37254=CARTESIAN_POINT('Ctrl Pts',(215.823213457511,-2.6772454543461,-4.15450759538554));
#37255=CARTESIAN_POINT('Ctrl Pts',(215.796816933825,-3.36604656028698,-3.71063077304514));
#37256=CARTESIAN_POINT('Ctrl Pts',(215.770420410139,-3.94208331389515,-3.09176799359182));
#37257=CARTESIAN_POINT('Ctrl Pts',(215.744023886454,-4.33551035697334,-2.37295733790345));
#37258=CARTESIAN_POINT('Ctrl Pts',(215.717627362768,-4.72893740005153,-1.65414668221509));
#37259=CARTESIAN_POINT('Ctrl Pts',(215.691230839082,-4.93975473259975,-0.835388150291677));
#37260=CARTESIAN_POINT('Ctrl Pts',(215.664834315396,-4.94240042299853,-0.0159574959476391));
#37261=CARTESIAN_POINT('Ctrl Pts',(215.664663028483,-4.94241759087058,-0.0106402144408186));
#37262=CARTESIAN_POINT('Ctrl Pts',(215.66449174157,-4.94242599324733,-0.00532290463290051));
#37263=CARTESIAN_POINT('Ctrl Pts',(215.664320454657,-4.94242563693782,-5.5936937812251E-6));
#37264=CARTESIAN_POINT('Ctrl Pts',(215.519679545343,-4.94242455630813,9.71285613910342E-6));
#37265=CARTESIAN_POINT('Ctrl Pts',(215.545778401411,-4.94233154185726,-0.810185414792319));
#37266=CARTESIAN_POINT('Ctrl Pts',(215.571877257479,-4.73900967080375,-1.62042552671124));
#37267=CARTESIAN_POINT('Ctrl Pts',(215.597976113546,-4.3563166654476,-2.33454102160172));
#37268=CARTESIAN_POINT('Ctrl Pts',(215.624372637232,-3.96925889731891,-3.05680128183612));
#37269=CARTESIAN_POINT('Ctrl Pts',(215.650769160918,-3.3987150664768,-3.68073174348307));
#37270=CARTESIAN_POINT('Ctrl Pts',(215.677165684604,-2.71386450563363,-4.13067986126492));
#37271=CARTESIAN_POINT('Ctrl Pts',(215.70356220829,-2.02901394479045,-4.58062797904678));
#37272=CARTESIAN_POINT('Ctrl Pts',(215.729958731976,-1.22985665394621,-4.85659375296355));
#37273=CARTESIAN_POINT('Ctrl Pts',(215.756355255662,-0.413291705747491,
-4.92511590088579));
#37274=CARTESIAN_POINT('Ctrl Pts',(215.782751779347,0.40327324245123,-4.99363804880802));
#37275=CARTESIAN_POINT('Ctrl Pts',(215.809148303033,1.23724584800443,-4.85471657073573));
#37276=CARTESIAN_POINT('Ctrl Pts',(215.835544826719,1.98750562685147,-4.52519591337562));
#37277=CARTESIAN_POINT('Ctrl Pts',(215.861941350405,2.73776540569852,-4.1956752560155));
#37278=CARTESIAN_POINT('Ctrl Pts',(215.888337874091,3.4043123578394,-3.67555541936756));
#37279=CARTESIAN_POINT('Ctrl Pts',(215.914734397777,3.90632662180527,-3.02790174790614));
#37280=CARTESIAN_POINT('Ctrl Pts',(215.941130921462,4.40834088577113,-2.38024807644474));
#37281=CARTESIAN_POINT('Ctrl Pts',(215.967527445148,4.74582246156199,-1.60506057016986));
#37282=CARTESIAN_POINT('Ctrl Pts',(215.993923968834,4.87785117976427,-0.796331927822826));
#37283=CARTESIAN_POINT('Ctrl Pts',(216.02032049252,5.00987989796655,0.0123967145242333));
#37284=CARTESIAN_POINT('Ctrl Pts',(216.046717016206,4.93645575858024,0.854666492943454));
#37285=CARTESIAN_POINT('Ctrl Pts',(216.073113539892,4.66648155345611,1.62835087817444));
#37286=CARTESIAN_POINT('Ctrl Pts',(216.099510063578,4.39650734833198,2.40203526340543));
#37287=CARTESIAN_POINT('Ctrl Pts',(216.125906587263,3.92998307747003,3.10713425544818));
#37288=CARTESIAN_POINT('Ctrl Pts',(216.152303110949,3.32347553908577,3.65815349764006));
#37289=CARTESIAN_POINT('Ctrl Pts',(216.178699634635,2.71696800070151,4.20917273983195));
#37290=CARTESIAN_POINT('Ctrl Pts',(216.205096158321,1.97047719479494,4.60611223217296));
#37291=CARTESIAN_POINT('Ctrl Pts',(216.231492682007,1.1745163002612,4.80084243978267));
#37292=CARTESIAN_POINT('Ctrl Pts',(216.257889205693,0.378555405727472,4.99557264739237));
#37293=CARTESIAN_POINT('Ctrl Pts',(216.284285729378,-0.46687557743342,4.98809357027076));
#37294=CARTESIAN_POINT('Ctrl Pts',(216.310682253064,-1.25926681893708,4.77931205822781));
#37295=CARTESIAN_POINT('Ctrl Pts',(216.33707877675,-2.05165806044073,4.57053054618486));
#37296=CARTESIAN_POINT('Ctrl Pts',(216.363475300436,-2.79100956028715,4.16044659922057));
#37297=CARTESIAN_POINT('Ctrl Pts',(216.389871824122,-3.38767379161803,3.59878353791694));
#37298=CARTESIAN_POINT('Ctrl Pts',(216.416268347808,-3.98433802294891,3.03712047661331));
#37299=CARTESIAN_POINT('Ctrl Pts',(216.442664871494,-4.43831498576424,2.32387830097037));
#37300=CARTESIAN_POINT('Ctrl Pts',(216.469061395179,-4.69455926259279,1.54553874141088));
#37301=CARTESIAN_POINT('Ctrl Pts',(216.485934111901,-4.85835117496055,1.04802236169082));
#37302=CARTESIAN_POINT('Ctrl Pts',(216.502806828622,-4.9413535679609,0.523908526256979));
#37303=CARTESIAN_POINT('Ctrl Pts',(216.519679545343,-4.94171357522401,-9.3938055576132E-5));
#37304=CARTESIAN_POINT('Origin',(215.7,0.,0.));
#37305=CARTESIAN_POINT('',(217.664320454657,-4.94195837962584,0.000126603499120692));
#37306=CARTESIAN_POINT('',(217.519679545343,-4.94191411506509,0.000125076744195484));
#37307=CARTESIAN_POINT('',(215.7,-4.942,-6.05220448138622E-16));
#37308=CARTESIAN_POINT('Ctrl Pts',(217.664320454657,-4.94195837962584,0.000126603499120692));
#37309=CARTESIAN_POINT('Ctrl Pts',(217.65773816705,-4.94216297129183,0.204518376639697));
#37310=CARTESIAN_POINT('Ctrl Pts',(217.651155879442,-4.92972032171904,0.408885406966804));
#37311=CARTESIAN_POINT('Ctrl Pts',(217.644573591835,-4.90443271504819,0.611650493744549));
#37312=CARTESIAN_POINT('Ctrl Pts',(217.618177068149,-4.80302345610052,1.4247862506487));
#37313=CARTESIAN_POINT('Ctrl Pts',(217.591780544463,-4.4950417374727,2.21215956889818));
#37314=CARTESIAN_POINT('Ctrl Pts',(217.565384020777,-4.01783082471338,2.87830020097209));
#37315=CARTESIAN_POINT('Ctrl Pts',(217.538987497091,-3.54061991195407,3.54444083304598));
#37316=CARTESIAN_POINT('Ctrl Pts',(217.512590973406,-2.89417980506328,4.08934877894429));
#37317=CARTESIAN_POINT('Ctrl Pts',(217.48619444972,-2.15689237904473,4.44695309713873));
#37318=CARTESIAN_POINT('Ctrl Pts',(217.459797926034,-1.41960495302616,4.80455741533317));
#37319=CARTESIAN_POINT('Ctrl Pts',(217.433401402348,-0.59147020787982,4.97485810582372));
#37320=CARTESIAN_POINT('Ctrl Pts',(217.407004878662,0.227099222047519,4.9372059432718));
#37321=CARTESIAN_POINT('Ctrl Pts',(217.380608354976,1.04566865197486,4.89955378071988));
#37322=CARTESIAN_POINT('Ctrl Pts',(217.35421183129,1.8546727666832,4.65394876512549));
#37323=CARTESIAN_POINT('Ctrl Pts',(217.327815307605,2.55601855071661,4.23017088913977));
#37324=CARTESIAN_POINT('Ctrl Pts',(217.301418783919,3.25736433475001,3.80639301315405));
#37325=CARTESIAN_POINT('Ctrl Pts',(217.275022260233,3.85105178810847,3.20444227677701));
#37326=CARTESIAN_POINT('Ctrl Pts',(217.248625736547,4.26509537761672,2.49730614918664));
#37327=CARTESIAN_POINT('Ctrl Pts',(217.222229212861,4.67913896712499,1.79017002159624));
#37328=CARTESIAN_POINT('Ctrl Pts',(217.195832689175,4.91353869278302,0.977848502792508));
#37329=CARTESIAN_POINT('Ctrl Pts',(217.16943616549,4.93987322088706,0.158836848671542));
#37330=CARTESIAN_POINT('Ctrl Pts',(217.143039641804,4.96620774899109,-0.660174805449401));
#37331=CARTESIAN_POINT('Ctrl Pts',(217.116643118118,4.78447707954115,-1.48587659488757));
#37332=CARTESIAN_POINT('Ctrl Pts',(217.090246594432,4.41671634071899,-2.21815088498478));
#37333=CARTESIAN_POINT('Ctrl Pts',(217.063850070746,4.04895560189684,-2.95042517508198));
#37334=CARTESIAN_POINT('Ctrl Pts',(217.03745354706,3.49516479370246,-3.58927196583822));
#37335=CARTESIAN_POINT('Ctrl Pts',(217.011057023374,2.82249191862427,-4.0572300837189));
#37336=CARTESIAN_POINT('Ctrl Pts',(216.984660499689,2.14981904354606,-4.52518820159958));
#37337=CARTESIAN_POINT('Ctrl Pts',(216.958263976003,1.35826410158404,-4.82225764660469));
#37338=CARTESIAN_POINT('Ctrl Pts',(216.931867452317,0.543804368680852,-4.9124182834462));
#37339=CARTESIAN_POINT('Ctrl Pts',(216.905470928631,-0.27065536422234,-5.00257892028772));
#37340=CARTESIAN_POINT('Ctrl Pts',(216.879074404945,-1.1080198880667,-4.88583074896562));
#37341=CARTESIAN_POINT('Ctrl Pts',(216.852677881259,-1.86675744338853,-4.57632966802944));
#37342=CARTESIAN_POINT('Ctrl Pts',(216.826281357573,-2.62549499871034,-4.26682858709326));
#37343=CARTESIAN_POINT('Ctrl Pts',(216.799884833888,-3.30560558550962,-3.764574596543));
#37344=CARTESIAN_POINT('Ctrl Pts',(216.773488310202,-3.82462473038045,-3.13046677904354));
#37345=CARTESIAN_POINT('Ctrl Pts',(216.747091786516,-4.34364387525129,-2.49635896154405));
#37346=CARTESIAN_POINT('Ctrl Pts',(216.72069526283,-4.70157157819368,-1.73039731709535));
#37347=CARTESIAN_POINT('Ctrl Pts',(216.694298739144,-4.85500854486718,-0.925455894248657));
#37348=CARTESIAN_POINT('Ctrl Pts',(216.684305977649,-4.91309418640272,-0.620734418334266));
#37349=CARTESIAN_POINT('Ctrl Pts',(216.674313216153,-4.94187418790405,-0.310426736535013));
#37350=CARTESIAN_POINT('Ctrl Pts',(216.664320454657,-4.94168438867978,-8.42883428375796E-5));
#37351=CARTESIAN_POINT('Ctrl Pts',(216.519679545343,-4.94171357522401,-9.3938055576132E-5));
#37352=CARTESIAN_POINT('Ctrl Pts',(216.529203352308,-4.94191678136659,-0.29586719150049));
#37353=CARTESIAN_POINT('Ctrl Pts',(216.538727159272,-4.91578979804439,-0.591604961667699));
#37354=CARTESIAN_POINT('Ctrl Pts',(216.548250966237,-4.86299941312486,-0.882504039166336));
#37355=CARTESIAN_POINT('Ctrl Pts',(216.574647489923,-4.71668369598663,-1.68877031670807));
#37356=CARTESIAN_POINT('Ctrl Pts',(216.601044013609,-4.3655406708684,-2.45786592831551));
#37357=CARTESIAN_POINT('Ctrl Pts',(216.627440537295,-3.85214697930256,-3.09653682701301));
#37358=CARTESIAN_POINT('Ctrl Pts',(216.65383706098,-3.33875328773674,-3.7352077257105));
#37359=CARTESIAN_POINT('Ctrl Pts',(216.680233584666,-2.66310892972333,-4.24345391149806));
#37360=CARTESIAN_POINT('Ctrl Pts',(216.706630108352,-1.90713684143578,-4.55964973865713));
#37361=CARTESIAN_POINT('Ctrl Pts',(216.733026632038,-1.15116475314824,-4.87584556581619));
#37362=CARTESIAN_POINT('Ctrl Pts',(216.759423155724,-0.314864934586568,
-4.99999103434677));
#37363=CARTESIAN_POINT('Ctrl Pts',(216.78581967941,0.500359951967919,-4.91703331183187));
#37364=CARTESIAN_POINT('Ctrl Pts',(216.812216203095,1.31558483852242,-4.83407558931698));
#37365=CARTESIAN_POINT('Ctrl Pts',(216.838612726781,2.10973479306973,-4.5440146757566));
#37366=CARTESIAN_POINT('Ctrl Pts',(216.865009250467,2.78651789032859,-4.0820209110288));
#37367=CARTESIAN_POINT('Ctrl Pts',(216.891405774153,3.46330098758745,-3.620027146301));
#37368=CARTESIAN_POINT('Ctrl Pts',(216.917802297839,4.02271722755784,-2.98610053040578));
#37369=CARTESIAN_POINT('Ctrl Pts',(216.944198821525,4.39693651534156,-2.25710565797298));
#37370=CARTESIAN_POINT('Ctrl Pts',(216.970595345211,4.77115580312528,-1.52811078554019));
#37371=CARTESIAN_POINT('Ctrl Pts',(216.996991868896,4.96017813872232,-0.704047656569832));
#37372=CARTESIAN_POINT('Ctrl Pts',(217.023388392582,4.94108426801502,0.115164784427049));
#37373=CARTESIAN_POINT('Ctrl Pts',(217.049784916268,4.92199039730772,0.93437722542393));
#37374=CARTESIAN_POINT('Ctrl Pts',(217.076181439954,4.69478032029607,1.74873897844733));
#37375=CARTESIAN_POINT('Ctrl Pts',(217.10257796364,4.28700361452962,2.45950740600789));
#37376=CARTESIAN_POINT('Ctrl Pts',(217.128974487326,3.87922690876317,3.17027583356844));
#37377=CARTESIAN_POINT('Ctrl Pts',(217.155371011012,3.29088357424191,3.77745093566615));
#37378=CARTESIAN_POINT('Ctrl Pts',(217.181767534697,2.59331116136556,4.20741178060033));
#37379=CARTESIAN_POINT('Ctrl Pts',(217.208164058383,1.89573874848922,4.63737262553451));
#37380=CARTESIAN_POINT('Ctrl Pts',(217.234560582069,1.08893725725779,4.89011921330515));
#37381=CARTESIAN_POINT('Ctrl Pts',(217.260957105755,0.27073263158228,4.93500562445416));
#37382=CARTESIAN_POINT('Ctrl Pts',(217.287353629441,-0.54747199409324,4.97989203560317));
#37383=CARTESIAN_POINT('Ctrl Pts',(217.313750153127,-1.37707975421284,4.81691827013054));
#37384=CARTESIAN_POINT('Ctrl Pts',(217.340146676812,-2.11749940905815,4.46584515224566));
#37385=CARTESIAN_POINT('Ctrl Pts',(217.366543200498,-2.85791906390345,4.11477203436078));
#37386=CARTESIAN_POINT('Ctrl Pts',(217.392939724184,-3.50915061347447,3.57559956406364));
#37387=CARTESIAN_POINT('Ctrl Pts',(217.41933624787,-3.99223121284117,2.91370324748667));
#37388=CARTESIAN_POINT('Ctrl Pts',(217.445732771556,-4.47531181220787,2.25180693090971));
#37389=CARTESIAN_POINT('Ctrl Pts',(217.472129295242,-4.79024146137026,1.46718676805292));
#37390=CARTESIAN_POINT('Ctrl Pts',(217.498525818928,-4.89883444732496,0.654979182035602));
#37391=CARTESIAN_POINT('Ctrl Pts',(217.505577061066,-4.92784263975307,0.438016053711726));
#37392=CARTESIAN_POINT('Ctrl Pts',(217.512628303205,-4.94212722614308,0.219084364183518));
#37393=CARTESIAN_POINT('Ctrl Pts',(217.519679545343,-4.94191411506509,0.000125076744195484));
#37394=CARTESIAN_POINT('Origin',(215.7,0.,0.));
#37395=CARTESIAN_POINT('',(218.664320454657,-4.94227242746027,-9.27502432238048E-5));
#37396=CARTESIAN_POINT('',(218.519679545343,-4.94230926220351,-8.20892703918941E-5));
#37397=CARTESIAN_POINT('',(215.7,-4.942,-6.05220448138622E-16));
#37398=CARTESIAN_POINT('Ctrl Pts',(218.664320454657,-4.94227242746027,-9.27502432238048E-5));
#37399=CARTESIAN_POINT('Ctrl Pts',(218.641163117946,-4.94165288350105,0.718852082944881));
#37400=CARTESIAN_POINT('Ctrl Pts',(218.618005781236,-4.78292211280577,1.43806153059028));
#37401=CARTESIAN_POINT('Ctrl Pts',(218.594848444525,-4.47899749627878,2.08953535774377));
#37402=CARTESIAN_POINT('Ctrl Pts',(218.568451920839,-4.13256070870011,2.83213561977484));
#37403=CARTESIAN_POINT('Ctrl Pts',(218.542055397154,-3.5974705980024,3.48672560956518));
#37404=CARTESIAN_POINT('Ctrl Pts',(218.515658873468,-2.93860767782546,3.9739352660503));
#37405=CARTESIAN_POINT('Ctrl Pts',(218.489262349782,-2.27974475764855,4.46114492253539));
#37406=CARTESIAN_POINT('Ctrl Pts',(218.462865826096,-1.49710902799241,4.7809742457153));
#37407=CARTESIAN_POINT('Ctrl Pts',(218.43646930241,-0.685596296344016,4.89464342944124));
#37408=CARTESIAN_POINT('Ctrl Pts',(218.410072778725,0.125916435304404,5.00831261316719));
#37409=CARTESIAN_POINT('Ctrl Pts',(218.383676255039,0.966306168945093,4.91582165743917));
#37410=CARTESIAN_POINT('Ctrl Pts',(218.357279731353,1.73367433369038,4.6283852354397));
#37411=CARTESIAN_POINT('Ctrl Pts',(218.330883207667,2.50104249843566,4.34094881344022));
#37412=CARTESIAN_POINT('Ctrl Pts',(218.304486683981,3.19538909428554,3.85856692516929));
#37413=CARTESIAN_POINT('Ctrl Pts',(218.278090160295,3.73252350944933,3.23972912977937));
#37414=CARTESIAN_POINT('Ctrl Pts',(218.251693636609,4.26965792461312,2.62089133438945));
#37415=CARTESIAN_POINT('Ctrl Pts',(218.225297112923,4.64958015909082,1.86559763188054));
#37416=CARTESIAN_POINT('Ctrl Pts',(218.198900589238,4.82622404715952,1.06542856614232));
#37417=CARTESIAN_POINT('Ctrl Pts',(218.172504065552,5.00286793522823,0.265259500404091));
#37418=CARTESIAN_POINT('Ctrl Pts',(218.146107541866,4.97623347688792,-0.579784928563423));
#37419=CARTESIAN_POINT('Ctrl Pts',(218.11971101818,4.74955014191032,-1.36724176077701));
#37420=CARTESIAN_POINT('Ctrl Pts',(218.093314494494,4.52286680693272,-2.15469859299058));
#37421=CARTESIAN_POINT('Ctrl Pts',(218.066917970808,4.09613459531782,-2.8845678284502));
#37422=CARTESIAN_POINT('Ctrl Pts',(218.040521447123,3.52109545580043,-3.46835167969953));
#37423=CARTESIAN_POINT('Ctrl Pts',(218.014124923437,2.94605631628303,-4.05213553094886));
#37424=CARTESIAN_POINT('Ctrl Pts',(217.987728399751,2.22271024886315,-4.48983399798791));
#37425=CARTESIAN_POINT('Ctrl Pts',(217.961331876065,1.43876409665984,-4.72837545644332));
#37426=CARTESIAN_POINT('Ctrl Pts',(217.934935352379,0.654817944456556,-4.96691691489872));
#37427=CARTESIAN_POINT('Ctrl Pts',(217.908538828693,-0.189728292530149,
-5.00630136477049));
#37428=CARTESIAN_POINT('Ctrl Pts',(217.882142305007,-0.99247206087463,-4.84175337985282));
#37429=CARTESIAN_POINT('Ctrl Pts',(217.855745781322,-1.79521582921913,-4.67720539493514));
#37430=CARTESIAN_POINT('Ctrl Pts',(217.829349257636,-2.55615712892142,-4.308724975228));
#37431=CARTESIAN_POINT('Ctrl Pts',(217.80295273395,-3.18303063609043,-3.7809909485005));
#37432=CARTESIAN_POINT('Ctrl Pts',(217.776556210264,-3.80990414325944,-3.253256921773));
#37433=CARTESIAN_POINT('Ctrl Pts',(217.750159686578,-4.30270985789518,-2.56626928802512));
#37434=CARTESIAN_POINT('Ctrl Pts',(217.723763162892,-4.60169431557929,-1.80332637337177));
#37435=CARTESIAN_POINT('Ctrl Pts',(217.703948926814,-4.82612343733975,-1.23063236240104));
#37436=CARTESIAN_POINT('Ctrl Pts',(217.684134690735,-4.94134251052207,-0.615140775726203));
#37437=CARTESIAN_POINT('Ctrl Pts',(217.664320454657,-4.94195837962584,0.000126603499120692));
#37438=CARTESIAN_POINT('Ctrl Pts',(217.519679545343,-4.94191411506509,0.000125076744195484));
#37439=CARTESIAN_POINT('Ctrl Pts',(217.53902482689,-4.94132943881606,-0.600595899744503));
#37440=CARTESIAN_POINT('Ctrl Pts',(217.558370108438,-4.83162136351427,-1.20152460424478));
#37441=CARTESIAN_POINT('Ctrl Pts',(217.577715389985,-4.61745498945683,-1.76257938588247));
#37442=CARTESIAN_POINT('Ctrl Pts',(217.604111913671,-4.32522622288702,-2.5281353586054));
#37443=CARTESIAN_POINT('Ctrl Pts',(217.630508437357,-3.83851236700038,-3.21945229487338));
#37444=CARTESIAN_POINT('Ctrl Pts',(217.656904961043,-3.21632823880477,-3.75270693386316));
#37445=CARTESIAN_POINT('Ctrl Pts',(217.683301484729,-2.59414411060916,-4.28596157285295));
#37446=CARTESIAN_POINT('Ctrl Pts',(217.709698008414,-1.83648971010458,-4.66115391456454));
#37447=CARTESIAN_POINT('Ctrl Pts',(217.7360945321,-1.0352318195085,-4.83279130017786));
#37448=CARTESIAN_POINT('Ctrl Pts',(217.762491055786,-0.233973928912422,
-5.00442868579118));
#37449=CARTESIAN_POINT('Ctrl Pts',(217.788887579472,0.610887451775157,-4.97251111530622));
#37450=CARTESIAN_POINT('Ctrl Pts',(217.815284103158,1.39691155746148,-4.7409086441133));
#37451=CARTESIAN_POINT('Ctrl Pts',(217.841680626844,2.1829356631478,-4.50930617292037));
#37452=CARTESIAN_POINT('Ctrl Pts',(217.868077150529,2.91012249383287,-4.07801880101947));
#37453=CARTESIAN_POINT('Ctrl Pts',(217.894473674215,3.49029950783875,-3.49934079746146));
#37454=CARTESIAN_POINT('Ctrl Pts',(217.920870197901,4.07047652184462,-2.92066279390347));
#37455=CARTESIAN_POINT('Ctrl Pts',(217.947266721587,4.50364371917131,-2.19459415868837));
#37456=CARTESIAN_POINT('Ctrl Pts',(217.973663245273,4.73727889899207,-1.40917185054278));
#37457=CARTESIAN_POINT('Ctrl Pts',(218.000059768959,4.97091407881283,-0.623749542397181));
#37458=CARTESIAN_POINT('Ctrl Pts',(218.026456292645,5.00501724112767,0.221026438678921));
#37459=CARTESIAN_POINT('Ctrl Pts',(218.05285281633,4.83545332411523,1.02272568242937));
#37460=CARTESIAN_POINT('Ctrl Pts',(218.079249340016,4.66588940710279,1.82442492617982));
#37461=CARTESIAN_POINT('Ctrl Pts',(218.105645863702,4.29265841076308,2.58304743260462));
#37462=CARTESIAN_POINT('Ctrl Pts',(218.132042387388,3.7610151777192,3.20660903512783));
#37463=CARTESIAN_POINT('Ctrl Pts',(218.158438911074,3.22937194467533,3.83017063765104));
#37464=CARTESIAN_POINT('Ctrl Pts',(218.18483543476,2.5393164749273,4.31867133627266));
#37465=CARTESIAN_POINT('Ctrl Pts',(218.211231958445,1.77451907450792,4.61287965650582));
#37466=CARTESIAN_POINT('Ctrl Pts',(218.237628482131,1.00972167408854,4.90708797673897));
#37467=CARTESIAN_POINT('Ctrl Pts',(218.264025005817,0.170182342997809,5.00700391858366));
#37468=CARTESIAN_POINT('Ctrl Pts',(218.290421529503,-0.642303460517146,
4.90051251766643));
#37469=CARTESIAN_POINT('Ctrl Pts',(218.316818053189,-1.45478926403208,4.7940211167492));
#37470=CARTESIAN_POINT('Ctrl Pts',(218.343214576875,-2.24022153997123,4.48112237307008));
#37471=CARTESIAN_POINT('Ctrl Pts',(218.369611100561,-2.90336539523267,3.99975574916308));
#37472=CARTESIAN_POINT('Ctrl Pts',(218.396007624246,-3.56650925049412,3.51838912525607));
#37473=CARTESIAN_POINT('Ctrl Pts',(218.422404147932,-4.10736468507784,2.86855462112118));
#37474=CARTESIAN_POINT('Ctrl Pts',(218.448800671618,-4.46035213079688,2.12904568774214));
#37475=CARTESIAN_POINT('Ctrl Pts',(218.47242696286,-4.77629465021573,1.46714589958227));
#37476=CARTESIAN_POINT('Ctrl Pts',(218.496053254102,-4.94173234535399,0.733406122622747));
#37477=CARTESIAN_POINT('Ctrl Pts',(218.519679545343,-4.94230926220351,-8.20892703918941E-5));
#37478=CARTESIAN_POINT('Origin',(215.7,0.,0.));
#37479=CARTESIAN_POINT('',(219.664320454657,-4.94158767198665,-3.94523114399803E-6));
#37480=CARTESIAN_POINT('',(219.519679545343,-4.94159107100858,-1.73410261375781E-5));
#37481=CARTESIAN_POINT('',(215.7,-4.942,-6.05220448138622E-16));
#37482=CARTESIAN_POINT('Ctrl Pts',(219.664320454657,-4.94158767198665,-3.94523114399803E-6));
#37483=CARTESIAN_POINT('Ctrl Pts',(219.650984592529,-4.94157610618106,0.41418746593572));
#37484=CARTESIAN_POINT('Ctrl Pts',(219.637648730401,-4.8900661808863,0.828381702435691));
#37485=CARTESIAN_POINT('Ctrl Pts',(219.624312868274,-4.78709218279223,1.22935959604286));
#37486=CARTESIAN_POINT('Ctrl Pts',(219.597916344588,-4.58326917130133,2.02304075176169));
#37487=CARTESIAN_POINT('Ctrl Pts',(219.571519820902,-4.17781602960576,2.76494184435379));
#37488=CARTESIAN_POINT('Ctrl Pts',(219.545123297216,-3.61989458589892,3.3651062048489));
#37489=CARTESIAN_POINT('Ctrl Pts',(219.51872677353,-3.06197314219209,3.965270565344));
#37490=CARTESIAN_POINT('Ctrl Pts',(219.492330249844,-2.351583396474,4.4236981937421));
#37491=CARTESIAN_POINT('Ctrl Pts',(219.465933726158,-1.5748612175734,4.68480402240224));
#37492=CARTESIAN_POINT('Ctrl Pts',(219.439537202473,-0.798139038672788,
4.94590985106238));
#37493=CARTESIAN_POINT('Ctrl Pts',(219.413140678787,0.0449155734103233,
5.00969387998454));
#37494=CARTESIAN_POINT('Ctrl Pts',(219.386744155101,0.852080927105088,4.86842219580397));
#37495=CARTESIAN_POINT('Ctrl Pts',(219.360347631415,1.65924628079983,4.72715051162339));
#37496=CARTESIAN_POINT('Ctrl Pts',(219.333951107729,2.43052237610621,4.38082311434008));
#37497=CARTESIAN_POINT('Ctrl Pts',(219.307554584043,3.07239077898644,3.87143274307227));
#37498=CARTESIAN_POINT('Ctrl Pts',(219.281158060357,3.7142591818667,3.36204237180443));
#37499=CARTESIAN_POINT('Ctrl Pts',(219.254761536672,4.22671989232077,2.68958902655207));
#37500=CARTESIAN_POINT('Ctrl Pts',(219.228365012986,4.54763624691617,1.93560872819564));
#37501=CARTESIAN_POINT('Ctrl Pts',(219.2019684893,4.86855260151157,1.18162842983922));
#37502=CARTESIAN_POINT('Ctrl Pts',(219.175571965614,4.9979246002483,0.346121178378721));
#37503=CARTESIAN_POINT('Ctrl Pts',(219.149175441928,4.9200656857394,-0.469606463906328));
#37504=CARTESIAN_POINT('Ctrl Pts',(219.122778918242,4.84220677123051,-1.28533410619134));
#37505=CARTESIAN_POINT('Ctrl Pts',(219.096382394557,4.55711694347603,-2.08128213930093));
#37506=CARTESIAN_POINT('Ctrl Pts',(219.069985870871,4.09936379041748,-2.76094061811314));
#37507=CARTESIAN_POINT('Ctrl Pts',(219.043589347185,3.64161063735894,-3.44059909692535));
#37508=CARTESIAN_POINT('Ctrl Pts',(219.017192823499,3.01119415899634,-4.00396802144018));
#37509=CARTESIAN_POINT('Ctrl Pts',(218.990796299813,2.28455334028836,-4.38273802757024));
#37510=CARTESIAN_POINT('Ctrl Pts',(218.964399776127,1.55791252158036,-4.7615080337003));
#37511=CARTESIAN_POINT('Ctrl Pts',(218.938003252441,0.735047362526965,-4.95567912144557));
#37512=CARTESIAN_POINT('Ctrl Pts',(218.911606728756,-0.0842684480886987,
-4.9417077424297));
#37513=CARTESIAN_POINT('Ctrl Pts',(218.88521020507,-0.903584258704351,-4.92773636341384));
#37514=CARTESIAN_POINT('Ctrl Pts',(218.858813681384,-1.7193507208823,-4.70562251763684));
#37515=CARTESIAN_POINT('Ctrl Pts',(218.832417157698,-2.43265487394899,-4.30229785663257));
#37516=CARTESIAN_POINT('Ctrl Pts',(218.806020634012,-3.1459590270157,-3.89897319562828));
#37517=CARTESIAN_POINT('Ctrl Pts',(218.779624110326,-3.75680087097117,-3.31443771939671));
#37518=CARTESIAN_POINT('Ctrl Pts',(218.753227586641,-4.19111487592392,-2.61956726955851));
#37519=CARTESIAN_POINT('Ctrl Pts',(218.726831062955,-4.62542888087664,-1.92469681972034));
#37520=CARTESIAN_POINT('Ctrl Pts',(218.700434539269,-4.88321504682666,-1.11949139627556));
#37521=CARTESIAN_POINT('Ctrl Pts',(218.674038015583,-4.93321639757186,-0.301583417417288));
#37522=CARTESIAN_POINT('Ctrl Pts',(218.670798828608,-4.93935219507348,-0.201215774174882));
#37523=CARTESIAN_POINT('Ctrl Pts',(218.667559641632,-4.94235908762972,-0.100656850889163));
#37524=CARTESIAN_POINT('Ctrl Pts',(218.664320454657,-4.94227242746027,-9.27502432238048E-5));
#37525=CARTESIAN_POINT('Ctrl Pts',(218.519679545343,-4.94230926220351,-8.20892703918941E-5));
#37526=CARTESIAN_POINT('Ctrl Pts',(218.522449777787,-4.94237690692006,-0.0860851280561018));
#37527=CARTESIAN_POINT('Ctrl Pts',(218.525220010232,-4.94017803630086,-0.172084708311003));
#37528=CARTESIAN_POINT('Ctrl Pts',(218.527990242676,-4.93568950871128,-0.257964619269936));
#37529=CARTESIAN_POINT('Ctrl Pts',(218.554386766362,-4.8929199840523,-1.07628263027977));
#37530=CARTESIAN_POINT('Ctrl Pts',(218.580783290047,-4.64226147788,-1.88373528967626));
#37531=CARTESIAN_POINT('Ctrl Pts',(218.607179813733,-4.21410672648965,-2.58241769838892));
#37532=CARTESIAN_POINT('Ctrl Pts',(218.633576337419,-3.7859519750993,-3.28110010710158));
#37533=CARTESIAN_POINT('Ctrl Pts',(218.659972861105,-3.1803009784909,-3.87101226513042));
#37534=CARTESIAN_POINT('Ctrl Pts',(218.686369384791,-2.4705898681885,-4.28062639976932));
#37535=CARTESIAN_POINT('Ctrl Pts',(218.712765908477,-1.76087875788611,-4.69024053440821));
#37536=CARTESIAN_POINT('Ctrl Pts',(218.739162432163,-0.947107533889707,
-4.91955664565717));
#37537=CARTESIAN_POINT('Ctrl Pts',(218.765558955848,-0.127947231119626,
-4.94076979601827));
#37538=CARTESIAN_POINT('Ctrl Pts',(218.791955479534,0.691213071650503,-4.96198294637938));
#37539=CARTESIAN_POINT('Ctrl Pts',(218.81835200322,1.51576245319432,-4.77509313585261));
#37540=CARTESIAN_POINT('Ctrl Pts',(218.844748526906,2.24572301011498,-4.40276104655224));
#37541=CARTESIAN_POINT('Ctrl Pts',(218.871145050592,2.97568356703559,-4.03042895725189));
#37542=CARTESIAN_POINT('Ctrl Pts',(218.897541574278,3.61105529933306,-3.47265458917798));
#37543=CARTESIAN_POINT('Ctrl Pts',(218.923938097963,4.07479838975134,-2.79706895769081));
#37544=CARTESIAN_POINT('Ctrl Pts',(218.950334621649,4.53854148016963,-2.12148332620362));
#37545=CARTESIAN_POINT('Ctrl Pts',(218.976731145335,4.83065592870871,-1.32808643130321));
#37546=CARTESIAN_POINT('Ctrl Pts',(219.003127669021,4.91572240115944,-0.513078888609636));
#37547=CARTESIAN_POINT('Ctrl Pts',(219.029524192707,5.00078887361018,0.301928654083976));
#37548=CARTESIAN_POINT('Ctrl Pts',(219.055920716393,4.87880736997254,1.13854684457073));
#37549=CARTESIAN_POINT('Ctrl Pts',(219.082317240079,4.56456833853241,1.89533441747495));
#37550=CARTESIAN_POINT('Ctrl Pts',(219.108713763764,4.25032930709229,2.65212199037915));
#37551=CARTESIAN_POINT('Ctrl Pts',(219.13511028745,3.74383274784969,3.32907894570083));
#37552=CARTESIAN_POINT('Ctrl Pts',(219.161506811136,3.10649216156546,3.84412319278793));
#37553=CARTESIAN_POINT('Ctrl Pts',(219.187903334822,2.46915157528122,4.35916743987503));
#37554=CARTESIAN_POINT('Ctrl Pts',(219.214299858508,1.70096696195534,4.71229897872756));
#37555=CARTESIAN_POINT('Ctrl Pts',(219.240696382194,0.895081908595595,4.86070005740969));
#37556=CARTESIAN_POINT('Ctrl Pts',(219.26709290588,0.0891968552358766,5.00910113609182));
#37557=CARTESIAN_POINT('Ctrl Pts',(219.293489429565,-0.754388638157707,
4.95277175460356));
#37558=CARTESIAN_POINT('Ctrl Pts',(219.319885953251,-1.53338850982428,4.69854193863762));
#37559=CARTESIAN_POINT('Ctrl Pts',(219.346282476937,-2.31238838149088,4.44431212267166));
#37560=CARTESIAN_POINT('Ctrl Pts',(219.372679000623,-3.02680263143046,3.99218187222801));
#37561=CARTESIAN_POINT('Ctrl Pts',(219.399075524309,-3.59000741337678,3.39697268801169));
#37562=CARTESIAN_POINT('Ctrl Pts',(219.425472047995,-4.1532121953231,2.80176350379538));
#37563=CARTESIAN_POINT('Ctrl Pts',(219.45186857168,-4.56520750927616,2.0634753858064));
#37564=CARTESIAN_POINT('Ctrl Pts',(219.478265095366,-4.7760382784142,1.27162692418807));
#37565=CARTESIAN_POINT('Ctrl Pts',(219.492069912025,-4.88629825615422,0.857507134612465));
#37566=CARTESIAN_POINT('Ctrl Pts',(219.505874728684,-4.94153840270628,0.428738237424155));
#37567=CARTESIAN_POINT('Ctrl Pts',(219.519679545343,-4.94159107100858,-1.73410261375781E-5));
#37568=CARTESIAN_POINT('Origin',(215.7,0.,0.));
#37569=CARTESIAN_POINT('',(220.664320454657,-4.94224935728931,9.83974689322542E-5));
#37570=CARTESIAN_POINT('',(220.519679545343,-4.94220801981422,0.000106916500303121));
#37571=CARTESIAN_POINT('',(215.7,-4.942,-6.05220448138622E-16));
#37572=CARTESIAN_POINT('Ctrl Pts',(220.664320454657,-4.94224935728931,9.83974689322542E-5));
#37573=CARTESIAN_POINT('Ctrl Pts',(220.660806067112,-4.9423474261517,0.109207874409882));
#37574=CARTESIAN_POINT('Ctrl Pts',(220.657291679567,-4.93880747706411,0.218310997006985));
#37575=CARTESIAN_POINT('Ctrl Pts',(220.653777292022,-4.93158559359821,0.327169853757778));
#37576=CARTESIAN_POINT('Ctrl Pts',(220.627380768336,-4.8773421114786,1.14480745170729));
#37577=CARTESIAN_POINT('Ctrl Pts',(220.60098424465,-4.61538250376007,1.9486648053616));
#37578=CARTESIAN_POINT('Ctrl Pts',(220.574587720964,-4.17746978173744,2.64127295196166));
#37579=CARTESIAN_POINT('Ctrl Pts',(220.548191197278,-3.73955705971481,3.33388109856173));
#37580=CARTESIAN_POINT('Ctrl Pts',(220.521794673592,-3.12569122338807,3.91524003810755));
#37581=CARTESIAN_POINT('Ctrl Pts',(220.495398149907,-2.41030446704932,4.31485908908992));
#37582=CARTESIAN_POINT('Ctrl Pts',(220.469001626221,-1.69491771071057,4.7144781400723));
#37583=CARTESIAN_POINT('Ctrl Pts',(220.442605102535,-0.878010034359826,
4.93235730249122));
#37584=CARTESIAN_POINT('Ctrl Pts',(220.416208578849,-0.0586327723971473,
4.94207838676895));
#37585=CARTESIAN_POINT('Ctrl Pts',(220.389812055163,0.760744489565531,4.95179947104668));
#37586=CARTESIAN_POINT('Ctrl Pts',(220.363415531477,1.58259133714014,4.75336247718321));
#37587=CARTESIAN_POINT('Ctrl Pts',(220.337019007791,2.3072575532734,4.37082820136474));
#37588=CARTESIAN_POINT('Ctrl Pts',(220.310622484106,3.03192376940667,3.98829392554627));
#37589=CARTESIAN_POINT('Ctrl Pts',(220.28422596042,3.65940935409858,3.42166236777279));
#37590=CARTESIAN_POINT('Ctrl Pts',(220.257829436734,4.11363069789834,2.73963849151537));
#37591=CARTESIAN_POINT('Ctrl Pts',(220.231432913048,4.5678520416981,2.05761461525795));
#37592=CARTESIAN_POINT('Ctrl Pts',(220.205036389362,4.8488091446057,1.2601984205166));
#37593=CARTESIAN_POINT('Ctrl Pts',(220.178639865676,4.92243551800822,0.444077869312822));
#37594=CARTESIAN_POINT('Ctrl Pts',(220.152243341991,4.99606189141075,-0.372042681890931));
#37595=CARTESIAN_POINT('Ctrl Pts',(220.125846818305,4.8623575353082,-1.2068675895571));
#37596=CARTESIAN_POINT('Ctrl Pts',(220.099450294619,4.53753431221443,-1.95917302666104));
#37597=CARTESIAN_POINT('Ctrl Pts',(220.073053770933,4.21271108912065,-2.711478463765));
#37598=CARTESIAN_POINT('Ctrl Pts',(220.046657247247,3.69676899903564,-3.38126443030673));
#37599=CARTESIAN_POINT('Ctrl Pts',(220.020260723561,3.05226682811599,-3.88731832924966));
#37600=CARTESIAN_POINT('Ctrl Pts',(219.993864199875,2.40776465719635,-4.39337222819259));
#37601=CARTESIAN_POINT('Ctrl Pts',(219.96746767619,1.63470240544207,-4.73569405953674));
#37602=CARTESIAN_POINT('Ctrl Pts',(219.941071152504,0.826815081159675,-4.87277676530528));
#37603=CARTESIAN_POINT('Ctrl Pts',(219.914674628818,0.0189277568772817,
-5.00985947107383));
#37604=CARTESIAN_POINT('Ctrl Pts',(219.888278105132,-0.823784639933227,
-4.94170305126679));
#37605=CARTESIAN_POINT('Ctrl Pts',(219.861881581446,-1.59914191184,-4.67657157848882));
#37606=CARTESIAN_POINT('Ctrl Pts',(219.83548505776,-2.37449918374677,-4.41144010571084));
#37607=CARTESIAN_POINT('Ctrl Pts',(219.809088534074,-3.0825013307498,-3.94933357996195));
#37608=CARTESIAN_POINT('Ctrl Pts',(219.782692010389,-3.63730198410177,-3.34628314094649));
#37609=CARTESIAN_POINT('Ctrl Pts',(219.756295486703,-4.19210263745373,-2.74323270193106));
#37610=CARTESIAN_POINT('Ctrl Pts',(219.729898963017,-4.59370179715464,-1.99923834964908));
#37611=CARTESIAN_POINT('Ctrl Pts',(219.703502439331,-4.79340493636199,-1.20451056408532));
#37612=CARTESIAN_POINT('Ctrl Pts',(219.690441777773,-4.89221548976318,-0.811289442942511));
#37613=CARTESIAN_POINT('Ctrl Pts',(219.677381116215,-4.94159899911878,-0.405648049051028));
#37614=CARTESIAN_POINT('Ctrl Pts',(219.664320454657,-4.94158767198665,-3.94523114399803E-6));
#37615=CARTESIAN_POINT('Ctrl Pts',(219.519679545343,-4.94159107100858,-1.73410261375781E-5));
#37616=CARTESIAN_POINT('Ctrl Pts',(219.53227125237,-4.94163911104044,-0.391095669943753));
#37617=CARTESIAN_POINT('Ctrl Pts',(219.544862959397,-4.89577279646112,-0.782162918064062));
#37618=CARTESIAN_POINT('Ctrl Pts',(219.557454666424,-4.803864906551,-1.1620923503773));
#37619=CARTESIAN_POINT('Ctrl Pts',(219.58385119011,-4.61119454122674,-1.95855435807664));
#37620=CARTESIAN_POINT('Ctrl Pts',(219.610247713796,-4.21618758625521,-2.70606956822765));
#37621=CARTESIAN_POINT('Ctrl Pts',(219.636644237481,-3.66673925333529,-3.31400059131676));
#37622=CARTESIAN_POINT('Ctrl Pts',(219.663040761167,-3.11729092041538,-3.92193161440586));
#37623=CARTESIAN_POINT('Ctrl Pts',(219.689437284853,-2.4134012095471,-4.39027845043306));
#37624=CARTESIAN_POINT('Ctrl Pts',(219.715833808539,-1.64041785015744,-4.66225331230324));
#37625=CARTESIAN_POINT('Ctrl Pts',(219.742230332225,-0.86743449076778,-4.93422817417342));
#37626=CARTESIAN_POINT('Ctrl Pts',(219.768626855911,-0.0253574828567601,
-5.00983106188657));
#37627=CARTESIAN_POINT('Ctrl Pts',(219.795023379597,0.783710018041144,-4.87989500694632));
#37628=CARTESIAN_POINT('Ctrl Pts',(219.821419903282,1.59277751893909,-4.74995895200607));
#37629=CARTESIAN_POINT('Ctrl Pts',(219.847816426968,2.36883551282391,-4.4144839544124));
#37630=CARTESIAN_POINT('Ctrl Pts',(219.874212950654,3.01778575296881,-3.91414688283106));
#37631=CARTESIAN_POINT('Ctrl Pts',(219.90060947434,3.66673599311367,-3.41380981124975));
#37632=CARTESIAN_POINT('Ctrl Pts',(219.927005998026,4.1885784795186,-2.7486106656808));
#37633=CARTESIAN_POINT('Ctrl Pts',(219.953402521712,4.52003899372927,-1.9992058839361));
#37634=CARTESIAN_POINT('Ctrl Pts',(219.979799045397,4.85149950793995,-1.24980110219136));
#37635=CARTESIAN_POINT('Ctrl Pts',(220.006195569083,4.99257804995633,-0.416190684270871));
#37636=CARTESIAN_POINT('Ctrl Pts',(220.032592092769,4.92616862569162,0.400548801582176));
#37637=CARTESIAN_POINT('Ctrl Pts',(220.058988616455,4.8597592014269,1.21728828743518));
#37638=CARTESIAN_POINT('Ctrl Pts',(220.085385140141,4.58586181088109,2.0171568412208));
#37639=CARTESIAN_POINT('Ctrl Pts',(220.111781663827,4.13768694146142,2.70316914854727));
#37640=CARTESIAN_POINT('Ctrl Pts',(220.138178187512,3.68951207204175,3.38918145587374));
#37641=CARTESIAN_POINT('Ctrl Pts',(220.164574711198,3.06705972374821,3.96133751674111));
#37642=CARTESIAN_POINT('Ctrl Pts',(220.190971234884,2.3458032183009,4.35026251302223));
#37643=CARTESIAN_POINT('Ctrl Pts',(220.21736775857,1.62454671285356,4.73918750930336));
#37644=CARTESIAN_POINT('Ctrl Pts',(220.243764282256,0.804486050252458,4.94488144099823));
#37645=CARTESIAN_POINT('Ctrl Pts',(220.270160805942,-0.0149451303061554,
4.94240359686225));
#37646=CARTESIAN_POINT('Ctrl Pts',(220.296557329628,-0.834376310864792,
4.93992575272628));
#37647=CARTESIAN_POINT('Ctrl Pts',(220.322953853313,-1.65317800938092,4.72927613275944));
#37648=CARTESIAN_POINT('Ctrl Pts',(220.349350376999,-2.37206923802024,4.33599633316731));
#37649=CARTESIAN_POINT('Ctrl Pts',(220.375746900685,-3.09096046665952,3.94271653357521));
#37650=CARTESIAN_POINT('Ctrl Pts',(220.402143424371,-3.70994122542199,3.36680655435784));
#37651=CARTESIAN_POINT('Ctrl Pts',(220.428539948057,-4.15395912826009,2.67809638212087));
#37652=CARTESIAN_POINT('Ctrl Pts',(220.454936471743,-4.59797703109819,1.98938620988389));
#37653=CARTESIAN_POINT('Ctrl Pts',(220.481332995429,-4.86703207801192,1.18787584462733));
#37654=CARTESIAN_POINT('Ctrl Pts',(220.507729519114,-4.9285009233269,0.370749672950385));
#37655=CARTESIAN_POINT('Ctrl Pts',(220.511712861191,-4.93777682044256,0.247442032142238));
#37656=CARTESIAN_POINT('Ctrl Pts',(220.515696203267,-4.94232555847162,0.123778787731126));
#37657=CARTESIAN_POINT('Ctrl Pts',(220.519679545343,-4.94220801981422,0.000106916500303121));
#37658=CARTESIAN_POINT('Origin',(215.7,0.,0.));
#37659=CARTESIAN_POINT('',(221.664320454657,-4.94199158848527,-0.000125892924181525));
#37660=CARTESIAN_POINT('',(221.519679545343,-4.94203042585278,-0.000125883567849882));
#37661=CARTESIAN_POINT('',(215.7,-4.942,-6.05220448138622E-16));
#37662=CARTESIAN_POINT('Ctrl Pts',(221.664320454657,-4.94199158848527,-0.000125892924181525));
#37663=CARTESIAN_POINT('Ctrl Pts',(221.644231018009,-4.9413595014958,0.623677216857374));
#37664=CARTESIAN_POINT('Ctrl Pts',(221.62414158136,-4.8228328568654,1.2477129064962));
#37665=CARTESIAN_POINT('Ctrl Pts',(221.604052144712,-4.59227556616025,1.82717265502392));
#37666=CARTESIAN_POINT('Ctrl Pts',(221.577655621026,-4.2893347176133,2.58855403394672));
#37667=CARTESIAN_POINT('Ctrl Pts',(221.551259097341,-3.79297680109525,3.27297657942667));
#37668=CARTESIAN_POINT('Ctrl Pts',(221.524862573655,-3.16337544666258,3.79745180908665));
#37669=CARTESIAN_POINT('Ctrl Pts',(221.498466049969,-2.53377409222991,4.32192703874663));
#37670=CARTESIAN_POINT('Ctrl Pts',(221.472069526283,-1.77092929988263,4.68645495258663));
#37671=CARTESIAN_POINT('Ctrl Pts',(221.445673002597,-0.967342154830876,
4.84683651533342));
#37672=CARTESIAN_POINT('Ctrl Pts',(221.419276478911,-0.16375500977912,5.00721807808021));
#37673=CARTESIAN_POINT('Ctrl Pts',(221.392879955225,0.680574487977104,4.96345328973378));
#37674=CARTESIAN_POINT('Ctrl Pts',(221.36648343154,1.46327240205375,4.72084844128926));
#37675=CARTESIAN_POINT('Ctrl Pts',(221.340086907854,2.24597031613039,4.47824359284474));
#37676=CARTESIAN_POINT('Ctrl Pts',(221.313690384168,2.96703664652745,4.03679868430212));
#37677=CARTESIAN_POINT('Ctrl Pts',(221.287293860482,3.53903987119754,3.45003972328623));
#37678=CARTESIAN_POINT('Ctrl Pts',(221.260897336796,4.11104309586764,2.86328076227034));
#37679=CARTESIAN_POINT('Ctrl Pts',(221.23450081311,4.53398321481077,2.13120774878118));
#37680=CARTESIAN_POINT('Ctrl Pts',(221.208104289424,4.75657859487517,1.3425856246213));
#37681=CARTESIAN_POINT('Ctrl Pts',(221.181707765739,4.97917397493956,0.553963500461416));
#37682=CARTESIAN_POINT('Ctrl Pts',(221.155311242053,5.00142461612522,-0.291207734369187));
#37683=CARTESIAN_POINT('Ctrl Pts',(221.128914718367,4.82063234918612,-1.09044971754622));
#37684=CARTESIAN_POINT('Ctrl Pts',(221.102518194681,4.63984008224701,-1.88969170072324));
#37685=CARTESIAN_POINT('Ctrl Pts',(221.076121670995,4.25600490718315,-2.64300443224668));
#37686=CARTESIAN_POINT('Ctrl Pts',(221.049725147309,3.71566755489277,-3.25904757674573));
#37687=CARTESIAN_POINT('Ctrl Pts',(221.023328623623,3.17533020260239,-3.87509072124477));
#37688=CARTESIAN_POINT('Ctrl Pts',(220.996932099938,2.47849067308549,-4.3538642787194));
#37689=CARTESIAN_POINT('Ctrl Pts',(220.970535576252,1.70964179607628,-4.63731619980054));
#37690=CARTESIAN_POINT('Ctrl Pts',(220.944139052566,0.940792919067059,-4.92076812088168));
#37691=CARTESIAN_POINT('Ctrl Pts',(220.91774252888,0.0999346945655297,-5.0088984055693));
#37692=CARTESIAN_POINT('Ctrl Pts',(220.891346005194,-0.710977475777925,
-4.89102112168558));
#37693=CARTESIAN_POINT('Ctrl Pts',(220.864949481508,-1.5218896461214,-4.77314383780185));
#37694=CARTESIAN_POINT('Ctrl Pts',(220.838552957823,-2.3028557623068,-4.44925898534677));
#37695=CARTESIAN_POINT('Ctrl Pts',(220.812156434137,-2.95918247211069,-3.95863810841745));
#37696=CARTESIAN_POINT('Ctrl Pts',(220.785759910451,-3.61550918191456,-3.46801723148815));
#37697=CARTESIAN_POINT('Ctrl Pts',(220.759363386765,-4.14719648533692,-2.81066033008462));
#37698=CARTESIAN_POINT('Ctrl Pts',(220.732966863079,-4.48977645878774,-2.0662729582605));
#37699=CARTESIAN_POINT('Ctrl Pts',(220.710084726939,-4.78674592661956,-1.4209920346718));
#37700=CARTESIAN_POINT('Ctrl Pts',(220.687202590798,-4.941610832075,-0.710312128852271));
#37701=CARTESIAN_POINT('Ctrl Pts',(220.664320454657,-4.94224935728931,9.83974689322542E-5));
#37702=CARTESIAN_POINT('Ctrl Pts',(220.519679545343,-4.94220801981422,0.000106916500303121));
#37703=CARTESIAN_POINT('Ctrl Pts',(220.542092726953,-4.94154666178272,-0.69576103981452));
#37704=CARTESIAN_POINT('Ctrl Pts',(220.564505908562,-4.79315067695678,-1.39190212180872));
#37705=CARTESIAN_POINT('Ctrl Pts',(220.586919090172,-4.50786581270915,-2.02650499277872));
#37706=CARTESIAN_POINT('Ctrl Pts',(220.613315613858,-4.1718792130602,-2.77389150873351));
#37707=CARTESIAN_POINT('Ctrl Pts',(220.639712137544,-3.64602337004608,-3.43592256254577));
#37708=CARTESIAN_POINT('Ctrl Pts',(220.66610866123,-2.99405912783336,-3.93232585250573));
#37709=CARTESIAN_POINT('Ctrl Pts',(220.692505184915,-2.34209488562064,-4.4287291424657));
#37710=CARTESIAN_POINT('Ctrl Pts',(220.718901708601,-1.56402224420932,-4.75950466857337));
#37711=CARTESIAN_POINT('Ctrl Pts',(220.745298232287,-0.754183729619758,
-4.88454538040227));
#37712=CARTESIAN_POINT('Ctrl Pts',(220.771694755973,0.0556547849698012,
-5.00958609223117));
#37713=CARTESIAN_POINT('Ctrl Pts',(220.798091279659,0.897259172737602,-4.92889198978129));
#37714=CARTESIAN_POINT('Ctrl Pts',(220.824487803345,1.66858358435085,-4.65224735938235));
#37715=CARTESIAN_POINT('Ctrl Pts',(220.850884327031,2.43990799596407,-4.37560272898341));
#37716=CARTESIAN_POINT('Ctrl Pts',(220.877280850716,3.14095243142275,-3.90300757063542));
#37717=CARTESIAN_POINT('Ctrl Pts',(220.903677374402,3.68671415482571,-3.29176478700478));
#37718=CARTESIAN_POINT('Ctrl Pts',(220.930073898088,4.23247587822868,-2.68052200337414));
#37719=CARTESIAN_POINT('Ctrl Pts',(220.956470421774,4.62295488957593,-1.93063159446086));
#37720=CARTESIAN_POINT('Ctrl Pts',(220.98286694546,4.81080499863636,-1.13301894668909));
#37721=CARTESIAN_POINT('Ctrl Pts',(221.009263469146,4.99865510769681,-0.33540629891727));
#37722=CARTESIAN_POINT('Ctrl Pts',(221.035659992831,4.98387631447041,0.509928587713042));
#37723=CARTESIAN_POINT('Ctrl Pts',(221.062056516517,4.76826056819422,1.30048753549871));
#37724=CARTESIAN_POINT('Ctrl Pts',(221.088453040203,4.55264482191805,2.09104648328436));
#37725=CARTESIAN_POINT('Ctrl Pts',(221.114849563889,4.1361921225921,2.82682949222537));
#37726=CARTESIAN_POINT('Ctrl Pts',(221.141246087575,3.56939801746833,3.4186217190299));
#37727=CARTESIAN_POINT('Ctrl Pts',(221.167642611261,3.00260391234456,4.01041394583443));
#37728=CARTESIAN_POINT('Ctrl Pts',(221.194039134947,2.28546840142296,4.45821539050247));
#37729=CARTESIAN_POINT('Ctrl Pts',(221.220435658632,1.50494527649849,4.70772943008145));
#37730=CARTESIAN_POINT('Ctrl Pts',(221.246832182318,0.724422151574042,4.95724346966042));
#37731=CARTESIAN_POINT('Ctrl Pts',(221.273228706004,-0.119488587353277,
5.00847010415033));
#37732=CARTESIAN_POINT('Ctrl Pts',(221.29962522969,-0.924461417308162,4.85519801696677));
#37733=CARTESIAN_POINT('Ctrl Pts',(221.326021753376,-1.72943424726307,4.70192592978319));
#37734=CARTESIAN_POINT('Ctrl Pts',(221.352418277062,-2.49546916824554,4.34415512092613));
#37735=CARTESIAN_POINT('Ctrl Pts',(221.378814800748,-3.1296832992209,3.82526587584749));
#37736=CARTESIAN_POINT('Ctrl Pts',(221.405211324433,-3.76389743019626,3.30637663076886));
#37737=CARTESIAN_POINT('Ctrl Pts',(221.431607848119,-4.26629077116451,2.62636894946865));
#37738=CARTESIAN_POINT('Ctrl Pts',(221.458004371805,-4.57594723172245,1.86769479654986));
#37739=CARTESIAN_POINT('Ctrl Pts',(221.478562762984,-4.81711681613945,1.27681699010054));
#37740=CARTESIAN_POINT('Ctrl Pts',(221.499121154164,-4.94137695401291,0.638222038707901));
#37741=CARTESIAN_POINT('Ctrl Pts',(221.519679545343,-4.94203042585278,-0.000125883567849882));
#37742=CARTESIAN_POINT('Origin',(207.493410108095,0.,0.));
#37743=CARTESIAN_POINT('',(221.993410108095,-4.37199255865188,-0.000111372696215136));
#37744=CARTESIAN_POINT('',(222.,-4.372,-3.09002298987926E-13));
#37745=CARTESIAN_POINT('',(207.493410108095,-4.372,-3.09002298987926E-13));
#37746=CARTESIAN_POINT('',(222.,-4.36825282109637,-0.180973177525291));
#37747=CARTESIAN_POINT('Ctrl Pts',(221.993410108095,-4.37199255865188,-0.000111372696215244));
#37748=CARTESIAN_POINT('Ctrl Pts',(221.99560673873,-4.372053701201,-0.06045261198359));
#37749=CARTESIAN_POINT('Ctrl Pts',(221.997803369365,-4.370867891782,-0.12079139131084));
#37750=CARTESIAN_POINT('Ctrl Pts',(222.,-4.36842834878727,-0.181075889670185));
#37751=CARTESIAN_POINT('Origin',(222.,0.,0.));
#37752=CARTESIAN_POINT('Origin',(207.493410108095,0.,0.));
#37753=CARTESIAN_POINT('',(220.993410108095,-4.37222059693825,8.70485094473427E-5));
#37754=CARTESIAN_POINT('',(221.190589891905,-4.37202691659821,-0.00011136441995574));
#37755=CARTESIAN_POINT('',(207.493410108095,-4.372,-3.09002298987926E-13));
#37756=CARTESIAN_POINT('Ctrl Pts',(220.993410108095,-4.37222059693825,8.70485094474523E-5));
#37757=CARTESIAN_POINT('Ctrl Pts',(221.016292244236,-4.37165571789394,-0.628386205451742));
#37758=CARTESIAN_POINT('Ctrl Pts',(221.065570904062,-4.07660766898167,-1.98237095103711));
#37759=CARTESIAN_POINT('Ctrl Pts',(221.141246087575,-2.72814027777575,-3.64956206171641));
#37760=CARTESIAN_POINT('Ctrl Pts',(221.220435658632,-0.655466951210102,
-4.50914800360244));
#37761=CARTESIAN_POINT('Ctrl Pts',(221.29962522969,1.57615920673447,-4.27525144067998));
#37762=CARTESIAN_POINT('Ctrl Pts',(221.378814800747,3.42556172983117,-3.00459300688041));
#37763=CARTESIAN_POINT('Ctrl Pts',(221.458004371805,4.44425500302777,-1.00531138270765));
#37764=CARTESIAN_POINT('Ctrl Pts',(221.537193942863,4.38520210748118,1.23776144530491));
#37765=CARTESIAN_POINT('Ctrl Pts',(221.61638351392,3.26272485129782,3.18067315006488));
#37766=CARTESIAN_POINT('Ctrl Pts',(221.695573084978,1.34902473201658,4.35226186322655));
#37767=CARTESIAN_POINT('Ctrl Pts',(221.774762656035,-0.891814137382579,
4.46841300931145));
#37768=CARTESIAN_POINT('Ctrl Pts',(221.853952227093,-2.91639371982429,3.50096094174254));
#37769=CARTESIAN_POINT('Ctrl Pts',(221.926834711113,-4.12880172544123,1.82918469772558));
#37770=CARTESIAN_POINT('Ctrl Pts',(221.973320671447,-4.37143337526095,0.551743583994388));
#37771=CARTESIAN_POINT('Ctrl Pts',(221.993410108095,-4.37199255865188,-0.000111372696215244));
#37772=CARTESIAN_POINT('',(222.,-1.59436307123045,4.07092009220233));
#37773=CARTESIAN_POINT('Origin',(222.,0.,0.));
#37774=CARTESIAN_POINT('Ctrl Pts',(221.190589891905,-4.37202691659821,-0.000111364419955705));
#37775=CARTESIAN_POINT('Ctrl Pts',(221.196428024412,-4.37219108482666,-0.160480092140677));
#37776=CARTESIAN_POINT('Ctrl Pts',(221.228662680604,-4.32440771702623,-1.04584244130126));
#37777=CARTESIAN_POINT('Ctrl Pts',(221.287293860482,-3.7409896782648,-2.60135569353455));
#37778=CARTESIAN_POINT('Ctrl Pts',(221.36648343154,-2.04579887264011,-4.07145650839735));
#37779=CARTESIAN_POINT('Ctrl Pts',(221.445673002597,0.14550072168771,-4.5542152892435));
#37780=CARTESIAN_POINT('Ctrl Pts',(221.524862573655,2.30152409777985,-3.93256490416486));
#37781=CARTESIAN_POINT('Ctrl Pts',(221.604052144712,3.89940335283094,-2.35725035066262));
#37782=CARTESIAN_POINT('Ctrl Pts',(221.68324171577,4.55170192744695,-0.210305677009054));
#37783=CARTESIAN_POINT('Ctrl Pts',(221.762431286827,4.10012073214107,1.98766009715916));
#37784=CARTESIAN_POINT('Ctrl Pts',(221.841620857885,2.65441560822601,3.70356057542857));
#37785=CARTESIAN_POINT('Ctrl Pts',(221.920810428942,0.56466538392668,4.52140736785216));
#37786=CARTESIAN_POINT('Ctrl Pts',(221.973603476314,-0.919183673409389,
4.33535198326386));
#37787=CARTESIAN_POINT('Ctrl Pts',(222.,-1.59436307123039,4.07092009220235));
#37788=CARTESIAN_POINT('Origin',(207.493410108095,0.,0.));
#37789=CARTESIAN_POINT('',(219.993410108095,-4.37163522904201,-3.49019642618775E-6));
#37790=CARTESIAN_POINT('',(220.190589891905,-4.37218402724156,9.45849734608484E-5));
#37791=CARTESIAN_POINT('',(207.493410108095,-4.372,-3.09002298987926E-13));
#37792=CARTESIAN_POINT('Ctrl Pts',(219.993410108095,-4.37163522904201,-3.49019642562065E-6));
#37793=CARTESIAN_POINT('Ctrl Pts',(220.006470769653,-4.37164524972628,-0.358861446873992));
#37794=CARTESIAN_POINT('Ctrl Pts',(220.045927954897,-4.2396615535932,-1.44298955297618));
#37795=CARTESIAN_POINT('Ctrl Pts',(220.111781663827,-3.35331469136689,-3.08501753966403));
#37796=CARTESIAN_POINT('Ctrl Pts',(220.190971234884,-1.47428673505533,-4.31144190059531));
#37797=CARTESIAN_POINT('Ctrl Pts',(220.270160805942,0.762260370684581,-4.49232810095734));
#37798=CARTESIAN_POINT('Ctrl Pts',(220.349350376999,2.81395694980418,-3.58381067078537));
#37799=CARTESIAN_POINT('Ctrl Pts',(220.428539948057,4.18326015772707,-1.80620793157832));
#37800=CARTESIAN_POINT('Ctrl Pts',(220.507729519115,4.53810967910322,0.409405886501342));
#37801=CARTESIAN_POINT('Ctrl Pts',(220.586919090172,3.79245339384702,2.52573749520784));
#37802=CARTESIAN_POINT('Ctrl Pts',(220.66610866123,2.12711528603252,4.02956985290854));
#37803=CARTESIAN_POINT('Ctrl Pts',(220.745298232287,-0.0540549391371643,
4.55621890420622));
#37804=CARTESIAN_POINT('Ctrl Pts',(220.824487803345,-2.22211667183979,3.97797060507901));
#37805=CARTESIAN_POINT('Ctrl Pts',(220.903677374402,-3.85130815489554,2.43505197879753));
#37806=CARTESIAN_POINT('Ctrl Pts',(220.959984809319,-4.34565384402969,0.918087508898033));
#37807=CARTESIAN_POINT('Ctrl Pts',(220.98989572055,-4.37230735474205,0.0966120653418909));
#37808=CARTESIAN_POINT('Ctrl Pts',(220.993410108095,-4.37222059693825,8.70485094474523E-5));
#37809=CARTESIAN_POINT('Ctrl Pts',(220.190589891905,-4.37218402724156,9.45849734610045E-5));
#37810=CARTESIAN_POINT('Ctrl Pts',(220.213003073515,-4.37159894886969,-0.615513408755456));
#37811=CARTESIAN_POINT('Ctrl Pts',(220.26181277881,-4.08570679415814,-1.95666340110848));
#37812=CARTESIAN_POINT('Ctrl Pts',(220.337019007791,-2.76029389481659,-3.62530417052153));
#37813=CARTESIAN_POINT('Ctrl Pts',(220.416208578849,-0.695299810488197,
-4.50317786546855));
#37814=CARTESIAN_POINT('Ctrl Pts',(220.495398149907,1.53830665449812,-4.28901682788606));
#37815=CARTESIAN_POINT('Ctrl Pts',(220.574587720964,3.39886894010639,-3.03475578035621));
#37816=CARTESIAN_POINT('Ctrl Pts',(220.653777292022,4.43519486338251,-1.044556953301));
#37817=CARTESIAN_POINT('Ctrl Pts',(220.732966863079,4.39597214951006,1.19895020433616));
#37818=CARTESIAN_POINT('Ctrl Pts',(220.812156434137,3.29071241572633,3.15170818597724));
#37819=CARTESIAN_POINT('Ctrl Pts',(220.891346005194,1.38744463724644,4.34016705855231));
#37820=CARTESIAN_POINT('Ctrl Pts',(220.970535576252,-0.852282851982811,
4.47612184162993));
#37821=CARTESIAN_POINT('Ctrl Pts',(221.049725147309,-2.88532899192737,3.52660303771061));
#37822=CARTESIAN_POINT('Ctrl Pts',(221.12307658586,-4.12037514219452,1.85492309998823));
#37823=CARTESIAN_POINT('Ctrl Pts',(221.170031500726,-4.37144881484117,0.564610836347166));
#37824=CARTESIAN_POINT('Ctrl Pts',(221.190589891905,-4.37202691659821,-0.000111364419955705));
#37825=CARTESIAN_POINT('Origin',(207.493410108095,0.,0.));
#37826=CARTESIAN_POINT('',(218.993410108095,-4.37224100624368,-8.20526232630265E-5));
#37827=CARTESIAN_POINT('',(219.190589891905,-4.37163823602782,-1.53409482898936E-5));
#37828=CARTESIAN_POINT('',(207.493410108095,-4.372,-3.09002298987926E-13));
#37829=CARTESIAN_POINT('Ctrl Pts',(218.993410108095,-4.37224100624368,-8.20526232626559E-5));
#37830=CARTESIAN_POINT('Ctrl Pts',(218.99664929507,-4.37231767120945,-0.0890472990870102));
#37831=CARTESIAN_POINT('Ctrl Pts',(219.026285005732,-4.34798024483397,-0.902959118710753));
#37832=CARTESIAN_POINT('Ctrl Pts',(219.082317240079,-3.8638878894494,-2.41504099698875));
#37833=CARTESIAN_POINT('Ctrl Pts',(219.161506811136,-2.24272204053807,-3.96639010792621));
#37834=CARTESIAN_POINT('Ctrl Pts',(219.240696382194,-0.077689074547423,
-4.55587719841812));
#37835=CARTESIAN_POINT('Ctrl Pts',(219.319885953251,2.10618373527536,-4.04054980326089));
#37836=CARTESIAN_POINT('Ctrl Pts',(219.399075524309,3.77930039456389,-2.54537642933601));
#37837=CARTESIAN_POINT('Ctrl Pts',(219.478265095366,4.53592487469901,-0.43294130139881));
#37838=CARTESIAN_POINT('Ctrl Pts',(219.557454666424,4.19257337016016,1.78448344772206));
#37839=CARTESIAN_POINT('Ctrl Pts',(219.636644237481,2.83250969587536,3.569165373325));
#37840=CARTESIAN_POINT('Ctrl Pts',(219.715833808539,0.785553551391572,4.48831352038449));
#37841=CARTESIAN_POINT('Ctrl Pts',(219.795023379596,-1.45190178897309,4.3190315852685));
#37842=CARTESIAN_POINT('Ctrl Pts',(219.874212950654,-3.33726639942199,3.10237096728598));
#37843=CARTESIAN_POINT('Ctrl Pts',(219.940341860154,-4.2358587294695,1.45812021942101));
#37844=CARTESIAN_POINT('Ctrl Pts',(219.980074245967,-4.37162499721238,0.366415945178225));
#37845=CARTESIAN_POINT('Ctrl Pts',(219.993410108095,-4.37163522904201,-3.49019642562065E-6));
#37846=CARTESIAN_POINT('Ctrl Pts',(219.190589891905,-4.37163823602782,-1.53409482897549E-5));
#37847=CARTESIAN_POINT('Ctrl Pts',(219.203181598932,-4.37168073522234,-0.345987508902117));
#37848=CARTESIAN_POINT('Ctrl Pts',(219.242169829645,-4.24604297815936,-1.41720529400801));
#37849=CARTESIAN_POINT('Ctrl Pts',(219.307554584043,-3.38045360582197,-3.05525549394406));
#37850=CARTESIAN_POINT('Ctrl Pts',(219.386744155101,-1.51233999842644,-4.29824155248976));
#37851=CARTESIAN_POINT('Ctrl Pts',(219.465933726158,0.722520793916989,-4.49889057621407));
#37852=CARTESIAN_POINT('Ctrl Pts',(219.545123297216,2.78216803143074,-3.60854454860609));
#37853=CARTESIAN_POINT('Ctrl Pts',(219.624312868274,4.16713080999959,-1.84311516914782));
#37854=CARTESIAN_POINT('Ctrl Pts',(219.703502439331,4.5415513193251,0.369275409857588));
#37855=CARTESIAN_POINT('Ctrl Pts',(219.782692010389,3.81463141353823,2.49211554572396));
#37856=CARTESIAN_POINT('Ctrl Pts',(219.861881581446,2.16265144586963,4.01060985862089));
#37857=CARTESIAN_POINT('Ctrl Pts',(219.941071152504,-0.0137782689576099,
4.55651872307046));
#37858=CARTESIAN_POINT('Ctrl Pts',(220.020260723561,-2.1868667104261,3.99745753013543));
#37859=CARTESIAN_POINT('Ctrl Pts',(220.099450294619,-3.82963312724697,2.46900036959006));
#37860=CARTESIAN_POINT('Ctrl Pts',(220.156226684067,-4.34159732403268,0.943867817456289));
#37861=CARTESIAN_POINT('Ctrl Pts',(220.186606549829,-4.37228800923471,0.109502399830049));
#37862=CARTESIAN_POINT('Ctrl Pts',(220.190589891905,-4.37218402724156,9.45849734610045E-5));
#37863=CARTESIAN_POINT('Origin',(207.493410108095,0.,0.));
#37864=CARTESIAN_POINT('',(217.993410108095,-4.37196318003322,0.000112001314848215));
#37865=CARTESIAN_POINT('',(218.190589891905,-4.37227359254426,-7.26212656684822E-5));
#37866=CARTESIAN_POINT('',(207.493410108095,-4.372,-3.09002298987926E-13));
#37867=CARTESIAN_POINT('Ctrl Pts',(217.993410108095,-4.37196318003322,0.000112001314848311));
#37868=CARTESIAN_POINT('Ctrl Pts',(218.013224344173,-4.37141834399079,-0.544191718226455));
#37869=CARTESIAN_POINT('Ctrl Pts',(218.059435103938,-4.13369733469641,-1.81407939528679));
#37870=CARTESIAN_POINT('Ctrl Pts',(218.132042387388,-2.93451119586052,-3.48578494470606));
#37871=CARTESIAN_POINT('Ctrl Pts',(218.211231958445,-0.914983456707324,
-4.46372690846136));
#37872=CARTESIAN_POINT('Ctrl Pts',(218.290421529503,1.32643063562732,-4.35920112041638));
#37873=CARTESIAN_POINT('Ctrl Pts',(218.369611100561,3.24618114559881,-3.1975554114556));
#37874=CARTESIAN_POINT('Ctrl Pts',(218.448800671618,4.37872256355528,-1.26049250326289));
#37875=CARTESIAN_POINT('Ctrl Pts',(218.527990242676,4.44941004951064,0.982243783733906));
#37876=CARTESIAN_POINT('Ctrl Pts',(218.607179813733,3.44110166678914,2.98678287764463));
#37877=CARTESIAN_POINT('Ctrl Pts',(218.686369384791,1.59831535534295,4.26701777172829));
#37878=CARTESIAN_POINT('Ctrl Pts',(218.765558955848,-0.632067434303197,
4.51248749559082));
#37879=CARTESIAN_POINT('Ctrl Pts',(218.844748526906,-2.70917189204705,3.66366487259853));
#37880=CARTESIAN_POINT('Ctrl Pts',(218.920698910988,-4.07120472088646,1.99745382197457));
#37881=CARTESIAN_POINT('Ctrl Pts',(218.970252771385,-4.37169291919601,0.635941179003326));
#37882=CARTESIAN_POINT('Ctrl Pts',(218.993410108095,-4.37224100624368,-8.20526232626559E-5));
#37883=CARTESIAN_POINT('Ctrl Pts',(218.190589891905,-4.37227359254426,-7.26212656684041E-5));
#37884=CARTESIAN_POINT('Ctrl Pts',(218.193360124349,-4.3723334352599,-0.0761562484549823));
#37885=CARTESIAN_POINT('Ctrl Pts',(218.222526880479,-4.35185253664576,-0.877180496390307));
#37886=CARTESIAN_POINT('Ctrl Pts',(218.278090160295,-3.88508462005382,-2.38079192904617));
#37887=CARTESIAN_POINT('Ctrl Pts',(218.357279731353,-2.27769520857755,-3.94641067949257));
#37888=CARTESIAN_POINT('Ctrl Pts',(218.43646930241,-0.117957577266953,-4.55501248344671));
#37889=CARTESIAN_POINT('Ctrl Pts',(218.515658873468,2.07038513587111,-4.05900949783985));
#37890=CARTESIAN_POINT('Ctrl Pts',(218.594848444525,3.75665297092044,-2.57868399973024));
#37891=CARTESIAN_POINT('Ctrl Pts',(218.674038015583,4.53192069796186,-0.473019557497457));
#37892=CARTESIAN_POINT('Ctrl Pts',(218.75322758664,4.20818346572563,1.74735360851304));
#37893=CARTESIAN_POINT('Ctrl Pts',(218.832417157698,2.86394856669164,3.54398805327205));
#37894=CARTESIAN_POINT('Ctrl Pts',(218.911606728756,0.825197172846602,4.48119429843385));
#37895=CARTESIAN_POINT('Ctrl Pts',(218.990796299813,-1.41366711921135,4.33169689503441));
#37896=CARTESIAN_POINT('Ctrl Pts',(219.069985870871,-3.30971270848846,3.13174943149354));
#37897=CARTESIAN_POINT('Ctrl Pts',(219.136583734901,-4.22927944508702,1.48390254504573));
#37898=CARTESIAN_POINT('Ctrl Pts',(219.176785075246,-4.37159164237796,0.379288460950675));
#37899=CARTESIAN_POINT('Ctrl Pts',(219.190589891905,-4.37163823602782,-1.53409482897549E-5));
#37900=CARTESIAN_POINT('Origin',(207.493410108095,0.,0.));
#37901=CARTESIAN_POINT('',(216.993410108095,-4.37172079063294,-7.45667008033409E-5));
#37902=CARTESIAN_POINT('',(217.190589891905,-4.37192402085483,0.000110650652629316));
#37903=CARTESIAN_POINT('',(207.493410108095,-4.372,-3.09002298987926E-13));
#37904=CARTESIAN_POINT('Ctrl Pts',(216.993410108095,-4.37172079063294,-7.45667008031012E-5));
#37905=CARTESIAN_POINT('Ctrl Pts',(217.003402869591,-4.37188869880949,-0.274622762470965));
#37906=CARTESIAN_POINT('Ctrl Pts',(217.039792154772,-4.27917236998106,-1.27429571461977));
#37907=CARTESIAN_POINT('Ctrl Pts',(217.10257796364,-3.52601195980057,-2.8860513333469));
#37908=CARTESIAN_POINT('Ctrl Pts',(217.181767534697,-1.72100782049271,-4.21902651344751));
#37909=CARTESIAN_POINT('Ctrl Pts',(217.260957105755,0.501346103979698,-4.52887455372684));
#37910=CARTESIAN_POINT('Ctrl Pts',(217.340146676813,2.60212202845841,-3.74045633424341));
#37911=CARTESIAN_POINT('Ctrl Pts',(217.41933624787,4.07187521345992,-2.04496574185997));
#37912=CARTESIAN_POINT('Ctrl Pts',(217.498525818928,4.55418590963663,0.146435445973139));
#37913=CARTESIAN_POINT('Ctrl Pts',(217.577715389985,3.93209226298936,2.3023255796497));
#37914=CARTESIAN_POINT('Ctrl Pts',(217.656904961043,2.35645393068466,3.89989455138609));
#37915=CARTESIAN_POINT('Ctrl Pts',(217.7360945321,0.209368141831046,4.55172688334399));
#37916=CARTESIAN_POINT('Ctrl Pts',(217.815284103158,-1.98849007697495,4.0997511940534));
#37917=CARTESIAN_POINT('Ctrl Pts',(217.894473674215,-3.70413322589841,2.65357300336085));
#37918=CARTESIAN_POINT('Ctrl Pts',(217.953849009194,-4.31699380515626,1.0867590052297));
#37919=CARTESIAN_POINT('Ctrl Pts',(217.986827820488,-4.37214417452203,0.180929652502748));
#37920=CARTESIAN_POINT('Ctrl Pts',(217.993410108095,-4.37196318003322,0.000112001314848311));
#37921=CARTESIAN_POINT('Ctrl Pts',(217.190589891905,-4.37192402085483,0.000110650652629211));
#37922=CARTESIAN_POINT('Ctrl Pts',(217.209935173452,-4.37140677994815,-0.531324417985278));
#37923=CARTESIAN_POINT('Ctrl Pts',(217.255676978685,-4.14192180632446,-1.78833405490227));
#37924=CARTESIAN_POINT('Ctrl Pts',(217.327815307605,-2.96520904301682,-3.45970924292799));
#37925=CARTESIAN_POINT('Ctrl Pts',(217.407004878662,-0.954404689107857,
-4.45546455532968));
#37926=CARTESIAN_POINT('Ctrl Pts',(217.48619444972,1.28784579027261,-4.37075576243597));
#37927=CARTESIAN_POINT('Ctrl Pts',(217.565384020777,3.21778963310249,-3.22612501175764));
#37928=CARTESIAN_POINT('Ctrl Pts',(217.644573591835,4.36740941459516,-1.2991488443191));
#37929=CARTESIAN_POINT('Ctrl Pts',(217.723763162892,4.45791873813246,0.942874985667582));
#37930=CARTESIAN_POINT('Ctrl Pts',(217.80295273395,3.46736880936034,2.95624867936802));
#37931=CARTESIAN_POINT('Ctrl Pts',(217.882142305007,1.63597108754423,4.25272281192996));
#37932=CARTESIAN_POINT('Ctrl Pts',(217.961331876065,-0.592154745435518,
4.5178983467812));
#37933=CARTESIAN_POINT('Ctrl Pts',(218.040521447122,-2.6766811985351,3.68746938642191));
#37934=CARTESIAN_POINT('Ctrl Pts',(218.116940785736,-4.06188970218061,2.02314982239138));
#37935=CARTESIAN_POINT('Ctrl Pts',(218.166963600663,-4.37176321608425,0.648816586018496));
#37936=CARTESIAN_POINT('Ctrl Pts',(218.190589891905,-4.37227359254426,-7.26212656684041E-5));
#37937=CARTESIAN_POINT('Origin',(207.493410108095,0.,0.));
#37938=CARTESIAN_POINT('',(215.993410108095,-4.37237677050361,-4.95149419051281E-6));
#37939=CARTESIAN_POINT('',(216.190589891905,-4.37174661086188,-8.31034356851834E-5));
#37940=CARTESIAN_POINT('',(207.493410108095,-4.372,-3.09002298987926E-13));
#37941=CARTESIAN_POINT('Ctrl Pts',(215.993410108095,-4.37237654485879,-4.94852878089684E-6));
#37942=CARTESIAN_POINT('Ctrl Pts',(215.993581395008,-4.3723768600723,-0.00470897188487751));
#37943=CARTESIAN_POINT('Ctrl Pts',(216.020149205607,-4.37122390828525,-0.734336079798519));
#37944=CARTESIAN_POINT('Ctrl Pts',(216.073113539892,-3.99700949719232,-2.18768547070287));
#37945=CARTESIAN_POINT('Ctrl Pts',(216.152303110949,-2.46821587915816,-3.83013877206057));
#37946=CARTESIAN_POINT('Ctrl Pts',(216.231492682007,-0.340872182129313,
-4.54377142854046));
#37947=CARTESIAN_POINT('Ctrl Pts',(216.310682253064,1.86913408638018,-4.15552528647124));
#37948=CARTESIAN_POINT('Ctrl Pts',(216.389871824122,3.62586948644518,-2.75955125095293));
#37949=CARTESIAN_POINT('Ctrl Pts',(216.469061395179,4.50332018298729,-0.694377396571518));
#37950=CARTESIAN_POINT('Ctrl Pts',(216.548250966237,4.28870163468497,1.5391851506627));
#37951=CARTESIAN_POINT('Ctrl Pts',(216.627440537294,3.03405951149959,3.39949047947615));
#37952=CARTESIAN_POINT('Ctrl Pts',(216.706630108352,1.04364845674816,4.43540872277824));
#37953=CARTESIAN_POINT('Ctrl Pts',(216.78581967941,-1.19985061656117,4.39572646297605));
#37954=CARTESIAN_POINT('Ctrl Pts',(216.865009250467,-3.15238215846906,3.29006677232181));
#37955=CARTESIAN_POINT('Ctrl Pts',(216.934206060029,-4.19053128720911,1.62675556634124));
#37956=CARTESIAN_POINT('Ctrl Pts',(216.977006345905,-4.37144515853675,0.450613995719711));
#37957=CARTESIAN_POINT('Ctrl Pts',(216.993410108095,-4.37172079063294,-7.45667008031012E-5));
#37958=CARTESIAN_POINT('Ctrl Pts',(216.190589891905,-4.37174661086188,-8.31034356850099E-5));
#37959=CARTESIAN_POINT('Ctrl Pts',(216.20011369887,-4.37192637963066,-0.261742485074944));
#37960=CARTESIAN_POINT('Ctrl Pts',(216.23603402952,-4.28475048323144,-1.24850796410071));
#37961=CARTESIAN_POINT('Ctrl Pts',(216.298350883856,-3.55138537175629,-2.85477050840615));
#37962=CARTESIAN_POINT('Ctrl Pts',(216.377540454914,-1.75823454219255,-4.20364889221627));
#37963=CARTESIAN_POINT('Ctrl Pts',(216.456730025972,0.46129366910955,-4.53312925750298));
#37964=CARTESIAN_POINT('Ctrl Pts',(216.535919597029,2.56895672128326,-3.76331158403921));
#37965=CARTESIAN_POINT('Ctrl Pts',(216.615109168087,4.05363972481456,-2.08087906803723));
#37966=CARTESIAN_POINT('Ctrl Pts',(216.694298739144,4.55530240261518,0.106173137461614));
#37967=CARTESIAN_POINT('Ctrl Pts',(216.773488310202,3.95228998454865,2.26747802468437));
#37968=CARTESIAN_POINT('Ctrl Pts',(216.852677881259,2.39083487010492,3.87891239115818));
#37969=CARTESIAN_POINT('Ctrl Pts',(216.931867452317,0.249594813651761,4.5496983574066));
#37970=CARTESIAN_POINT('Ctrl Pts',(217.011057023374,-1.95217276662517,4.11716822629792));
#37971=CARTESIAN_POINT('Ctrl Pts',(217.090246594432,-3.68053233849351,2.68621190893303));
#37972=CARTESIAN_POINT('Ctrl Pts',(217.150090883942,-4.31216843510475,1.11254484294713));
#37973=CARTESIAN_POINT('Ctrl Pts',(217.183538649767,-4.37211255214439,0.193815629342384));
#37974=CARTESIAN_POINT('Ctrl Pts',(217.190589891905,-4.37192402085483,0.000110650652629211));
#37975=CARTESIAN_POINT('Origin',(207.493410108095,0.,0.));
#37976=CARTESIAN_POINT('',(214.993410108095,-4.37173935379323,8.08904380046663E-5));
#37977=CARTESIAN_POINT('',(215.190589891905,-4.37237558886668,8.59259548038633E-6));
#37978=CARTESIAN_POINT('',(207.493410108095,-4.372,-3.09002298987926E-13));
#37979=CARTESIAN_POINT('Ctrl Pts',(214.993410108095,-4.37173935379323,8.08904380046604E-5));
#37980=CARTESIAN_POINT('Ctrl Pts',(215.010156444111,-4.37143236352728,-0.460014190704367));
#37981=CARTESIAN_POINT('Ctrl Pts',(215.053299303813,-4.18513208821824,-1.6455800269089));
#37982=CARTESIAN_POINT('Ctrl Pts',(215.122838687201,-3.13107142267409,-3.31035411783751));
#37983=CARTESIAN_POINT('Ctrl Pts',(215.202028258259,-1.17144099051237,-4.40338263669165));
#37984=CARTESIAN_POINT('Ctrl Pts',(215.281217829316,1.07226754977981,-4.42857707859527));
#37985=CARTESIAN_POINT('Ctrl Pts',(215.360407400374,3.05594785184388,-3.37982771249969));
#37986=CARTESIAN_POINT('Ctrl Pts',(215.439596971431,4.29855123127321,-1.5114595434512));
#37987=CARTESIAN_POINT('Ctrl Pts',(215.518786542489,4.49874247780649,0.723442297456857));
#37988=CARTESIAN_POINT('Ctrl Pts',(215.597976113546,3.60797458733507,2.7829071160415));
#37989=CARTESIAN_POINT('Ctrl Pts',(215.677165684604,1.84226156240618,4.16750824534888));
#37990=CARTESIAN_POINT('Ctrl Pts',(215.756355255662,-0.370205659762209,
4.54147557615916));
#37991=CARTESIAN_POINT('Ctrl Pts',(215.835544826719,-2.49289685027711,3.81412085981142));
#37992=CARTESIAN_POINT('Ctrl Pts',(215.914563110864,-4.0077689802887,2.16540379512807));
#37993=CARTESIAN_POINT('Ctrl Pts',(215.967184871322,-4.37232828344233,0.720214267893106));
#37994=CARTESIAN_POINT('Ctrl Pts',(215.993410108095,-4.37237654485879,-4.94852878089684E-6));
#37995=CARTESIAN_POINT('Ctrl Pts',(215.190589891905,-4.37237558886668,8.59259548050451E-6));
#37996=CARTESIAN_POINT('Ctrl Pts',(215.216688747973,-4.37229330250909,-0.716740314340791));
#37997=CARTESIAN_POINT('Ctrl Pts',(215.269184127726,-4.01049950323238,-2.15849297429132));
#37998=CARTESIAN_POINT('Ctrl Pts',(215.348076031166,-2.50197584827897,-3.8081714206452));
#37999=CARTESIAN_POINT('Ctrl Pts',(215.427265602223,-0.381023394472204,
-4.54058078743843));
#38000=CARTESIAN_POINT('Ctrl Pts',(215.506455173281,1.83232842552693,-4.17188509614013));
#38001=CARTESIAN_POINT('Ctrl Pts',(215.585644744338,3.60133486508171,-2.79149420632338));
#38002=CARTESIAN_POINT('Ctrl Pts',(215.664834315396,4.49700632361528,-0.734157230948736));
#38003=CARTESIAN_POINT('Ctrl Pts',(215.744023886454,4.30213966797164,1.50121517167094));
#38004=CARTESIAN_POINT('Ctrl Pts',(215.823213457511,3.06399067229672,3.3725381946642));
#38005=CARTESIAN_POINT('Ctrl Pts',(215.902403028569,1.08281434484414,4.42601014560404));
#38006=CARTESIAN_POINT('Ctrl Pts',(215.981592599626,-1.16094785166298,4.40616077783247));
#38007=CARTESIAN_POINT('Ctrl Pts',(216.060782170684,-3.12317655906599,3.31780362518501));
#38008=CARTESIAN_POINT('Ctrl Pts',(216.130447934777,-4.18312293967722,1.65252427293828));
#38009=CARTESIAN_POINT('Ctrl Pts',(216.173717175184,-4.37142812608763,0.463482006636045));
#38010=CARTESIAN_POINT('Ctrl Pts',(216.190589891905,-4.37174661086188,-8.31034356850099E-5));
#38011=CARTESIAN_POINT('Origin',(207.493410108095,0.,0.));
#38012=CARTESIAN_POINT('',(213.993410108095,-4.37193445885121,-0.000111146439951045));
#38013=CARTESIAN_POINT('',(214.190589891905,-4.3717143632787,7.2119750405969E-5));
#38014=CARTESIAN_POINT('',(207.493410108095,-4.372,-3.09002298987926E-13));
#38015=CARTESIAN_POINT('Ctrl Pts',(213.993410108095,-4.37193445885121,-0.00011114643995053));
#38016=CARTESIAN_POINT('Ctrl Pts',(214.000334969528,-4.37212121263154,-0.19034300863519));
#38017=CARTESIAN_POINT('Ctrl Pts',(214.033656354648,-4.31348053118326,-1.10559563790858));
#38018=CARTESIAN_POINT('Ctrl Pts',(214.093374263453,-3.68692103050771,-2.6774364519387));
#38019=CARTESIAN_POINT('Ctrl Pts',(214.172563834511,-1.96197521572409,-4.11250603552804));
#38020=CARTESIAN_POINT('Ctrl Pts',(214.251753405568,0.238755732067328,-4.55028002872078));
#38021=CARTESIAN_POINT('Ctrl Pts',(214.330942976626,2.38158766725776,-3.88459686744144));
#38022=CARTESIAN_POINT('Ctrl Pts',(214.410132547683,3.94687713608336,-2.27688680263919));
#38023=CARTESIAN_POINT('Ctrl Pts',(214.489322118741,4.55503654123292,-0.117024558973872));
#38024=CARTESIAN_POINT('Ctrl Pts',(214.568511689798,4.05858532273295,2.07121650666143));
#38025=CARTESIAN_POINT('Ctrl Pts',(214.647701260856,2.57791445552183,3.75718108418821));
#38026=CARTESIAN_POINT('Ctrl Pts',(214.726890831913,0.472091261067617,4.53201748458606));
#38027=CARTESIAN_POINT('Ctrl Pts',(214.806080402971,-1.74821554237347,4.20782545464685));
#38028=CARTESIAN_POINT('Ctrl Pts',(214.885269974028,-3.54457460290309,2.86322257671746));
#38029=CARTESIAN_POINT('Ctrl Pts',(214.94771320907,-4.2832591449728,1.25545762566034));
#38030=CARTESIAN_POINT('Ctrl Pts',(214.983759920425,-4.37191625897872,0.265213745447506));
#38031=CARTESIAN_POINT('Ctrl Pts',(214.993410108095,-4.37173935379323,8.08904380046604E-5));
#38032=CARTESIAN_POINT('Ctrl Pts',(214.190589891905,-4.3717143632787,7.21197504059343E-5));
#38033=CARTESIAN_POINT('Ctrl Pts',(214.20686727339,-4.37145034324393,-0.447146056196735));
#38034=CARTESIAN_POINT('Ctrl Pts',(214.249541178561,-4.19250586234899,-1.61981056612665));
#38035=CARTESIAN_POINT('Ctrl Pts',(214.318611607418,-3.16021087534511,-3.28254778148629));
#38036=CARTESIAN_POINT('Ctrl Pts',(214.397801178475,-1.21031879251578,-4.39285569247082));
#38037=CARTESIAN_POINT('Ctrl Pts',(214.476990749533,1.03307938716119,-4.43788234343958));
#38038=CARTESIAN_POINT('Ctrl Pts',(214.55618032059,3.02595258074822,-3.40670863054845));
#38039=CARTESIAN_POINT('Ctrl Pts',(214.635369891648,4.28502279886023,-1.54939740790998));
#38040=CARTESIAN_POINT('Ctrl Pts',(214.714559462705,4.50496157129557,0.683647537507614));
#38041=CARTESIAN_POINT('Ctrl Pts',(214.793749033763,3.63243305708234,2.75090581449194));
#38042=CARTESIAN_POINT('Ctrl Pts',(214.872938604821,1.87902815291533,4.15106081802492));
#38043=CARTESIAN_POINT('Ctrl Pts',(214.952128175878,-0.330046961810515,
4.54457057568587));
#38044=CARTESIAN_POINT('Ctrl Pts',(215.031317746936,-2.45908465487818,3.83600773911274));
#38045=CARTESIAN_POINT('Ctrl Pts',(215.110507317993,-3.99178661943011,2.19720101477514));
#38046=CARTESIAN_POINT('Ctrl Pts',(215.163598032983,-4.37036335382686,0.74128143659256));
#38047=CARTESIAN_POINT('Ctrl Pts',(215.190292224287,-4.37237652737464,0.00818339302941881));
#38048=CARTESIAN_POINT('Ctrl Pts',(215.190589891905,-4.37237558886668,8.59259548050451E-6));
#38049=CARTESIAN_POINT('Origin',(207.493410108095,0.,0.));
#38050=CARTESIAN_POINT('',(212.993410108095,-4.37226510377645,7.5272650791474E-5));
#38051=CARTESIAN_POINT('',(213.190589891905,-4.37197391080243,-0.000112134234356298));
#38052=CARTESIAN_POINT('',(207.493410108095,-4.372,-3.09002298987926E-13));
#38053=CARTESIAN_POINT('Ctrl Pts',(212.993410108095,-4.37226510377645,7.52726507913769E-5));
#38054=CARTESIAN_POINT('Ctrl Pts',(213.016910018632,-4.37174339242606,-0.645346551482844));
#38055=CARTESIAN_POINT('Ctrl Pts',(213.066806452854,-4.06441348752009,-2.01622563803203));
#38056=CARTESIAN_POINT('Ctrl Pts',(213.143099410762,-2.685457954271,-3.68108247872997));
#38057=CARTESIAN_POINT('Ctrl Pts',(213.22228898182,-0.602915682492534,-4.51647487750953));
#38058=CARTESIAN_POINT('Ctrl Pts',(213.301478552877,1.62583553009629,-4.25660797683398));
#38059=CARTESIAN_POINT('Ctrl Pts',(213.380668123935,3.46031653593829,-2.96450031379357));
#38060=CARTESIAN_POINT('Ctrl Pts',(213.459857694992,4.45565994712272,-0.953492042429545));
#38061=CARTESIAN_POINT('Ctrl Pts',(213.53904726605,4.37049186989017,1.28874103472886));
#38062=CARTESIAN_POINT('Ctrl Pts',(213.618236837108,3.22546582964164,3.21845037575295));
#38063=CARTESIAN_POINT('Ctrl Pts',(213.697426408165,1.29825422636,4.36767542327822));
#38064=CARTESIAN_POINT('Ctrl Pts',(213.776615979223,-0.943788091813559,
4.45772550490954));
#38065=CARTESIAN_POINT('Ctrl Pts',(213.85580555028,-2.9569588426014,3.46676319389305));
#38066=CARTESIAN_POINT('Ctrl Pts',(213.928070259904,-4.13971832299312,1.79527273839626));
#38067=CARTESIAN_POINT('Ctrl Pts',(213.973938445843,-4.37140933548667,0.534792057890676));
#38068=CARTESIAN_POINT('Ctrl Pts',(213.993410108095,-4.37193445885121,-0.00011114643995053));
#38069=CARTESIAN_POINT('Ctrl Pts',(213.190589891905,-4.37197391080243,-0.000112134234356263));
#38070=CARTESIAN_POINT('Ctrl Pts',(213.197045798807,-4.37215244790249,-0.177456814333501));
#38071=CARTESIAN_POINT('Ctrl Pts',(213.229898229396,-4.31827393176692,-1.079809973257));
#38072=CARTESIAN_POINT('Ctrl Pts',(213.28914718367,-3.71044411132438,-2.6447414261376));
#38073=CARTESIAN_POINT('Ctrl Pts',(213.368336754727,-1.99825093901252,-4.09500255178501));
#38074=CARTESIAN_POINT('Ctrl Pts',(213.447526325785,0.198524342788504,-4.55221273664913));
#38075=CARTESIAN_POINT('Ctrl Pts',(213.526715896842,2.34715684985826,-3.90549707931699));
#38076=CARTESIAN_POINT('Ctrl Pts',(213.6059054679,3.92659647158984,-2.31168615164089));
#38077=CARTESIAN_POINT('Ctrl Pts',(213.685095038957,4.55382415428641,-0.157284094007629));
#38078=CARTESIAN_POINT('Ctrl Pts',(213.764284610015,4.07673522096414,2.03525984889906));
#38079=CARTESIAN_POINT('Ctrl Pts',(213.843474181072,2.61102523177998,3.7342469057895));
#38080=CARTESIAN_POINT('Ctrl Pts',(213.92266375213,0.512133448436073,4.5276673956225));
#38081=CARTESIAN_POINT('Ctrl Pts',(214.001853323188,-1.71095229970873,4.22311436531282));
#38082=CARTESIAN_POINT('Ctrl Pts',(214.081042894245,-3.51912675796424,2.89444287830494));
#38083=CARTESIAN_POINT('Ctrl Pts',(214.143955083818,-4.27764833622274,1.28124536185332));
#38084=CARTESIAN_POINT('Ctrl Pts',(214.180470749704,-4.3718784963291,0.278093761091111));
#38085=CARTESIAN_POINT('Ctrl Pts',(214.190589891905,-4.3717143632787,7.21197504059343E-5));
#38086=CARTESIAN_POINT('Origin',(207.493410108095,0.,0.));
#38087=CARTESIAN_POINT('',(211.993410108095,-4.37163704855645,1.21582882285062E-5));
#38088=CARTESIAN_POINT('',(212.190589891905,-4.37223174941664,8.43980496761931E-5));
#38089=CARTESIAN_POINT('',(207.493410108095,-4.372,-3.09002298987926E-13));
#38090=CARTESIAN_POINT('Ctrl Pts',(211.993410108095,-4.37163704855645,1.21582882286683E-5));
#38091=CARTESIAN_POINT('Ctrl Pts',(212.007088544049,-4.37160047135746,-0.375819472462299));
#38092=CARTESIAN_POINT('Ctrl Pts',(212.047163503689,-4.23106483712903,-1.47695448277203));
#38093=CARTESIAN_POINT('Ctrl Pts',(212.113634987014,-3.31716382083363,-3.1238560826521));
#38094=CARTESIAN_POINT('Ctrl Pts',(212.192824558072,-1.42398215132184,-4.32831693295292));
#38095=CARTESIAN_POINT('Ctrl Pts',(212.272014129129,0.814519648555283,-4.48314737450014));
#38096=CARTESIAN_POINT('Ctrl Pts',(212.351203700187,2.85549788329282,-3.5508005404247));
#38097=CARTESIAN_POINT('Ctrl Pts',(212.430393271244,4.20400894040367,-1.75737345728678));
#38098=CARTESIAN_POINT('Ctrl Pts',(212.509582842302,4.53303466617831,0.462222191803663));
#38099=CARTESIAN_POINT('Ctrl Pts',(212.588772413359,3.76278529189487,2.56972751210507));
#38100=CARTESIAN_POINT('Ctrl Pts',(212.667961984417,2.08004870256613,4.05406586457634));
#38101=CARTESIAN_POINT('Ctrl Pts',(212.747151555475,-0.107106210032759,
4.55528055109042));
#38102=CARTESIAN_POINT('Ctrl Pts',(212.826341126532,-2.2682875313355,3.95182544080049));
#38103=CARTESIAN_POINT('Ctrl Pts',(212.90553069759,-3.87940202399173,2.39004028744685));
#38104=CARTESIAN_POINT('Ctrl Pts',(212.961220358111,-4.35082037023268,0.884127586732209));
#38105=CARTESIAN_POINT('Ctrl Pts',(212.990513494946,-4.37232941023223,0.0796303560494513));
#38106=CARTESIAN_POINT('Ctrl Pts',(212.993410108095,-4.37226510377645,7.52726507913769E-5));
#38107=CARTESIAN_POINT('Ctrl Pts',(212.190589891905,-4.37223174941664,8.43980496762972E-5));
#38108=CARTESIAN_POINT('Ctrl Pts',(212.21362084791,-4.37167547872142,-0.632471629830828));
#38109=CARTESIAN_POINT('Ctrl Pts',(212.263048327602,-4.07369174834855,-1.99052761130526));
#38110=CARTESIAN_POINT('Ctrl Pts',(212.338872330979,-2.71789185781366,-3.65720064579733));
#38111=CARTESIAN_POINT('Ctrl Pts',(212.418061902036,-0.642815370532352,
-4.51096897725948));
#38112=CARTESIAN_POINT('Ctrl Pts',(212.497251473094,1.58814585683998,-4.27081320731686));
#38113=CARTESIAN_POINT('Ctrl Pts',(212.576441044152,3.43397674124133,-2.99497186213889));
#38114=CARTESIAN_POINT('Ctrl Pts',(212.655630615209,4.44705751367238,-0.992840462753262));
#38115=CARTESIAN_POINT('Ctrl Pts',(212.734820186267,4.38171291473348,1.25005785756018));
#38116=CARTESIAN_POINT('Ctrl Pts',(212.814009757324,3.25378921426957,3.18981323332466));
#38117=CARTESIAN_POINT('Ctrl Pts',(212.893199328382,1.33681144131616,4.35602891229573));
#38118=CARTESIAN_POINT('Ctrl Pts',(212.972388899439,-0.904347291883607,
4.46589394075284));
#38119=CARTESIAN_POINT('Ctrl Pts',(213.051578470497,-2.92619897517484,3.4927657052937));
#38120=CARTESIAN_POINT('Ctrl Pts',(213.124312134652,-4.13145831734779,1.82101681823968));
#38121=CARTESIAN_POINT('Ctrl Pts',(213.170649275122,-4.37142245615048,0.547659442705151));
#38122=CARTESIAN_POINT('Ctrl Pts',(213.190589891905,-4.37197391080243,-0.000112134234356263));
#38123=CARTESIAN_POINT('Origin',(207.493410108095,0.,0.));
#38124=CARTESIAN_POINT('',(210.993410108095,-4.37219407540291,-9.26783309010704E-5));
#38125=CARTESIAN_POINT('',(211.190589891905,-4.37163507512868,2.84626229390961E-7));
#38126=CARTESIAN_POINT('',(207.493410108095,-4.372,-3.09002298987926E-13));
#38127=CARTESIAN_POINT('Ctrl Pts',(210.993410108095,-4.37219407540291,-9.26783309011282E-5));
#38128=CARTESIAN_POINT('Ctrl Pts',(210.997267069466,-4.37229343375423,-0.106028573797621));
#38129=CARTESIAN_POINT('Ctrl Pts',(211.027520554523,-4.3427019859007,-0.936920061828269));
#38130=CARTESIAN_POINT('Ctrl Pts',(211.084170563266,-3.83550395069923,-2.45987033873152));
#38131=CARTESIAN_POINT('Ctrl Pts',(211.163360134324,-2.19638331619705,-3.99223658715306));
#38132=CARTESIAN_POINT('Ctrl Pts',(211.242549705381,-0.0246328503458637,
-4.55647296294042));
#38133=CARTESIAN_POINT('Ctrl Pts',(211.321739276439,2.1530911588358,-4.01575037833895));
#38134=CARTESIAN_POINT('Ctrl Pts',(211.400928847496,3.80868382039997,-2.501195753153));
#38135=CARTESIAN_POINT('Ctrl Pts',(211.480118418554,4.54065873004066,-0.380093326269416));
#38136=CARTESIAN_POINT('Ctrl Pts',(211.559307989612,4.17150968026545,1.83318292235754));
#38137=CARTESIAN_POINT('Ctrl Pts',(211.638497560669,2.79075647149654,3.60190657238208));
#38138=CARTESIAN_POINT('Ctrl Pts',(211.717687131727,0.733236080175323,4.4971566005755));
#38139=CARTESIAN_POINT('Ctrl Pts',(211.796876702784,-1.50209635644419,4.30183207195806));
#38140=CARTESIAN_POINT('Ctrl Pts',(211.876066273842,-3.37316572337063,3.06329979630588));
#38141=CARTESIAN_POINT('Ctrl Pts',(211.941577408945,-4.24433544629584,1.42415411441826));
#38142=CARTESIAN_POINT('Ctrl Pts',(211.980692020363,-4.3716710577098,0.349457055968407));
#38143=CARTESIAN_POINT('Ctrl Pts',(211.993410108095,-4.37163704855645,1.21582882286683E-5));
#38144=CARTESIAN_POINT('Ctrl Pts',(211.190589891905,-4.37163507512868,2.84626229390961E-7));
#38145=CARTESIAN_POINT('Ctrl Pts',(211.203799373328,-4.37163424866656,-0.36294672243026));
#38146=CARTESIAN_POINT('Ctrl Pts',(211.243405378436,-4.23761044520356,-1.45117179924369));
#38147=CARTESIAN_POINT('Ctrl Pts',(211.309407907231,-3.34464745971568,-3.09441207414373));
#38148=CARTESIAN_POINT('Ctrl Pts',(211.388597478288,-1.46218654627958,-4.31556059142606));
#38149=CARTESIAN_POINT('Ctrl Pts',(211.467787049346,0.774859182922043,-4.49017215271657));
#38150=CARTESIAN_POINT('Ctrl Pts',(211.546976620403,2.82399913408206,-3.57590290767156));
#38151=CARTESIAN_POINT('Ctrl Pts',(211.626166191461,4.18831045292564,-1.79446601090796));
#38152=CARTESIAN_POINT('Ctrl Pts',(211.705355762519,4.53694337280039,0.42213451220282));
#38153=CARTESIAN_POINT('Ctrl Pts',(211.784545333576,3.78535331902254,2.53636609434741));
#38154=CARTESIAN_POINT('Ctrl Pts',(211.863734904634,2.11580323295756,4.03552095692693));
#38155=CARTESIAN_POINT('Ctrl Pts',(211.942924475691,-0.0668357619494714,
4.55604935172072));
#38156=CARTESIAN_POINT('Ctrl Pts',(212.022114046749,-2.23326687531246,3.97172151315046));
#38157=CARTESIAN_POINT('Ctrl Pts',(212.101303617806,-3.85812377876869,2.42423877167448));
#38158=CARTESIAN_POINT('Ctrl Pts',(212.157462232858,-4.34691686173918,0.909906504712177));
#38159=CARTESIAN_POINT('Ctrl Pts',(212.187224324225,-4.37231303855952,0.0925212957176837));
#38160=CARTESIAN_POINT('Ctrl Pts',(212.190589891905,-4.37223174941664,8.43980496762972E-5));
#38161=CARTESIAN_POINT('Origin',(207.493410108095,0.,0.));
#38162=CARTESIAN_POINT('',(209.993410108095,-4.37201596611874,0.000111980929712991));
#38163=CARTESIAN_POINT('',(210.190589891905,-4.37223008469844,-8.48050595506078E-5));
#38164=CARTESIAN_POINT('',(207.493410108095,-4.372,-3.09002298987926E-13));
#38165=CARTESIAN_POINT('Ctrl Pts',(209.993410108095,-4.37201596611874,0.000111980929712943));
#38166=CARTESIAN_POINT('Ctrl Pts',(210.013842118569,-4.37144249704474,-0.561142687935352));
#38167=CARTESIAN_POINT('Ctrl Pts',(210.06067065273,-4.12266125418189,-1.84798782433965));
#38168=CARTESIAN_POINT('Ctrl Pts',(210.133895710575,-2.89372191923785,-3.5197193599864));
#38169=CARTESIAN_POINT('Ctrl Pts',(210.213085281633,-0.862943537879242,
-4.47407889498736));
#38170=CARTESIAN_POINT('Ctrl Pts',(210.29227485269,1.37710147802978,-4.3434598905811));
#38171=CARTESIAN_POINT('Ctrl Pts',(210.371464423748,3.2831950149358,-3.15953845045613));
#38172=CARTESIAN_POINT('Ctrl Pts',(210.450653994806,4.39310350826522,-1.20941895478298));
#38173=CARTESIAN_POINT('Ctrl Pts',(210.529843565863,4.43767063245068,1.03398838263629));
#38174=CARTESIAN_POINT('Ctrl Pts',(210.609033136921,3.40608873948736,3.02665031932622));
#38175=CARTESIAN_POINT('Ctrl Pts',(210.688222707978,1.54851965941115,4.28534006751519));
#38176=CARTESIAN_POINT('Ctrl Pts',(210.767412279036,-0.68457028532424,4.50482143573546));
#38177=CARTESIAN_POINT('Ctrl Pts',(210.846601850094,-2.75164979303246,3.63186949857032));
#38178=CARTESIAN_POINT('Ctrl Pts',(210.92193445978,-4.08326796574857,1.9635921272198));
#38179=CARTESIAN_POINT('Ctrl Pts',(210.97087054578,-4.37161343859181,0.618982414065456));
#38180=CARTESIAN_POINT('Ctrl Pts',(210.993410108095,-4.37219407540291,-9.26783309011282E-5));
#38181=CARTESIAN_POINT('Ctrl Pts',(210.190589891905,-4.37223008469844,-8.48050595506078E-5));
#38182=CARTESIAN_POINT('Ctrl Pts',(210.193977898745,-4.37231219702262,-0.0931381070659649));
#38183=CARTESIAN_POINT('Ctrl Pts',(210.223762429271,-4.34672717194406,-0.9111400330763));
#38184=CARTESIAN_POINT('Ctrl Pts',(210.279943483483,-3.85709805879303,-2.425870420406));
#38185=CARTESIAN_POINT('Ctrl Pts',(210.35913305454,-2.23158676324473,-3.97266575777209));
#38186=CARTESIAN_POINT('Ctrl Pts',(210.438322625598,-0.0649086922827653,
-4.55607721401773));
#38187=CARTESIAN_POINT('Ctrl Pts',(210.517512196655,2.11750994076351,-4.0346256782917));
#38188=CARTESIAN_POINT('Ctrl Pts',(210.596701767713,3.7864257825248,-2.53476478355335));
#38189=CARTESIAN_POINT('Ctrl Pts',(210.67589133877,4.53712151645643,-0.420215491706979));
#38190=CARTESIAN_POINT('Ctrl Pts',(210.755080909828,4.18755107623993,1.79623737242675));
#38191=CARTESIAN_POINT('Ctrl Pts',(210.834270480885,2.82248638832623,3.57709704959276));
#38192=CARTESIAN_POINT('Ctrl Pts',(210.913460051943,0.77295991365603,4.49049949184098));
#38193=CARTESIAN_POINT('Ctrl Pts',(210.992649623001,-1.46401176030129,4.31494174701186));
#38194=CARTESIAN_POINT('Ctrl Pts',(211.071839194058,-3.34595599838294,3.09299711788944));
#38195=CARTESIAN_POINT('Ctrl Pts',(211.137819283693,-4.23792051755099,1.44993808277174));
#38196=CARTESIAN_POINT('Ctrl Pts',(211.177402849642,-4.37163590018688,0.362330747734179));
#38197=CARTESIAN_POINT('Ctrl Pts',(211.190589891905,-4.37163507512868,2.84626229390961E-7));
#38198=CARTESIAN_POINT('Origin',(227.75,0.85,3.75));
#38199=CARTESIAN_POINT('',(227.6,0.699999999999996,-6.96491205974634));
#38200=CARTESIAN_POINT('',(228.,1.1,-6.50768776140958));
#38201=CARTESIAN_POINT('Ctrl Pts',(227.6,0.69999999999998,-6.96491205974636));
#38202=CARTESIAN_POINT('Ctrl Pts',(227.806787469448,0.906787469447637,-6.73629991057805));
#38203=CARTESIAN_POINT('Ctrl Pts',(228.,1.09999999999999,-6.5076877614096));
#38204=CARTESIAN_POINT('',(228.,1.1,6.50768776140958));
#38205=CARTESIAN_POINT('',(228.,1.1,3.75));
#38206=CARTESIAN_POINT('',(227.6,0.699999999999996,6.96491205974634));
#38207=CARTESIAN_POINT('Ctrl Pts',(228.,1.09999999999999,6.5076877614096));
#38208=CARTESIAN_POINT('Ctrl Pts',(227.806787469448,0.906787469447637,6.73629991057805));
#38209=CARTESIAN_POINT('Ctrl Pts',(227.6,0.69999999999998,6.96491205974636));
#38210=CARTESIAN_POINT('',(227.5,0.6,6.97423830966508));
#38211=CARTESIAN_POINT('Origin',(226.9,0.,0.));
#38212=CARTESIAN_POINT('',(227.5,0.6,-6.97423830966508));
#38213=CARTESIAN_POINT('',(227.5,0.6,3.75));
#38214=CARTESIAN_POINT('Origin',(226.9,0.,0.));
#38215=CARTESIAN_POINT('Origin',(228.,0.,0.));
#38216=CARTESIAN_POINT('Origin',(228.,0.,0.));
#38217=CARTESIAN_POINT('Origin',(227.75,-0.85,-3.75));
#38218=CARTESIAN_POINT('',(227.6,-0.699999999999996,6.96491205974634));
#38219=CARTESIAN_POINT('',(228.,-1.1,6.50768776140958));
#38220=CARTESIAN_POINT('Ctrl Pts',(227.6,-0.69999999999998,6.96491205974636));
#38221=CARTESIAN_POINT('Ctrl Pts',(227.806787469448,-0.906787469447637,
6.73629991057805));
#38222=CARTESIAN_POINT('Ctrl Pts',(228.,-1.09999999999999,6.5076877614096));
#38223=CARTESIAN_POINT('',(228.,-1.1,-6.50768776140958));
#38224=CARTESIAN_POINT('',(228.,-1.1,-3.75));
#38225=CARTESIAN_POINT('',(227.6,-0.699999999999996,-6.96491205974634));
#38226=CARTESIAN_POINT('Ctrl Pts',(228.,-1.09999999999999,-6.5076877614096));
#38227=CARTESIAN_POINT('Ctrl Pts',(227.806787469448,-0.906787469447637,
-6.73629991057805));
#38228=CARTESIAN_POINT('Ctrl Pts',(227.6,-0.69999999999998,-6.96491205974636));
#38229=CARTESIAN_POINT('',(227.5,-0.6,-6.97423830966508));
#38230=CARTESIAN_POINT('Origin',(226.9,0.,0.));
#38231=CARTESIAN_POINT('',(227.5,-0.6,6.97423830966508));
#38232=CARTESIAN_POINT('',(227.5,-0.6,-3.75));
#38233=CARTESIAN_POINT('Origin',(226.9,0.,0.));
#38234=CARTESIAN_POINT('Origin',(225.,0.,0.));
#38235=CARTESIAN_POINT('Origin',(227.6,0.,0.));
#38236=CARTESIAN_POINT('',(226.2,0.6,-6.97423830966508));
#38237=CARTESIAN_POINT('',(225.,0.6,-6.97423830966508));
#38238=CARTESIAN_POINT('',(226.2,0.197221149720988,-6.99722114972099));
#38239=CARTESIAN_POINT('Origin',(226.2,0.,0.));
#38240=CARTESIAN_POINT('',(222.5,0.197221149720988,-6.99722114972099));
#38241=CARTESIAN_POINT('',(225.,0.197221149720988,-6.99722114972099));
#38242=CARTESIAN_POINT('',(222.5,-0.19722114972099,-6.99722114972099));
#38243=CARTESIAN_POINT('Origin',(222.5,0.,0.));
#38244=CARTESIAN_POINT('',(226.2,-0.19722114972099,-6.99722114972099));
#38245=CARTESIAN_POINT('',(225.,-0.19722114972099,-6.99722114972099));
#38246=CARTESIAN_POINT('',(226.2,-0.6,-6.97423830966508));
#38247=CARTESIAN_POINT('Origin',(226.2,0.,0.));
#38248=CARTESIAN_POINT('',(225.,-0.6,-6.97423830966508));
#38249=CARTESIAN_POINT('',(227.6,-7.,-8.57252759403147E-16));
#38250=CARTESIAN_POINT('Origin',(227.6,0.,0.));
#38251=CARTESIAN_POINT('',(227.5,-7.,-8.57252759403147E-16));
#38252=CARTESIAN_POINT('',(225.,-7.,-8.57252759403147E-16));
#38253=CARTESIAN_POINT('',(227.5,-6.99722114972099,-0.197221149720988));
#38254=CARTESIAN_POINT('Origin',(227.5,0.,0.));
#38255=CARTESIAN_POINT('',(222.5,-6.99722114972099,-0.197221149720988));
#38256=CARTESIAN_POINT('',(225.,-6.99722114972099,-0.197221149720988));
#38257=CARTESIAN_POINT('',(222.5,-7.,-8.57252759403147E-16));
#38258=CARTESIAN_POINT('Origin',(222.5,0.,0.));
#38259=CARTESIAN_POINT('',(222.4,-7.,-8.57252759403147E-16));
#38260=CARTESIAN_POINT('',(225.,-7.,-8.57252759403147E-16));
#38261=CARTESIAN_POINT('Origin',(222.4,0.,0.));
#38262=CARTESIAN_POINT('',(222.5,-6.99722114972099,0.19722114972099));
#38263=CARTESIAN_POINT('Origin',(222.5,0.,0.));
#38264=CARTESIAN_POINT('',(227.5,-6.99722114972099,0.19722114972099));
#38265=CARTESIAN_POINT('',(225.,-6.99722114972099,0.19722114972099));
#38266=CARTESIAN_POINT('Origin',(227.5,0.,0.));
#38267=CARTESIAN_POINT('Origin',(227.6,0.,0.));
#38268=CARTESIAN_POINT('',(226.2,-0.6,6.97423830966508));
#38269=CARTESIAN_POINT('',(225.,-0.6,6.97423830966508));
#38270=CARTESIAN_POINT('',(226.2,-0.197221149720991,6.99722114972099));
#38271=CARTESIAN_POINT('Origin',(226.2,0.,0.));
#38272=CARTESIAN_POINT('',(222.5,-0.197221149720991,6.99722114972099));
#38273=CARTESIAN_POINT('',(225.,-0.197221149720991,6.99722114972099));
#38274=CARTESIAN_POINT('',(222.5,0.197221149720991,6.99722114972099));
#38275=CARTESIAN_POINT('Origin',(222.5,0.,0.));
#38276=CARTESIAN_POINT('',(226.2,0.197221149720991,6.99722114972099));
#38277=CARTESIAN_POINT('',(225.,0.197221149720991,6.99722114972099));
#38278=CARTESIAN_POINT('',(226.2,0.6,6.97423830966508));
#38279=CARTESIAN_POINT('Origin',(226.2,0.,0.));
#38280=CARTESIAN_POINT('',(225.,0.6,6.97423830966508));
#38281=CARTESIAN_POINT('',(222.5,6.99722114972099,-0.19722114972099));
#38282=CARTESIAN_POINT('',(227.5,6.99722114972099,-0.19722114972099));
#38283=CARTESIAN_POINT('',(225.,6.99722114972099,-0.19722114972099));
#38284=CARTESIAN_POINT('',(227.5,6.99722114972099,0.197221149720991));
#38285=CARTESIAN_POINT('Origin',(227.5,0.,0.));
#38286=CARTESIAN_POINT('',(222.5,6.99722114972099,0.197221149720991));
#38287=CARTESIAN_POINT('',(225.,6.99722114972099,0.197221149720991));
#38288=CARTESIAN_POINT('Origin',(222.5,0.,0.));
#38289=CARTESIAN_POINT('',(222.5,6.8098412104164,1.62051309433602));
#38290=CARTESIAN_POINT('',(227.5,6.8098412104164,1.62051309433602));
#38291=CARTESIAN_POINT('',(225.,6.8098412104164,1.62051309433602));
#38292=CARTESIAN_POINT('',(227.5,6.70775203112678,2.00151509834788));
#38293=CARTESIAN_POINT('Origin',(227.5,0.,0.));
#38294=CARTESIAN_POINT('',(222.5,6.70775203112678,2.00151509834788));
#38295=CARTESIAN_POINT('',(225.,6.70775203112678,2.00151509834787));
#38296=CARTESIAN_POINT('Origin',(222.5,0.,0.));
#38297=CARTESIAN_POINT('',(222.5,6.15838184641663,3.32781204903854));
#38298=CARTESIAN_POINT('',(227.5,6.15838184641663,3.32781204903854));
#38299=CARTESIAN_POINT('',(225.,6.15838184641663,3.32781204903854));
#38300=CARTESIAN_POINT('',(227.5,5.96116069669564,3.66940910068244));
#38301=CARTESIAN_POINT('Origin',(227.5,0.,0.));
#38302=CARTESIAN_POINT('',(222.5,5.96116069669564,3.66940910068244));
#38303=CARTESIAN_POINT('',(225.,5.96116069669564,3.66940910068244));
#38304=CARTESIAN_POINT('Origin',(222.5,0.,0.));
#38305=CARTESIAN_POINT('',(222.5,5.08723893679076,4.80832611206852));
#38306=CARTESIAN_POINT('',(227.5,5.08723893679076,4.80832611206852));
#38307=CARTESIAN_POINT('',(225.,5.08723893679076,4.80832611206852));
#38308=CARTESIAN_POINT('',(227.5,4.80832611206852,5.08723893679076));
#38309=CARTESIAN_POINT('Origin',(227.5,0.,0.));
#38310=CARTESIAN_POINT('',(222.5,4.80832611206852,5.08723893679076));
#38311=CARTESIAN_POINT('',(225.,4.80832611206852,5.08723893679076));
#38312=CARTESIAN_POINT('Origin',(222.5,0.,0.));
#38313=CARTESIAN_POINT('',(222.5,3.66940910068245,5.96116069669564));
#38314=CARTESIAN_POINT('',(227.5,3.66940910068245,5.96116069669564));
#38315=CARTESIAN_POINT('',(225.,3.66940910068245,5.96116069669564));
#38316=CARTESIAN_POINT('',(227.5,3.32781204903854,6.15838184641663));
#38317=CARTESIAN_POINT('Origin',(227.5,0.,0.));
#38318=CARTESIAN_POINT('',(222.5,3.32781204903854,6.15838184641663));
#38319=CARTESIAN_POINT('',(225.,3.32781204903854,6.15838184641663));
#38320=CARTESIAN_POINT('Origin',(222.5,0.,0.));
#38321=CARTESIAN_POINT('',(222.5,2.00151509834788,6.70775203112678));
#38322=CARTESIAN_POINT('',(227.5,2.00151509834788,6.70775203112678));
#38323=CARTESIAN_POINT('',(225.,2.00151509834788,6.70775203112678));
#38324=CARTESIAN_POINT('',(227.5,1.62051309433602,6.8098412104164));
#38325=CARTESIAN_POINT('Origin',(227.5,0.,0.));
#38326=CARTESIAN_POINT('',(222.5,1.62051309433602,6.8098412104164));
#38327=CARTESIAN_POINT('',(225.,1.62051309433602,6.8098412104164));
#38328=CARTESIAN_POINT('Origin',(222.5,0.,0.));
#38329=CARTESIAN_POINT('',(222.5,-1.62051309433602,6.8098412104164));
#38330=CARTESIAN_POINT('',(227.5,-1.62051309433602,6.8098412104164));
#38331=CARTESIAN_POINT('',(225.,-1.62051309433602,6.8098412104164));
#38332=CARTESIAN_POINT('',(227.5,-2.00151509834787,6.70775203112678));
#38333=CARTESIAN_POINT('Origin',(227.5,0.,0.));
#38334=CARTESIAN_POINT('',(222.5,-2.00151509834787,6.70775203112678));
#38335=CARTESIAN_POINT('',(225.,-2.00151509834787,6.70775203112678));
#38336=CARTESIAN_POINT('Origin',(222.5,0.,0.));
#38337=CARTESIAN_POINT('',(222.5,-3.32781204903854,6.15838184641663));
#38338=CARTESIAN_POINT('',(227.5,-3.32781204903854,6.15838184641663));
#38339=CARTESIAN_POINT('',(225.,-3.32781204903854,6.15838184641663));
#38340=CARTESIAN_POINT('',(227.5,-3.66940910068244,5.96116069669564));
#38341=CARTESIAN_POINT('Origin',(227.5,0.,0.));
#38342=CARTESIAN_POINT('',(222.5,-3.66940910068244,5.96116069669564));
#38343=CARTESIAN_POINT('',(225.,-3.66940910068244,5.96116069669564));
#38344=CARTESIAN_POINT('Origin',(222.5,0.,0.));
#38345=CARTESIAN_POINT('',(222.5,-4.80832611206852,5.08723893679076));
#38346=CARTESIAN_POINT('',(227.5,-4.80832611206852,5.08723893679076));
#38347=CARTESIAN_POINT('',(225.,-4.80832611206852,5.08723893679076));
#38348=CARTESIAN_POINT('',(227.5,-5.08723893679076,4.80832611206852));
#38349=CARTESIAN_POINT('Origin',(227.5,0.,0.));
#38350=CARTESIAN_POINT('',(222.5,-5.08723893679076,4.80832611206852));
#38351=CARTESIAN_POINT('',(225.,-5.08723893679076,4.80832611206852));
#38352=CARTESIAN_POINT('Origin',(222.5,0.,0.));
#38353=CARTESIAN_POINT('',(222.5,-5.96116069669564,3.66940910068245));
#38354=CARTESIAN_POINT('',(227.5,-5.96116069669564,3.66940910068245));
#38355=CARTESIAN_POINT('',(225.,-5.96116069669564,3.66940910068245));
#38356=CARTESIAN_POINT('',(227.5,-6.15838184641663,3.32781204903855));
#38357=CARTESIAN_POINT('Origin',(227.5,0.,0.));
#38358=CARTESIAN_POINT('',(222.5,-6.15838184641663,3.32781204903855));
#38359=CARTESIAN_POINT('',(225.,-6.15838184641663,3.32781204903855));
#38360=CARTESIAN_POINT('Origin',(222.5,0.,0.));
#38361=CARTESIAN_POINT('',(222.5,-6.70775203112678,2.00151509834788));
#38362=CARTESIAN_POINT('',(227.5,-6.70775203112678,2.00151509834788));
#38363=CARTESIAN_POINT('',(225.,-6.70775203112678,2.00151509834788));
#38364=CARTESIAN_POINT('',(227.5,-6.8098412104164,1.62051309433602));
#38365=CARTESIAN_POINT('Origin',(227.5,0.,0.));
#38366=CARTESIAN_POINT('',(222.5,-6.8098412104164,1.62051309433602));
#38367=CARTESIAN_POINT('',(225.,-6.8098412104164,1.62051309433602));
#38368=CARTESIAN_POINT('Origin',(222.5,0.,0.));
#38369=CARTESIAN_POINT('',(222.5,-6.8098412104164,-1.62051309433602));
#38370=CARTESIAN_POINT('',(227.5,-6.8098412104164,-1.62051309433602));
#38371=CARTESIAN_POINT('',(225.,-6.8098412104164,-1.62051309433602));
#38372=CARTESIAN_POINT('',(227.5,-6.70775203112678,-2.00151509834787));
#38373=CARTESIAN_POINT('Origin',(227.5,0.,0.));
#38374=CARTESIAN_POINT('',(222.5,-6.70775203112678,-2.00151509834787));
#38375=CARTESIAN_POINT('',(225.,-6.70775203112678,-2.00151509834787));
#38376=CARTESIAN_POINT('Origin',(222.5,0.,0.));
#38377=CARTESIAN_POINT('',(222.5,-6.15838184641663,-3.32781204903854));
#38378=CARTESIAN_POINT('',(227.5,-6.15838184641663,-3.32781204903854));
#38379=CARTESIAN_POINT('',(225.,-6.15838184641663,-3.32781204903854));
#38380=CARTESIAN_POINT('',(227.5,-5.96116069669564,-3.66940910068244));
#38381=CARTESIAN_POINT('Origin',(227.5,0.,0.));
#38382=CARTESIAN_POINT('',(222.5,-5.96116069669564,-3.66940910068244));
#38383=CARTESIAN_POINT('',(225.,-5.96116069669564,-3.66940910068244));
#38384=CARTESIAN_POINT('Origin',(222.5,0.,0.));
#38385=CARTESIAN_POINT('',(222.5,-5.08723893679076,-4.80832611206852));
#38386=CARTESIAN_POINT('',(227.5,-5.08723893679076,-4.80832611206852));
#38387=CARTESIAN_POINT('',(225.,-5.08723893679076,-4.80832611206852));
#38388=CARTESIAN_POINT('',(227.5,-4.80832611206853,-5.08723893679076));
#38389=CARTESIAN_POINT('Origin',(227.5,0.,0.));
#38390=CARTESIAN_POINT('',(222.5,-4.80832611206853,-5.08723893679076));
#38391=CARTESIAN_POINT('',(225.,-4.80832611206853,-5.08723893679076));
#38392=CARTESIAN_POINT('Origin',(222.5,0.,0.));
#38393=CARTESIAN_POINT('',(222.5,-3.66940910068245,-5.96116069669564));
#38394=CARTESIAN_POINT('',(227.5,-3.66940910068245,-5.96116069669564));
#38395=CARTESIAN_POINT('',(225.,-3.66940910068245,-5.96116069669564));
#38396=CARTESIAN_POINT('',(227.5,-3.32781204903855,-6.15838184641663));
#38397=CARTESIAN_POINT('Origin',(227.5,0.,0.));
#38398=CARTESIAN_POINT('',(222.5,-3.32781204903855,-6.15838184641663));
#38399=CARTESIAN_POINT('',(225.,-3.32781204903855,-6.15838184641663));
#38400=CARTESIAN_POINT('Origin',(222.5,0.,0.));
#38401=CARTESIAN_POINT('',(222.5,-2.00151509834788,-6.70775203112678));
#38402=CARTESIAN_POINT('',(227.5,-2.00151509834788,-6.70775203112678));
#38403=CARTESIAN_POINT('',(225.,-2.00151509834788,-6.70775203112678));
#38404=CARTESIAN_POINT('',(227.5,-1.62051309433603,-6.8098412104164));
#38405=CARTESIAN_POINT('Origin',(227.5,0.,0.));
#38406=CARTESIAN_POINT('',(222.5,-1.62051309433603,-6.8098412104164));
#38407=CARTESIAN_POINT('',(225.,-1.62051309433603,-6.8098412104164));
#38408=CARTESIAN_POINT('Origin',(222.5,0.,0.));
#38409=CARTESIAN_POINT('',(222.5,1.62051309433602,-6.8098412104164));
#38410=CARTESIAN_POINT('',(227.5,1.62051309433602,-6.8098412104164));
#38411=CARTESIAN_POINT('',(225.,1.62051309433602,-6.8098412104164));
#38412=CARTESIAN_POINT('',(227.5,2.00151509834787,-6.70775203112678));
#38413=CARTESIAN_POINT('Origin',(227.5,0.,0.));
#38414=CARTESIAN_POINT('',(222.5,2.00151509834787,-6.70775203112678));
#38415=CARTESIAN_POINT('',(225.,2.00151509834787,-6.70775203112678));
#38416=CARTESIAN_POINT('Origin',(222.5,0.,0.));
#38417=CARTESIAN_POINT('',(222.5,3.32781204903854,-6.15838184641663));
#38418=CARTESIAN_POINT('',(227.5,3.32781204903854,-6.15838184641663));
#38419=CARTESIAN_POINT('',(225.,3.32781204903854,-6.15838184641663));
#38420=CARTESIAN_POINT('',(227.5,3.66940910068244,-5.96116069669564));
#38421=CARTESIAN_POINT('Origin',(227.5,0.,0.));
#38422=CARTESIAN_POINT('',(222.5,3.66940910068244,-5.96116069669564));
#38423=CARTESIAN_POINT('',(225.,3.66940910068244,-5.96116069669564));
#38424=CARTESIAN_POINT('Origin',(222.5,0.,0.));
#38425=CARTESIAN_POINT('',(222.5,4.80832611206852,-5.08723893679076));
#38426=CARTESIAN_POINT('',(227.5,4.80832611206852,-5.08723893679076));
#38427=CARTESIAN_POINT('',(225.,4.80832611206852,-5.08723893679076));
#38428=CARTESIAN_POINT('',(227.5,5.08723893679076,-4.80832611206852));
#38429=CARTESIAN_POINT('Origin',(227.5,0.,0.));
#38430=CARTESIAN_POINT('',(222.5,5.08723893679076,-4.80832611206852));
#38431=CARTESIAN_POINT('',(225.,5.08723893679076,-4.80832611206852));
#38432=CARTESIAN_POINT('Origin',(222.5,0.,0.));
#38433=CARTESIAN_POINT('',(222.5,5.96116069669564,-3.66940910068245));
#38434=CARTESIAN_POINT('',(227.5,5.96116069669564,-3.66940910068245));
#38435=CARTESIAN_POINT('',(225.,5.96116069669564,-3.66940910068245));
#38436=CARTESIAN_POINT('',(227.5,6.15838184641663,-3.32781204903855));
#38437=CARTESIAN_POINT('Origin',(227.5,0.,0.));
#38438=CARTESIAN_POINT('',(222.5,6.15838184641663,-3.32781204903855));
#38439=CARTESIAN_POINT('',(225.,6.15838184641663,-3.32781204903855));
#38440=CARTESIAN_POINT('Origin',(222.5,0.,0.));
#38441=CARTESIAN_POINT('',(222.5,6.70775203112678,-2.00151509834788));
#38442=CARTESIAN_POINT('',(227.5,6.70775203112678,-2.00151509834788));
#38443=CARTESIAN_POINT('',(225.,6.70775203112678,-2.00151509834788));
#38444=CARTESIAN_POINT('',(227.5,6.8098412104164,-1.62051309433603));
#38445=CARTESIAN_POINT('Origin',(227.5,0.,0.));
#38446=CARTESIAN_POINT('',(222.5,6.8098412104164,-1.62051309433603));
#38447=CARTESIAN_POINT('',(225.,6.8098412104164,-1.62051309433603));
#38448=CARTESIAN_POINT('Origin',(222.5,0.,0.));
#38449=CARTESIAN_POINT('Origin',(227.8,0.,0.));
#38450=CARTESIAN_POINT('Origin',(228.,0.,0.));
#38451=CARTESIAN_POINT('Origin',(228.,0.,0.));
#38452=CARTESIAN_POINT('Ctrl Pts',(209.012910346562,-1.91898364243922,3.92834389788505));
#38453=CARTESIAN_POINT('Ctrl Pts',(209.039306870248,-2.57051617251472,3.61007230552139));
#38454=CARTESIAN_POINT('Ctrl Pts',(209.092099917619,-3.7114647271083,2.64329361995669));
#38455=CARTESIAN_POINT('Ctrl Pts',(209.171289488677,-4.52311191657194,0.551127705008165));
#38456=CARTESIAN_POINT('Ctrl Pts',(209.250479059734,-4.23771212707877,-1.67438902528095));
#38457=CARTESIAN_POINT('Ctrl Pts',(209.329668630792,-2.92472974788555,-3.4940198648462));
#38458=CARTESIAN_POINT('Ctrl Pts',(209.40885820185,-0.90245430475216,-4.4662682355186));
#38459=CARTESIAN_POINT('Ctrl Pts',(209.488047772907,1.33865191662591,-4.35546678832985));
#38460=CARTESIAN_POINT('Ctrl Pts',(209.567237343965,3.25513899273275,-3.1884349607263));
#38461=CARTESIAN_POINT('Ctrl Pts',(209.646426915022,4.38224084314362,-1.24820523943406));
#38462=CARTESIAN_POINT('Ctrl Pts',(209.72561648608,4.4466373711158,0.994721723380339));
#38463=CARTESIAN_POINT('Ctrl Pts',(209.804806057137,3.43270956435134,2.99642387551628));
#38464=CARTESIAN_POINT('Ctrl Pts',(209.883995628195,1.58633933997099,4.27148464599025));
#38465=CARTESIAN_POINT('Ctrl Pts',(209.963185199253,-0.644723329766792,
4.51069664301433));
#38466=CARTESIAN_POINT('Ctrl Pts',(210.04237477031,-2.71943848460081,3.6560507558529));
#38467=CARTESIAN_POINT('Ctrl Pts',(210.121564341368,-4.1346813337972,1.91480103026804));
#38468=CARTESIAN_POINT('Ctrl Pts',(210.200753912425,-4.54725099365243,-0.29079390175578));
#38469=CARTESIAN_POINT('Ctrl Pts',(210.279943483483,-3.85709805879303,-2.425870420406));
#38470=CARTESIAN_POINT('Ctrl Pts',(210.35913305454,-2.23158676324473,-3.97266575777209));
#38471=CARTESIAN_POINT('Ctrl Pts',(210.438322625598,-0.0649086922827653,
-4.55607721401773));
#38472=CARTESIAN_POINT('Ctrl Pts',(210.517512196655,2.11750994076351,-4.0346256782917));
#38473=CARTESIAN_POINT('Ctrl Pts',(210.596701767713,3.7864257825248,-2.53476478355335));
#38474=CARTESIAN_POINT('Ctrl Pts',(210.67589133877,4.53712151645643,-0.420215491706979));
#38475=CARTESIAN_POINT('Ctrl Pts',(210.755080909828,4.18755107623993,1.79623737242675));
#38476=CARTESIAN_POINT('Ctrl Pts',(210.834270480885,2.82248638832623,3.57709704959276));
#38477=CARTESIAN_POINT('Ctrl Pts',(210.913460051943,0.77295991365603,4.49049949184098));
#38478=CARTESIAN_POINT('Ctrl Pts',(210.992649623001,-1.46401176030129,4.31494174701186));
#38479=CARTESIAN_POINT('Ctrl Pts',(211.071839194058,-3.34595599838294,3.09299711788944));
#38480=CARTESIAN_POINT('Ctrl Pts',(211.151028765116,-4.41649543023929,1.12099100311488));
#38481=CARTESIAN_POINT('Ctrl Pts',(211.230218336173,-4.41602089165307,-1.12285893988305));
#38482=CARTESIAN_POINT('Ctrl Pts',(211.309407907231,-3.34464745971568,-3.09441207414373));
#38483=CARTESIAN_POINT('Ctrl Pts',(211.388597478288,-1.46218654627958,-4.31556059142606));
#38484=CARTESIAN_POINT('Ctrl Pts',(211.467787049346,0.774859182922043,-4.49017215271657));
#38485=CARTESIAN_POINT('Ctrl Pts',(211.546976620403,2.82399913408206,-3.57590290767156));
#38486=CARTESIAN_POINT('Ctrl Pts',(211.626166191461,4.18831045292564,-1.79446601090796));
#38487=CARTESIAN_POINT('Ctrl Pts',(211.705355762519,4.53694337280039,0.42213451220282));
#38488=CARTESIAN_POINT('Ctrl Pts',(211.784545333576,3.78535331902254,2.53636609434741));
#38489=CARTESIAN_POINT('Ctrl Pts',(211.863734904634,2.11580323295756,4.03552095692693));
#38490=CARTESIAN_POINT('Ctrl Pts',(211.942924475691,-0.0668357619494714,
4.55604935172072));
#38491=CARTESIAN_POINT('Ctrl Pts',(212.022114046749,-2.23326687531246,3.97172151315046));
#38492=CARTESIAN_POINT('Ctrl Pts',(212.101303617806,-3.85812377876869,2.42423877167448));
#38493=CARTESIAN_POINT('Ctrl Pts',(212.180493188864,-4.54737358559575,0.28887053746655));
#38494=CARTESIAN_POINT('Ctrl Pts',(212.259682759921,-4.133871059509,-1.91654970656751));
#38495=CARTESIAN_POINT('Ctrl Pts',(212.338872330979,-2.71789185781366,-3.65720064579733));
#38496=CARTESIAN_POINT('Ctrl Pts',(212.418061902036,-0.642815370532352,
-4.51096897725948));
#38497=CARTESIAN_POINT('Ctrl Pts',(212.497251473094,1.58814585683998,-4.27081320731686));
#38498=CARTESIAN_POINT('Ctrl Pts',(212.576441044152,3.43397674124133,-2.99497186213889));
#38499=CARTESIAN_POINT('Ctrl Pts',(212.655630615209,4.44705751367238,-0.992840462753262));
#38500=CARTESIAN_POINT('Ctrl Pts',(212.734820186267,4.38171291473348,1.25005785756018));
#38501=CARTESIAN_POINT('Ctrl Pts',(212.814009757324,3.25378921426957,3.18981323332466));
#38502=CARTESIAN_POINT('Ctrl Pts',(212.893199328382,1.33681144131616,4.35602891229573));
#38503=CARTESIAN_POINT('Ctrl Pts',(212.972388899439,-0.904347291883607,
4.46589394075284));
#38504=CARTESIAN_POINT('Ctrl Pts',(213.051578470497,-2.92619897517484,3.4927657052937));
#38505=CARTESIAN_POINT('Ctrl Pts',(213.130768041554,-4.23843824468386,1.67263085000584));
#38506=CARTESIAN_POINT('Ctrl Pts',(213.209957612612,-4.5228429687662,-0.553122223629014));
#38507=CARTESIAN_POINT('Ctrl Pts',(213.28914718367,-3.71044411132438,-2.6447414261376));
#38508=CARTESIAN_POINT('Ctrl Pts',(213.368336754727,-1.99825093901252,-4.09500255178501));
#38509=CARTESIAN_POINT('Ctrl Pts',(213.447526325785,0.198524342788504,-4.55221273664913));
#38510=CARTESIAN_POINT('Ctrl Pts',(213.526715896842,2.34715684985826,-3.90549707931699));
#38511=CARTESIAN_POINT('Ctrl Pts',(213.6059054679,3.92659647158984,-2.31168615164089));
#38512=CARTESIAN_POINT('Ctrl Pts',(213.685095038957,4.55382415428641,-0.157284094007629));
#38513=CARTESIAN_POINT('Ctrl Pts',(213.764284610015,4.07673522096414,2.03525984889906));
#38514=CARTESIAN_POINT('Ctrl Pts',(213.843474181072,2.61102523177998,3.7342469057895));
#38515=CARTESIAN_POINT('Ctrl Pts',(213.92266375213,0.512133448436073,4.5276673956225));
#38516=CARTESIAN_POINT('Ctrl Pts',(214.001853323188,-1.71095229970873,4.22311436531282));
#38517=CARTESIAN_POINT('Ctrl Pts',(214.081042894245,-3.51912675796424,2.89444287830494));
#38518=CARTESIAN_POINT('Ctrl Pts',(214.160232465302,-4.4739019585786,0.863859930438193));
#38519=CARTESIAN_POINT('Ctrl Pts',(214.23942203636,-4.34374192587985,-1.37621175541547));
#38520=CARTESIAN_POINT('Ctrl Pts',(214.318611607418,-3.16021087534511,-3.28254778148629));
#38521=CARTESIAN_POINT('Ctrl Pts',(214.397801178475,-1.21031879251578,-4.39285569247082));
#38522=CARTESIAN_POINT('Ctrl Pts',(214.476990749533,1.03307938716119,-4.43788234343958));
#38523=CARTESIAN_POINT('Ctrl Pts',(214.55618032059,3.02595258074822,-3.40670863054845));
#38524=CARTESIAN_POINT('Ctrl Pts',(214.635369891648,4.28502279886023,-1.54939740790998));
#38525=CARTESIAN_POINT('Ctrl Pts',(214.714559462705,4.50496157129557,0.683647537507614));
#38526=CARTESIAN_POINT('Ctrl Pts',(214.793749033763,3.63243305708234,2.75090581449194));
#38527=CARTESIAN_POINT('Ctrl Pts',(214.872938604821,1.87902815291533,4.15106081802492));
#38528=CARTESIAN_POINT('Ctrl Pts',(214.952128175878,-0.330046961810515,
4.54457057568587));
#38529=CARTESIAN_POINT('Ctrl Pts',(215.031317746936,-2.45908465487818,3.83600773911274));
#38530=CARTESIAN_POINT('Ctrl Pts',(215.110507317993,-3.99178661943011,2.19720101477514));
#38531=CARTESIAN_POINT('Ctrl Pts',(215.189696889051,-4.55646782997706,0.0255661646378894));
#38532=CARTESIAN_POINT('Ctrl Pts',(215.268886460108,-4.0161913248725,-2.15226856047496));
#38533=CARTESIAN_POINT('Ctrl Pts',(215.348076031166,-2.50197584827897,-3.8081714206452));
#38534=CARTESIAN_POINT('Ctrl Pts',(215.427265602223,-0.381023394472204,
-4.54058078743843));
#38535=CARTESIAN_POINT('Ctrl Pts',(215.506455173281,1.83232842552693,-4.17188509614013));
#38536=CARTESIAN_POINT('Ctrl Pts',(215.585644744338,3.60133486508171,-2.79149420632338));
#38537=CARTESIAN_POINT('Ctrl Pts',(215.664834315396,4.49700632361528,-0.734157230948736));
#38538=CARTESIAN_POINT('Ctrl Pts',(215.744023886454,4.30213966797164,1.50121517167094));
#38539=CARTESIAN_POINT('Ctrl Pts',(215.823213457511,3.06399067229672,3.3725381946642));
#38540=CARTESIAN_POINT('Ctrl Pts',(215.902403028569,1.08281434484414,4.42601014560404));
#38541=CARTESIAN_POINT('Ctrl Pts',(215.981592599626,-1.16094785166298,4.40616077783247));
#38542=CARTESIAN_POINT('Ctrl Pts',(216.060782170684,-3.12317655906599,3.31780362518501));
#38543=CARTESIAN_POINT('Ctrl Pts',(216.139971741741,-4.32802517183125,1.42486870496378));
#38544=CARTESIAN_POINT('Ctrl Pts',(216.219161312799,-4.48331412882848,-0.813601337656876));
#38545=CARTESIAN_POINT('Ctrl Pts',(216.298350883856,-3.55138537175629,-2.85477050840615));
#38546=CARTESIAN_POINT('Ctrl Pts',(216.377540454914,-1.75823454219255,-4.20364889221627));
#38547=CARTESIAN_POINT('Ctrl Pts',(216.456730025972,0.46129366910955,-4.53312925750298));
#38548=CARTESIAN_POINT('Ctrl Pts',(216.535919597029,2.56895672128326,-3.76331158403921));
#38549=CARTESIAN_POINT('Ctrl Pts',(216.615109168087,4.05363972481456,-2.08087906803723));
#38550=CARTESIAN_POINT('Ctrl Pts',(216.694298739144,4.55530240261518,0.106173137461614));
#38551=CARTESIAN_POINT('Ctrl Pts',(216.773488310202,3.95228998454865,2.26747802468437));
#38552=CARTESIAN_POINT('Ctrl Pts',(216.852677881259,2.39083487010492,3.87891239115818));
#38553=CARTESIAN_POINT('Ctrl Pts',(216.931867452317,0.249594813651761,4.5496983574066));
#38554=CARTESIAN_POINT('Ctrl Pts',(217.011057023374,-1.95217276662517,4.11716822629792));
#38555=CARTESIAN_POINT('Ctrl Pts',(217.090246594432,-3.68053233849351,2.68621190893303));
#38556=CARTESIAN_POINT('Ctrl Pts',(217.16943616549,-4.51635129406087,0.603840792779706));
#38557=CARTESIAN_POINT('Ctrl Pts',(217.248625736547,-4.2569409195464,-1.62496360632525));
#38558=CARTESIAN_POINT('Ctrl Pts',(217.327815307605,-2.96520904301682,-3.45970924292799));
#38559=CARTESIAN_POINT('Ctrl Pts',(217.407004878662,-0.954404689107857,
-4.45546455532968));
#38560=CARTESIAN_POINT('Ctrl Pts',(217.48619444972,1.28784579027261,-4.37075576243597));
#38561=CARTESIAN_POINT('Ctrl Pts',(217.565384020777,3.21778963310249,-3.22612501175764));
#38562=CARTESIAN_POINT('Ctrl Pts',(217.644573591835,4.36740941459516,-1.2991488443191));
#38563=CARTESIAN_POINT('Ctrl Pts',(217.723763162892,4.45791873813246,0.942874985667582));
#38564=CARTESIAN_POINT('Ctrl Pts',(217.80295273395,3.46736880936034,2.95624867936802));
#38565=CARTESIAN_POINT('Ctrl Pts',(217.882142305007,1.63597108754423,4.25272281192996));
#38566=CARTESIAN_POINT('Ctrl Pts',(217.961331876065,-0.592154745435518,
4.5178983467812));
#38567=CARTESIAN_POINT('Ctrl Pts',(218.040521447122,-2.6766811985351,3.68746938642191));
#38568=CARTESIAN_POINT('Ctrl Pts',(218.11971101818,-4.11210407995962,1.96281755391823));
#38569=CARTESIAN_POINT('Ctrl Pts',(218.198900589238,-4.55032884647146,-0.237823681242803));
#38570=CARTESIAN_POINT('Ctrl Pts',(218.278090160295,-3.88508462005382,-2.38079192904617));
#38571=CARTESIAN_POINT('Ctrl Pts',(218.357279731353,-2.27769520857755,-3.94641067949257));
#38572=CARTESIAN_POINT('Ctrl Pts',(218.43646930241,-0.117957577266953,-4.55501248344671));
#38573=CARTESIAN_POINT('Ctrl Pts',(218.515658873468,2.07038513587111,-4.05900949783985));
#38574=CARTESIAN_POINT('Ctrl Pts',(218.594848444525,3.75665297092044,-2.57868399973024));
#38575=CARTESIAN_POINT('Ctrl Pts',(218.674038015583,4.53192069796186,-0.473019557497457));
#38576=CARTESIAN_POINT('Ctrl Pts',(218.75322758664,4.20818346572563,1.74735360851304));
#38577=CARTESIAN_POINT('Ctrl Pts',(218.832417157698,2.86394856669164,3.54398805327205));
#38578=CARTESIAN_POINT('Ctrl Pts',(218.911606728756,0.825197172846602,4.48119429843385));
#38579=CARTESIAN_POINT('Ctrl Pts',(218.990796299813,-1.41366711921135,4.33169689503441));
#38580=CARTESIAN_POINT('Ctrl Pts',(219.069985870871,-3.30971270848846,3.13174943149354));
#38581=CARTESIAN_POINT('Ctrl Pts',(219.149175441928,-4.4031426028244,1.17234292490846));
#38582=CARTESIAN_POINT('Ctrl Pts',(219.228365012986,-4.42879662917418,-1.07136041172219));
#38583=CARTESIAN_POINT('Ctrl Pts',(219.307554584043,-3.38045360582197,-3.05525549394406));
#38584=CARTESIAN_POINT('Ctrl Pts',(219.386744155101,-1.51233999842644,-4.29824155248976));
#38585=CARTESIAN_POINT('Ctrl Pts',(219.465933726158,0.722520793916989,-4.49889057621407));
#38586=CARTESIAN_POINT('Ctrl Pts',(219.545123297216,2.78216803143074,-3.60854454860609));
#38587=CARTESIAN_POINT('Ctrl Pts',(219.624312868274,4.16713080999959,-1.84311516914782));
#38588=CARTESIAN_POINT('Ctrl Pts',(219.703502439331,4.5415513193251,0.369275409857588));
#38589=CARTESIAN_POINT('Ctrl Pts',(219.782692010389,3.81463141353823,2.49211554572396));
#38590=CARTESIAN_POINT('Ctrl Pts',(219.861881581446,2.16265144586963,4.01060985862089));
#38591=CARTESIAN_POINT('Ctrl Pts',(219.941071152504,-0.0137782689576099,
4.55651872307046));
#38592=CARTESIAN_POINT('Ctrl Pts',(220.020260723561,-2.1868667104261,3.99745753013543));
#38593=CARTESIAN_POINT('Ctrl Pts',(220.099450294619,-3.82963312724697,2.46900036959006));
#38594=CARTESIAN_POINT('Ctrl Pts',(220.178639865676,-4.54370151966309,0.34180288867031));
#38595=CARTESIAN_POINT('Ctrl Pts',(220.257829436734,-4.15590806660398,-1.86828286299391));
#38596=CARTESIAN_POINT('Ctrl Pts',(220.337019007791,-2.76029389481659,-3.62530417052153));
#38597=CARTESIAN_POINT('Ctrl Pts',(220.416208578849,-0.695299810488197,
-4.50317786546855));
#38598=CARTESIAN_POINT('Ctrl Pts',(220.495398149907,1.53830665449812,-4.28901682788606));
#38599=CARTESIAN_POINT('Ctrl Pts',(220.574587720964,3.39886894010639,-3.03475578035621));
#38600=CARTESIAN_POINT('Ctrl Pts',(220.653777292022,4.43519486338251,-1.044556953301));
#38601=CARTESIAN_POINT('Ctrl Pts',(220.732966863079,4.39597214951006,1.19895020433616));
#38602=CARTESIAN_POINT('Ctrl Pts',(220.812156434137,3.29071241572633,3.15170818597724));
#38603=CARTESIAN_POINT('Ctrl Pts',(220.891346005194,1.38744463724644,4.34016705855231));
#38604=CARTESIAN_POINT('Ctrl Pts',(220.970535576252,-0.852282851982811,
4.47612184162993));
#38605=CARTESIAN_POINT('Ctrl Pts',(221.049725147309,-2.88532899192737,3.52660303771061));
#38606=CARTESIAN_POINT('Ctrl Pts',(221.128914718367,-4.21867400611988,1.72187200818135));
#38607=CARTESIAN_POINT('Ctrl Pts',(221.208104289424,-4.52897696306373,-0.500418487859158));
#38608=CARTESIAN_POINT('Ctrl Pts',(221.287293860482,-3.7409896782648,-2.60135569353455));
#38609=CARTESIAN_POINT('Ctrl Pts',(221.36648343154,-2.04579887264011,-4.07145650839735));
#38610=CARTESIAN_POINT('Ctrl Pts',(221.445673002597,0.14550072168771,-4.5542152892435));
#38611=CARTESIAN_POINT('Ctrl Pts',(221.524862573655,2.30152409777985,-3.93256490416486));
#38612=CARTESIAN_POINT('Ctrl Pts',(221.604052144712,3.89940335283094,-2.35725035066262));
#38613=CARTESIAN_POINT('Ctrl Pts',(221.68324171577,4.55170192744695,-0.210305677009054));
#38614=CARTESIAN_POINT('Ctrl Pts',(221.762431286827,4.10012073214107,1.98766009715916));
#38615=CARTESIAN_POINT('Ctrl Pts',(221.841620857885,2.65441560822601,3.70356057542857));
#38616=CARTESIAN_POINT('Ctrl Pts',(221.920810428942,0.56466538392668,4.52140736785216));
#38617=CARTESIAN_POINT('Ctrl Pts',(221.973603476314,-0.919183673409389,
4.33535198326386));
#38618=CARTESIAN_POINT('Ctrl Pts',(222.,-1.59436307123039,4.07092009220235));
#38619=CARTESIAN_POINT('Ctrl Pts',(209.122606897708,-2.00237954638784,4.0990633262012));
#38620=CARTESIAN_POINT('Ctrl Pts',(209.149003421394,-2.6822266191702,3.76696016875312));
#38621=CARTESIAN_POINT('Ctrl Pts',(209.201796468765,-3.87275893986003,2.75816685595665));
#38622=CARTESIAN_POINT('Ctrl Pts',(209.280986039823,-4.71967899437356,0.575078817531406));
#38623=CARTESIAN_POINT('Ctrl Pts',(209.360175610881,-4.4218761948155,-1.74715524550129));
#38624=CARTESIAN_POINT('Ctrl Pts',(209.439365181938,-3.05183373967382,-3.64586427800282));
#38625=CARTESIAN_POINT('Ctrl Pts',(209.518554752996,-0.941673499148998,
-4.66036497951415));
#38626=CARTESIAN_POINT('Ctrl Pts',(209.597744324053,1.39682754886719,-4.54474828187575));
#38627=CARTESIAN_POINT('Ctrl Pts',(209.676933895111,3.39660203221564,-3.32699915160874));
#38628=CARTESIAN_POINT('Ctrl Pts',(209.756123466168,4.57268589350896,-1.30245020638111));
#38629=CARTESIAN_POINT('Ctrl Pts',(209.835313037226,4.63988098971415,1.03795070952906));
#38630=CARTESIAN_POINT('Ctrl Pts',(209.914502608283,3.58188953169507,3.12664357733423));
#38631=CARTESIAN_POINT('Ctrl Pts',(209.993692179341,1.65527906426069,4.45711641239878));
#38632=CARTESIAN_POINT('Ctrl Pts',(210.072881750399,-0.672741955717303,
4.70672417324597));
#38633=CARTESIAN_POINT('Ctrl Pts',(210.152071321456,-2.83762085241282,3.81493676765804));
#38634=CARTESIAN_POINT('Ctrl Pts',(210.231260892514,-4.31436785104821,1.99801516470331));
#38635=CARTESIAN_POINT('Ctrl Pts',(210.310450463571,-4.74486711643238,-0.303431331155035));
#38636=CARTESIAN_POINT('Ctrl Pts',(210.389640034629,-4.02472125896932,-2.53129479823699));
#38637=CARTESIAN_POINT('Ctrl Pts',(210.468829605686,-2.32856788973525,-4.14531134193876));
#38638=CARTESIAN_POINT('Ctrl Pts',(210.548019176744,-0.067729518342643,
-4.75407690996086));
#38639=CARTESIAN_POINT('Ctrl Pts',(210.627208747801,2.20953347432824,-4.20996393969962));
#38640=CARTESIAN_POINT('Ctrl Pts',(210.706398318859,3.95097768066745,-2.64492153306734));
#38641=CARTESIAN_POINT('Ctrl Pts',(210.785587889916,4.73429742865376,-0.43847737263662));
#38642=CARTESIAN_POINT('Ctrl Pts',(210.864777460974,4.36953522639674,1.87429892337849));
#38643=CARTESIAN_POINT('Ctrl Pts',(210.943967032032,2.94514705021599,3.73255186190351));
#38644=CARTESIAN_POINT('Ctrl Pts',(211.023156603089,0.806551492703307,4.6856492867746));
#38645=CARTESIAN_POINT('Ctrl Pts',(211.102346174147,-1.52763532719452,4.50246208825895));
#38646=CARTESIAN_POINT('Ctrl Pts',(211.181535745204,-3.49136579703178,3.22741373554704));
#38647=CARTESIAN_POINT('Ctrl Pts',(211.260725316262,-4.60842912917466,1.16970744652565));
#38648=CARTESIAN_POINT('Ctrl Pts',(211.339914887319,-4.60793396791431,-1.17165656078372));
#38649=CARTESIAN_POINT('Ctrl Pts',(211.419104458377,-3.49000039140507,-3.2288901834958));
#38650=CARTESIAN_POINT('Ctrl Pts',(211.498294029434,-1.5257307923439,-4.50310782664356));
#38651=CARTESIAN_POINT('Ctrl Pts',(211.577483600492,0.808533301118549,-4.68530772202493));
#38652=CARTESIAN_POINT('Ctrl Pts',(211.65667317155,2.94672553743877,-3.73130582451915));
#38653=CARTESIAN_POINT('Ctrl Pts',(211.735862742607,4.37032760435653,-1.87245058137286));
#38654=CARTESIAN_POINT('Ctrl Pts',(211.815052313665,4.73411154316455,0.440479790637971));
#38655=CARTESIAN_POINT('Ctrl Pts',(211.894241884722,3.94985860964796,2.64659243422069));
#38656=CARTESIAN_POINT('Ctrl Pts',(211.97343145578,2.20775259578052,4.21089812568633));
#38657=CARTESIAN_POINT('Ctrl Pts',(212.052621026837,-0.0697403353187167,
4.75404783681379));
#38658=CARTESIAN_POINT('Ctrl Pts',(212.131810597895,-2.33032101673728,4.14432606198363));
#38659=CARTESIAN_POINT('Ctrl Pts',(212.211000168953,-4.02579155506466,2.52959224070883));
#38660=CARTESIAN_POINT('Ctrl Pts',(212.29018974001,-4.74499503602191,0.30142438058611));
#38661=CARTESIAN_POINT('Ctrl Pts',(212.369379311067,-4.31352236355903,-1.99983983562693));
#38662=CARTESIAN_POINT('Ctrl Pts',(212.448568882125,-2.83600701174427,-3.81613662994679));
#38663=CARTESIAN_POINT('Ctrl Pts',(212.527758453182,-0.670751079681758,
-4.7070083426939));
#38664=CARTESIAN_POINT('Ctrl Pts',(212.60694802424,1.65716408941078,-4.45641579409413));
#38665=CARTESIAN_POINT('Ctrl Pts',(212.686137595298,3.58321177802902,-3.12512846182015));
#38666=CARTESIAN_POINT('Ctrl Pts',(212.765327166355,4.64031939098202,-1.03598769237887));
#38667=CARTESIAN_POINT('Ctrl Pts',(212.844516737413,4.57213502218987,1.3043833362739));
#38668=CARTESIAN_POINT('Ctrl Pts',(212.92370630847,3.39519359457865,3.32843732168963));
#38669=CARTESIAN_POINT('Ctrl Pts',(213.002895879528,1.3949070894978,4.54533483483374));
#38670=CARTESIAN_POINT('Ctrl Pts',(213.082085450586,-0.943648752418333,
4.65997441850743));
#38671=CARTESIAN_POINT('Ctrl Pts',(213.161275021643,-3.05336681718838,3.64455561471865));
#38672=CARTESIAN_POINT('Ctrl Pts',(213.240464592701,-4.42263386830918,1.74532066279202));
#38673=CARTESIAN_POINT('Ctrl Pts',(213.319654163758,-4.71939835853417,-0.577160014683326));
#38674=CARTESIAN_POINT('Ctrl Pts',(213.398843734816,-3.87169396977627,-2.75967758143634));
#38675=CARTESIAN_POINT('Ctrl Pts',(213.478033305873,-2.08509167057987,-4.27296469378847));
#38676=CARTESIAN_POINT('Ctrl Pts',(213.557222876931,0.207151887420196,-4.7500444886993));
#38677=CARTESIAN_POINT('Ctrl Pts',(213.636412447988,2.44916046410186,-4.07522362210525));
#38678=CARTESIAN_POINT('Ctrl Pts',(213.715602019046,4.09723995960495,-2.41214826710563));
#38679=CARTESIAN_POINT('Ctrl Pts',(213.794791590103,4.75172593592283,-0.164119404588944));
#38680=CARTESIAN_POINT('Ctrl Pts',(213.873981161161,4.25390349451931,2.12370892741937));
#38681=CARTESIAN_POINT('Ctrl Pts',(213.953170732219,2.72449613618031,3.8965311949249));
#38682=CARTESIAN_POINT('Ctrl Pts',(214.032360303276,0.534389934072604,4.72443244712485));
#38683=CARTESIAN_POINT('Ctrl Pts',(214.111549874334,-1.78530750029075,4.40664403809632));
#38684=CARTESIAN_POINT('Ctrl Pts',(214.190739445391,-3.67206227580806,3.02023065206477));
#38685=CARTESIAN_POINT('Ctrl Pts',(214.269929016449,-4.66833045174647,0.901401876180031));
#38686=CARTESIAN_POINT('Ctrl Pts',(214.349118587506,-4.53251387599815,-1.43601967708264));
#38687=CARTESIAN_POINT('Ctrl Pts',(214.428308158564,-3.29754849344109,-3.42520196229195));
#38688=CARTESIAN_POINT('Ctrl Pts',(214.507497729621,-1.26291727617956,-4.58376204690116));
#38689=CARTESIAN_POINT('Ctrl Pts',(214.586687300679,1.07797533491064,-4.63074548279309));
#38690=CARTESIAN_POINT('Ctrl Pts',(214.665876871737,3.15745555200671,-3.55475863965281));
#38691=CARTESIAN_POINT('Ctrl Pts',(214.745066442794,4.47124291134501,-1.61673169599391));
#38692=CARTESIAN_POINT('Ctrl Pts',(214.824256013852,4.70073986465014,0.713357746136703));
#38693=CARTESIAN_POINT('Ctrl Pts',(214.903445584909,3.79029268216141,2.87045570121504));
#38694=CARTESIAN_POINT('Ctrl Pts',(214.982635155967,1.9606876563586,4.33145916098574));
#38695=CARTESIAN_POINT('Ctrl Pts',(215.061824727024,-0.344390265274361,
4.74207021186618));
#38696=CARTESIAN_POINT('Ctrl Pts',(215.141014298082,-2.56595246924845,4.00271438834225));
#38697=CARTESIAN_POINT('Ctrl Pts',(215.220203869139,-4.16526316510524,2.29268779263592));
#38698=CARTESIAN_POINT('Ctrl Pts',(215.299393440197,-4.75448450145365,0.0266772285174098));
#38699=CARTESIAN_POINT('Ctrl Pts',(215.378583011254,-4.19072845930201,-2.24580264704637));
#38700=CARTESIAN_POINT('Ctrl Pts',(215.457772582312,-2.61070764406421,-3.9736683488068));
#38701=CARTESIAN_POINT('Ctrl Pts',(215.536962153369,-0.397582050682125,
-4.73790703391906));
#38702=CARTESIAN_POINT('Ctrl Pts',(215.616151724427,1.91195843487049,-4.35318842831457));
#38703=CARTESIAN_POINT('Ctrl Pts',(215.695341295484,3.75784301338123,-2.91280799845547));
#38704=CARTESIAN_POINT('Ctrl Pts',(215.774530866542,4.69243889486114,-0.766062508597483));
#38705=CARTESIAN_POINT('Ctrl Pts',(215.8537204376,4.48910365171241,1.56645553823485));
#38706=CARTESIAN_POINT('Ctrl Pts',(215.932910008657,3.19714671706717,3.51910321227311));
#38707=CARTESIAN_POINT('Ctrl Pts',(216.012099579715,1.12987169285888,4.61835733857402));
#38708=CARTESIAN_POINT('Ctrl Pts',(216.091289150772,-1.21140075464009,4.5976453496047));
#38709=CARTESIAN_POINT('Ctrl Pts',(216.17047872183,-3.25890472608852,3.4619899675421));
#38710=CARTESIAN_POINT('Ctrl Pts',(216.249668292887,-4.51611409741403,1.4867911784183));
#38711=CARTESIAN_POINT('Ctrl Pts',(216.328857863945,-4.67815165958727,-0.848959126804803));
#38712=CARTESIAN_POINT('Ctrl Pts',(216.408047435003,-3.70572279642092,-2.97883418557841));
#38713=CARTESIAN_POINT('Ctrl Pts',(216.48723700606,-1.83464455203167,-4.38633262723938));
#38714=CARTESIAN_POINT('Ctrl Pts',(216.566426577118,0.481340740731405,-4.73013167262777));
#38715=CARTESIAN_POINT('Ctrl Pts',(216.645616148175,2.68059939672786,-3.92685897675821));
#38716=CARTESIAN_POINT('Ctrl Pts',(216.724805719233,4.22980430571912,-2.17131068352834));
#38717=CARTESIAN_POINT('Ctrl Pts',(216.80399529029,4.75326842651658,0.110787249107921));
#38718=CARTESIAN_POINT('Ctrl Pts',(216.883184861348,4.12405007079391,2.36601892694649));
#38719=CARTESIAN_POINT('Ctrl Pts',(216.962374432405,2.49473665997683,4.04748360669341));
#38720=CARTESIAN_POINT('Ctrl Pts',(217.041564003463,0.260441797776623,4.74742083862966));
#38721=CARTESIAN_POINT('Ctrl Pts',(217.120753574521,-2.03701101586092,4.29609365241792));
#38722=CARTESIAN_POINT('Ctrl Pts',(217.199943145578,-3.84048228001083,2.80295030387752));
#38723=CARTESIAN_POINT('Ctrl Pts',(217.279132716635,-4.71262456621813,0.630082730251849));
#38724=CARTESIAN_POINT('Ctrl Pts',(217.358322287693,-4.44194063928881,-1.69558187832931));
#38725=CARTESIAN_POINT('Ctrl Pts',(217.437511858751,-3.09407219904913,-3.61006257233245));
#38726=CARTESIAN_POINT('Ctrl Pts',(217.516701429808,-0.995881562605238,
-4.6490917889785));
#38727=CARTESIAN_POINT('Ctrl Pts',(217.595891000865,1.34381347100266,-4.56070168989774));
#38728=CARTESIAN_POINT('Ctrl Pts',(217.675080571923,3.35762953024097,-3.36632715087795));
#38729=CARTESIAN_POINT('Ctrl Pts',(217.754270142981,4.55720991522943,-1.3556077373705));
#38730=CARTESIAN_POINT('Ctrl Pts',(217.833459714038,4.65165262656914,0.983850797030065));
#38731=CARTESIAN_POINT('Ctrl Pts',(217.912649285096,3.61805501104801,3.08472243258849));
#38732=CARTESIAN_POINT('Ctrl Pts',(217.991838856153,1.70706772675591,4.43753921958473));
#38733=CARTESIAN_POINT('Ctrl Pts',(218.071028427211,-0.61788882632131,4.71423885133025));
#38734=CARTESIAN_POINT('Ctrl Pts',(218.150217998268,-2.79300540432687,3.84772080074492));
#38735=CARTESIAN_POINT('Ctrl Pts',(218.229407569326,-4.29080942652693,2.04811840827425));
#38736=CARTESIAN_POINT('Ctrl Pts',(218.308597140384,-4.74807872772251,-0.248159111122965));
#38737=CARTESIAN_POINT('Ctrl Pts',(218.387786711441,-4.05392407060511,-2.48425726905503));
#38738=CARTESIAN_POINT('Ctrl Pts',(218.466976282499,-2.37668013301254,-4.11791526071479));
#38739=CARTESIAN_POINT('Ctrl Pts',(218.546165853556,-0.123083821475732,
-4.75296590793319));
#38740=CARTESIAN_POINT('Ctrl Pts',(218.625355424614,2.16036070216009,-4.23540744033519));
#38741=CARTESIAN_POINT('Ctrl Pts',(218.704544995671,3.91991099115714,-2.69074940685485));
#38742=CARTESIAN_POINT('Ctrl Pts',(218.783734566729,4.72887059105718,-0.493576217132539));
#38743=CARTESIAN_POINT('Ctrl Pts',(218.862924137786,4.39106426592872,1.82329075069452));
#38744=CARTESIAN_POINT('Ctrl Pts',(218.942113708844,2.98841110733013,3.6980040025222));
#38745=CARTESIAN_POINT('Ctrl Pts',(219.021303279902,0.861058898107562,4.67593970481593));
#38746=CARTESIAN_POINT('Ctrl Pts',(219.100492850959,-1.47510278999134,4.51994538772804));
#38747=CARTESIAN_POINT('Ctrl Pts',(219.179682422017,-3.45354743278232,3.26785016159048));
#38748=CARTESIAN_POINT('Ctrl Pts',(219.258871993074,-4.594496009626,1.22329103921145));
#38749=CARTESIAN_POINT('Ctrl Pts',(219.338061564132,-4.62126491818221,-1.11791999045667));
#38750=CARTESIAN_POINT('Ctrl Pts',(219.417251135189,-3.52736261430921,-3.18803192208892));
#38751=CARTESIAN_POINT('Ctrl Pts',(219.496440706247,-1.57806383184389,-4.48503613047993));
#38752=CARTESIAN_POINT('Ctrl Pts',(219.575630277304,0.753920370962774,-4.69440503400928));
#38753=CARTESIAN_POINT('Ctrl Pts',(219.654819848362,2.90307652319007,-3.76536601801031));
#38754=CARTESIAN_POINT('Ctrl Pts',(219.73400941942,4.34822752864093,-1.92321395280247));
#38755=CARTESIAN_POINT('Ctrl Pts',(219.813198990477,4.73891974354097,0.385323517788255));
#38756=CARTESIAN_POINT('Ctrl Pts',(219.892388561535,3.98040908247059,2.60041882881808));
#38757=CARTESIAN_POINT('Ctrl Pts',(219.971578132592,2.25663675573131,4.18490443161675));
#38758=CARTESIAN_POINT('Ctrl Pts',(220.05076770365,-0.0143770500879572,
4.75453760627801));
#38759=CARTESIAN_POINT('Ctrl Pts',(220.129957274707,-2.28190437624973,4.17118052435449));
#38760=CARTESIAN_POINT('Ctrl Pts',(220.209146845765,-3.99606274622613,2.57629910477353));
#38761=CARTESIAN_POINT('Ctrl Pts',(220.288336416822,-4.74116338808395,0.356657085570453));
#38762=CARTESIAN_POINT('Ctrl Pts',(220.36752598788,-4.33651706309409,-1.94947539363636));
#38763=CARTESIAN_POINT('Ctrl Pts',(220.446715558937,-2.88025177222171,-3.78285398580036));
#38764=CARTESIAN_POINT('Ctrl Pts',(220.525905129995,-0.725516407924797,
-4.69887864187271));
#38765=CARTESIAN_POINT('Ctrl Pts',(220.605094701053,1.60515895650054,-4.47541051436785));
#38766=CARTESIAN_POINT('Ctrl Pts',(220.68428427211,3.54657824903141,-3.16664132433328));
#38767=CARTESIAN_POINT('Ctrl Pts',(220.763473843168,4.62794120922941,-1.08995169738317));
#38768=CARTESIAN_POINT('Ctrl Pts',(220.842663414225,4.58701394008804,1.25105462767189));
#38769=CARTESIAN_POINT('Ctrl Pts',(220.921852985283,3.4337214182396,3.28867629104029));
#38770=CARTESIAN_POINT('Ctrl Pts',(221.00104255634,1.44774072166475,4.52878365075838));
#38771=CARTESIAN_POINT('Ctrl Pts',(221.080232127398,-0.889321676748745,
4.67064680730003));
#38772=CARTESIAN_POINT('Ctrl Pts',(221.159421698456,-3.01072069102759,3.67986346249677));
#38773=CARTESIAN_POINT('Ctrl Pts',(221.238611269513,-4.40201070812417,1.79670176151038));
#38774=CARTESIAN_POINT('Ctrl Pts',(221.317800840571,-4.72579892623439,-0.522165860387332));
#38775=CARTESIAN_POINT('Ctrl Pts',(221.396990411628,-3.90356699731108,-2.71440637554999));
#38776=CARTESIAN_POINT('Ctrl Pts',(221.476179982686,-2.13470595996895,-4.24839537770098));
#38777=CARTESIAN_POINT('Ctrl Pts',(221.555369553743,0.151823946097727,-4.75213406896817));
#38778=CARTESIAN_POINT('Ctrl Pts',(221.634559124801,2.40154458693313,-4.10346777053982));
#38779=CARTESIAN_POINT('Ctrl Pts',(221.713748695858,4.06886507219001,-2.45969261201348));
#38780=CARTESIAN_POINT('Ctrl Pts',(221.792938266916,4.74951148056106,-0.219445219239563));
#38781=CARTESIAN_POINT('Ctrl Pts',(221.872127837973,4.27830530192763,2.0740405679872));
#38782=CARTESIAN_POINT('Ctrl Pts',(221.951317409031,2.76977218772349,3.86451128662056));
#38783=CARTESIAN_POINT('Ctrl Pts',(222.030506980089,0.589204821928996,4.71790036874235));
#38784=CARTESIAN_POINT('Ctrl Pts',(222.08330002746,-0.959129898923508,4.52375932013947));
#38785=CARTESIAN_POINT('Ctrl Pts',(222.109696551146,-1.66365149381358,4.24783564973174));
#38786=CARTESIAN_POINT('Ctrl Pts',(209.232303448854,-2.08577545033647,4.26978275451734));
#38787=CARTESIAN_POINT('Ctrl Pts',(209.25869997254,-2.79393706582568,3.92384803198484));
#38788=CARTESIAN_POINT('Ctrl Pts',(209.311493019911,-4.03405315261176,2.8730400919566));
#38789=CARTESIAN_POINT('Ctrl Pts',(209.390682590969,-4.91624607217517,0.599029930054648));
#38790=CARTESIAN_POINT('Ctrl Pts',(209.469872162026,-4.60604026255224,-1.81992146572163));
#38791=CARTESIAN_POINT('Ctrl Pts',(209.549061733084,-3.17893773146209,-3.79770869115944));
#38792=CARTESIAN_POINT('Ctrl Pts',(209.628251304142,-0.980892693545834,
-4.8544617235097));
#38793=CARTESIAN_POINT('Ctrl Pts',(209.707440875199,1.45500318110846,-4.73402977542166));
#38794=CARTESIAN_POINT('Ctrl Pts',(209.786630446257,3.53806507169852,-3.46556334249118));
#38795=CARTESIAN_POINT('Ctrl Pts',(209.865820017314,4.7631309438743,-1.35669517332817));
#38796=CARTESIAN_POINT('Ctrl Pts',(209.945009588372,4.83312460831251,1.08117969567778));
#38797=CARTESIAN_POINT('Ctrl Pts',(210.024199159429,3.7310694990388,3.25686327915217));
#38798=CARTESIAN_POINT('Ctrl Pts',(210.103388730487,1.72421878855038,4.64274817880732));
#38799=CARTESIAN_POINT('Ctrl Pts',(210.182578301545,-0.700760581667812,
4.90275170347761));
#38800=CARTESIAN_POINT('Ctrl Pts',(210.261767872602,-2.95580322022483,3.97382277946319));
#38801=CARTESIAN_POINT('Ctrl Pts',(210.34095744366,-4.49405436829923,2.08122929913857));
#38802=CARTESIAN_POINT('Ctrl Pts',(210.420147014717,-4.94248323921234,-0.316068760554286));
#38803=CARTESIAN_POINT('Ctrl Pts',(210.499336585775,-4.1923444591456,-2.63671917606798));
#38804=CARTESIAN_POINT('Ctrl Pts',(210.578526156832,-2.42554901622577,-4.31795692610543));
#38805=CARTESIAN_POINT('Ctrl Pts',(210.65771572789,-0.0705503444025215,
-4.952076605904));
#38806=CARTESIAN_POINT('Ctrl Pts',(210.736905298947,2.30155700789298,-4.38530220110755));
#38807=CARTESIAN_POINT('Ctrl Pts',(210.816094870005,4.1155295788101,-2.75507828258134));
#38808=CARTESIAN_POINT('Ctrl Pts',(210.895284441063,4.93147334085109,-0.456739253566259));
#38809=CARTESIAN_POINT('Ctrl Pts',(210.97447401212,4.55151937655356,1.95236047433024));
#38810=CARTESIAN_POINT('Ctrl Pts',(211.053663583178,3.06780771210575,3.88800667421426));
#38811=CARTESIAN_POINT('Ctrl Pts',(211.132853154235,0.840143071750589,4.88079908170822));
#38812=CARTESIAN_POINT('Ctrl Pts',(211.212042725293,-1.59125889408775,4.68998242950604));
#38813=CARTESIAN_POINT('Ctrl Pts',(211.29123229635,-3.63677559568062,3.36183035320464));
#38814=CARTESIAN_POINT('Ctrl Pts',(211.370421867408,-4.80036282811003,1.21842388993642));
#38815=CARTESIAN_POINT('Ctrl Pts',(211.449611438465,-4.79984704417553,-1.22045418168439));
#38816=CARTESIAN_POINT('Ctrl Pts',(211.528801009523,-3.63535332309447,-3.36336829284788));
#38817=CARTESIAN_POINT('Ctrl Pts',(211.60799058058,-1.58927503840821,-4.69065506186107));
#38818=CARTESIAN_POINT('Ctrl Pts',(211.687180151638,0.842207419315057,-4.88044329133328));
#38819=CARTESIAN_POINT('Ctrl Pts',(211.766369722696,3.06945194079548,-3.88670874136673));
#38820=CARTESIAN_POINT('Ctrl Pts',(211.845559293753,4.55234475578742,-1.95043515183777));
#38821=CARTESIAN_POINT('Ctrl Pts',(211.924748864811,4.9312797135287,0.458825069073119));
#38822=CARTESIAN_POINT('Ctrl Pts',(212.003938435868,4.11436390027337,2.75681877409396));
#38823=CARTESIAN_POINT('Ctrl Pts',(212.083128006926,2.29970195860349,4.38627529444573));
#38824=CARTESIAN_POINT('Ctrl Pts',(212.162317577983,-0.0726449086879616,
4.95204632190687));
#38825=CARTESIAN_POINT('Ctrl Pts',(212.241507149041,-2.4273751581621,4.31693061081681));
#38826=CARTESIAN_POINT('Ctrl Pts',(212.320696720099,-4.19345933136064,2.63494570974319));
#38827=CARTESIAN_POINT('Ctrl Pts',(212.399886291156,-4.94261648644808,0.313978223705665));
#38828=CARTESIAN_POINT('Ctrl Pts',(212.479075862214,-4.49317366760906,-2.08312996468635));
#38829=CARTESIAN_POINT('Ctrl Pts',(212.558265433271,-2.95412216567489,-3.97507261409625));
#38830=CARTESIAN_POINT('Ctrl Pts',(212.637455004329,-0.698686788831166,
-4.90304770812833));
#38831=CARTESIAN_POINT('Ctrl Pts',(212.716644575386,1.72618232198158,-4.6420183808714));
#38832=CARTESIAN_POINT('Ctrl Pts',(212.795834146444,3.73244681481672,-3.2552850615014));
#38833=CARTESIAN_POINT('Ctrl Pts',(212.875023717501,4.83358126829166,-1.07913492200449));
#38834=CARTESIAN_POINT('Ctrl Pts',(212.954213288559,4.76255712964628,1.35870881498762));
#38835=CARTESIAN_POINT('Ctrl Pts',(213.033402859616,3.53659797488772,3.4670614100546));
#38836=CARTESIAN_POINT('Ctrl Pts',(213.112592430674,1.45300273767944,4.73464075737175));
#38837=CARTESIAN_POINT('Ctrl Pts',(213.191782001731,-0.982950212953061,
4.85405489626201));
#38838=CARTESIAN_POINT('Ctrl Pts',(213.270971572789,-3.18053465920191,3.79634552414359));
#38839=CARTESIAN_POINT('Ctrl Pts',(213.350161143847,-4.60682949193451,1.81801047557819));
#38840=CARTESIAN_POINT('Ctrl Pts',(213.429350714904,-4.91595374830214,-0.601197805737639));
#38841=CARTESIAN_POINT('Ctrl Pts',(213.508540285962,-4.03294382822817,-2.87461373673508));
#38842=CARTESIAN_POINT('Ctrl Pts',(213.587729857019,-2.17193240214721,-4.45092683579193));
#38843=CARTESIAN_POINT('Ctrl Pts',(213.666919428077,0.215779432051886,-4.94787624074946));
#38844=CARTESIAN_POINT('Ctrl Pts',(213.746108999134,2.55116407834546,-4.24495016489351));
#38845=CARTESIAN_POINT('Ctrl Pts',(213.825298570192,4.26788344762005,-2.51261038257036));
#38846=CARTESIAN_POINT('Ctrl Pts',(213.904488141249,4.94962771755924,-0.17095471517026));
#38847=CARTESIAN_POINT('Ctrl Pts',(213.983677712307,4.43107176807448,2.21215800593967));
#38848=CARTESIAN_POINT('Ctrl Pts',(214.062867283364,2.83796704058064,4.0588154840603));
#38849=CARTESIAN_POINT('Ctrl Pts',(214.142056854422,0.556646419709134,4.9211974986272));
#38850=CARTESIAN_POINT('Ctrl Pts',(214.22124642548,-1.85966270087277,4.59017371087982));
#38851=CARTESIAN_POINT('Ctrl Pts',(214.300435996537,-3.82499779365188,3.14601842582461));
#38852=CARTESIAN_POINT('Ctrl Pts',(214.379625567595,-4.86275894491434,0.938943821921869));
#38853=CARTESIAN_POINT('Ctrl Pts',(214.458815138652,-4.72128582611645,-1.49582759874982));
#38854=CARTESIAN_POINT('Ctrl Pts',(214.53800470971,-3.43488611153707,-3.56785614309761));
#38855=CARTESIAN_POINT('Ctrl Pts',(214.617194280767,-1.31551575984334,-4.7746684013315));
#38856=CARTESIAN_POINT('Ctrl Pts',(214.696383851825,1.12287128266008,-4.82360862214659));
#38857=CARTESIAN_POINT('Ctrl Pts',(214.775573422882,3.2889585232652,-3.70280864875716));
#38858=CARTESIAN_POINT('Ctrl Pts',(214.85476299394,4.65746302382978,-1.68406598407784));
#38859=CARTESIAN_POINT('Ctrl Pts',(214.933952564997,4.89651815800471,0.743067954765796));
#38860=CARTESIAN_POINT('Ctrl Pts',(215.013142136055,3.94815230724047,2.99000558793815));
#38861=CARTESIAN_POINT('Ctrl Pts',(215.092331707113,2.04234715980187,4.51185750394656));
#38862=CARTESIAN_POINT('Ctrl Pts',(215.17152127817,-0.358733568738209,4.93956984804649));
#38863=CARTESIAN_POINT('Ctrl Pts',(215.250710849228,-2.67282028361871,4.16942103757177));
#38864=CARTESIAN_POINT('Ctrl Pts',(215.329900420285,-4.33873971078038,2.3881745704967));
#38865=CARTESIAN_POINT('Ctrl Pts',(215.409089991343,-4.95250117293023,0.027788292396928));
#38866=CARTESIAN_POINT('Ctrl Pts',(215.4882795624,-4.36526559373151,-2.33933673361777));
#38867=CARTESIAN_POINT('Ctrl Pts',(215.567469133458,-2.71943943984944,-4.13916527696841));
#38868=CARTESIAN_POINT('Ctrl Pts',(215.646658704515,-0.414140706892048,
-4.93523328039969));
#38869=CARTESIAN_POINT('Ctrl Pts',(215.725848275573,1.99158844421406,-4.53449176048901));
#38870=CARTESIAN_POINT('Ctrl Pts',(215.805037846631,3.91435116168074,-3.03412179058756));
#38871=CARTESIAN_POINT('Ctrl Pts',(215.884227417688,4.887871466107,-0.797967786246231));
#38872=CARTESIAN_POINT('Ctrl Pts',(215.963416988746,4.67606763545317,1.63169590479877));
#38873=CARTESIAN_POINT('Ctrl Pts',(216.042606559803,3.33030276183762,3.66566822988202));
#38874=CARTESIAN_POINT('Ctrl Pts',(216.121796130861,1.17692904087363,4.810704531544));
#38875=CARTESIAN_POINT('Ctrl Pts',(216.200985701918,-1.2618536576172,4.78912992137693));
#38876=CARTESIAN_POINT('Ctrl Pts',(216.280175272976,-3.39463289311104,3.60617630989919));
#38877=CARTESIAN_POINT('Ctrl Pts',(216.359364844033,-4.70420302299682,1.54871365187283));
#38878=CARTESIAN_POINT('Ctrl Pts',(216.438554415091,-4.87298919034606,-0.884316915952731));
#38879=CARTESIAN_POINT('Ctrl Pts',(216.517743986149,-3.86006022108554,-3.10289786275067));
#38880=CARTESIAN_POINT('Ctrl Pts',(216.596933557206,-1.91105456187079,-4.5690163622625));
#38881=CARTESIAN_POINT('Ctrl Pts',(216.676123128264,0.50138781235326,-4.92713408775256));
#38882=CARTESIAN_POINT('Ctrl Pts',(216.755312699321,2.79224207217245,-4.09040636947721));
#38883=CARTESIAN_POINT('Ctrl Pts',(216.834502270379,4.40596888662368,-2.26174229901945));
#38884=CARTESIAN_POINT('Ctrl Pts',(216.913691841436,4.95123445041797,0.115401360754224));
#38885=CARTESIAN_POINT('Ctrl Pts',(216.992881412494,4.29581015703917,2.4645598292086));
#38886=CARTESIAN_POINT('Ctrl Pts',(217.072070983551,2.59863844984874,4.21605482222864));
#38887=CARTESIAN_POINT('Ctrl Pts',(217.151260554609,0.271288781901483,4.94514331985273));
#38888=CARTESIAN_POINT('Ctrl Pts',(217.230450125666,-2.12184926509668,4.47501907853792));
#38889=CARTESIAN_POINT('Ctrl Pts',(217.309639696724,-4.00043222152815,2.91968869882202));
#38890=CARTESIAN_POINT('Ctrl Pts',(217.388829267781,-4.90889783837539,0.656324667723989));
#38891=CARTESIAN_POINT('Ctrl Pts',(217.468018838839,-4.62694035903123,-1.76620015033337));
#38892=CARTESIAN_POINT('Ctrl Pts',(217.547208409896,-3.22293535508144,-3.7604159017369));
#38893=CARTESIAN_POINT('Ctrl Pts',(217.626397980954,-1.03735843610262,-4.84271902262731));
#38894=CARTESIAN_POINT('Ctrl Pts',(217.705587552012,1.39978115173269,-4.75064761735951));
#38895=CARTESIAN_POINT('Ctrl Pts',(217.784777123069,3.49746942737946,-3.50652928999826));
#38896=CARTESIAN_POINT('Ctrl Pts',(217.863966694127,4.74701041586371,-1.41206663042189));
#38897=CARTESIAN_POINT('Ctrl Pts',(217.943156265184,4.84538651500583,1.02482660839255));
#38898=CARTESIAN_POINT('Ctrl Pts',(218.022345836242,3.76874121273569,3.21319618580896));
#38899=CARTESIAN_POINT('Ctrl Pts',(218.101535407299,1.77816436596759,4.62235562723951));
#38900=CARTESIAN_POINT('Ctrl Pts',(218.180724978357,-0.643622907207105,
4.91057935587929));
#38901=CARTESIAN_POINT('Ctrl Pts',(218.259914549415,-2.90932961011864,4.00797221506793));
#38902=CARTESIAN_POINT('Ctrl Pts',(218.339104120472,-4.46951477309425,2.13341926263027));
#38903=CARTESIAN_POINT('Ctrl Pts',(218.41829369153,-4.94582860897356,-0.258494541003129));
#38904=CARTESIAN_POINT('Ctrl Pts',(218.497483262587,-4.22276352115641,-2.58772260906389));
#38905=CARTESIAN_POINT('Ctrl Pts',(218.576672833645,-2.47566505744753,-4.28941984193701));
#38906=CARTESIAN_POINT('Ctrl Pts',(218.655862404702,-0.12821006568451,-4.95091933241967));
#38907=CARTESIAN_POINT('Ctrl Pts',(218.73505197576,2.25033626844908,-4.41180538283052));
#38908=CARTESIAN_POINT('Ctrl Pts',(218.814241546818,4.08316901139384,-2.80281481397946));
#38909=CARTESIAN_POINT('Ctrl Pts',(218.893431117875,4.9258204841525,-0.514132876767619));
#38910=CARTESIAN_POINT('Ctrl Pts',(218.972620688933,4.5739450661318,1.899227892876));
#38911=CARTESIAN_POINT('Ctrl Pts',(219.05181025999,3.11287364796861,3.85201995177236));
#38912=CARTESIAN_POINT('Ctrl Pts',(219.130999831048,0.896920623368521,4.870685111198));
#38913=CARTESIAN_POINT('Ctrl Pts',(219.210189402105,-1.53653846077132,4.70819388042167));
#38914=CARTESIAN_POINT('Ctrl Pts',(219.289378973163,-3.59738215707619,3.40395089168742));
#38915=CARTESIAN_POINT('Ctrl Pts',(219.36856854422,-4.78584941642761,1.27423915351443));
#38916=CARTESIAN_POINT('Ctrl Pts',(219.447758115278,-4.81373320719024,-1.16447956919115));
#38917=CARTESIAN_POINT('Ctrl Pts',(219.526947686335,-3.67427162279645,-3.32080835023378));
#38918=CARTESIAN_POINT('Ctrl Pts',(219.606137257393,-1.64378766526134,-4.67183070847011));
#38919=CARTESIAN_POINT('Ctrl Pts',(219.68532682845,0.785319948008557,-4.8899194918045));
#38920=CARTESIAN_POINT('Ctrl Pts',(219.764516399508,3.0239850149494,-3.92218748741451));
#38921=CARTESIAN_POINT('Ctrl Pts',(219.843705970566,4.52932424728226,-2.00331273645713));
#38922=CARTESIAN_POINT('Ctrl Pts',(219.922895541623,4.93628816775683,0.401371625718925));
#38923=CARTESIAN_POINT('Ctrl Pts',(220.002085112681,4.14618675140296,2.7087221119122));
#38924=CARTESIAN_POINT('Ctrl Pts',(220.081274683738,2.35062206559299,4.35919900461263));
#38925=CARTESIAN_POINT('Ctrl Pts',(220.160464254796,-0.0149758312183077,
4.95255648948555));
#38926=CARTESIAN_POINT('Ctrl Pts',(220.239653825853,-2.37694204207336,4.34490351857356));
#38927=CARTESIAN_POINT('Ctrl Pts',(220.318843396911,-4.1624923652053,2.68359783995701));
#38928=CARTESIAN_POINT('Ctrl Pts',(220.398032967968,-4.93862525650481,0.371511282470593));
#38929=CARTESIAN_POINT('Ctrl Pts',(220.477222539026,-4.5171260595842,-2.03066792427881));
#38930=CARTESIAN_POINT('Ctrl Pts',(220.556412110083,-3.00020964962683,-3.94040380107919));
#38931=CARTESIAN_POINT('Ctrl Pts',(220.635601681141,-0.755733005361399,
-4.89457941827688));
#38932=CARTESIAN_POINT('Ctrl Pts',(220.714791252199,1.67201125850296,-4.66180420084963));
#38933=CARTESIAN_POINT('Ctrl Pts',(220.793980823256,3.69428755795643,-3.29852686831034));
#38934=CARTESIAN_POINT('Ctrl Pts',(220.873170394314,4.82068755507631,-1.13534644146534));
#38935=CARTESIAN_POINT('Ctrl Pts',(220.952359965371,4.77805573066601,1.30315905100762));
#38936=CARTESIAN_POINT('Ctrl Pts',(221.031549536429,3.57673042075288,3.42564439610333));
#38937=CARTESIAN_POINT('Ctrl Pts',(221.110739107487,1.50803680608307,4.71740024296444));
#38938=CARTESIAN_POINT('Ctrl Pts',(221.189928678544,-0.926360501514684,
4.86517177297014));
#38939=CARTESIAN_POINT('Ctrl Pts',(221.269118249601,-3.1361123901278,3.83312388728291));
#38940=CARTESIAN_POINT('Ctrl Pts',(221.348307820659,-4.58534741012846,1.87153151483941));
#38941=CARTESIAN_POINT('Ctrl Pts',(221.427497391717,-4.92262088940505,-0.543913232915508));
#38942=CARTESIAN_POINT('Ctrl Pts',(221.506686962774,-4.06614431635736,-2.82745705756544));
#38943=CARTESIAN_POINT('Ctrl Pts',(221.585876533832,-2.22361304729779,-4.42533424700461));
#38944=CARTESIAN_POINT('Ctrl Pts',(221.665066104889,0.158147170507748,-4.95005284869285));
#38945=CARTESIAN_POINT('Ctrl Pts',(221.744255675947,2.5015650760864,-4.27437063691479));
#38946=CARTESIAN_POINT('Ctrl Pts',(221.823445247004,4.23832679154908,-2.56213487336434));
#38947=CARTESIAN_POINT('Ctrl Pts',(221.902634818062,4.94732103367518,-0.22858476147007));
#38948=CARTESIAN_POINT('Ctrl Pts',(221.981824389119,4.45648987171418,2.16042103881523));
#38949=CARTESIAN_POINT('Ctrl Pts',(222.061013960177,2.88512876722097,4.02546199781256));
#38950=CARTESIAN_POINT('Ctrl Pts',(222.140203531234,0.613744259931314,4.91439336963254));
#38951=CARTESIAN_POINT('Ctrl Pts',(222.192996578606,-0.999076124437626,
4.71216665701508));
#38952=CARTESIAN_POINT('Ctrl Pts',(222.219393102292,-1.73293991639677,4.42475120726112));
#38953=CARTESIAN_POINT('Ctrl Pts',(209.342,-2.1691713542851,4.44050218283349));
#38954=CARTESIAN_POINT('Ctrl Pts',(209.368396523686,-2.90564751248116,4.08073589521657));
#38955=CARTESIAN_POINT('Ctrl Pts',(209.421189571058,-4.19534736536348,2.98791332795656));
#38956=CARTESIAN_POINT('Ctrl Pts',(209.500379142115,-5.11281314997678,0.62298104257789));
#38957=CARTESIAN_POINT('Ctrl Pts',(209.579568713173,-4.79020433028897,-1.89268768594197));
#38958=CARTESIAN_POINT('Ctrl Pts',(209.65875828423,-3.30604172325035,-3.94955310431605));
#38959=CARTESIAN_POINT('Ctrl Pts',(209.737947855288,-1.02011188794267,-5.04855846750524));
#38960=CARTESIAN_POINT('Ctrl Pts',(209.817137426345,1.51317881334974,-4.92331126896756));
#38961=CARTESIAN_POINT('Ctrl Pts',(209.896326997403,3.67952811118141,-3.60412753337363));
#38962=CARTESIAN_POINT('Ctrl Pts',(209.975516568461,4.95357599423964,-1.41094014027523));
#38963=CARTESIAN_POINT('Ctrl Pts',(210.054706139518,5.02636822691087,1.1244086818265));
#38964=CARTESIAN_POINT('Ctrl Pts',(210.133895710575,3.88024946638254,3.38708298097011));
#38965=CARTESIAN_POINT('Ctrl Pts',(210.213085281633,1.79315851284007,4.82837994521586));
#38966=CARTESIAN_POINT('Ctrl Pts',(210.292274852691,-0.728779207618322,
5.09877923370925));
#38967=CARTESIAN_POINT('Ctrl Pts',(210.371464423748,-3.07398558803684,4.13270879126833));
#38968=CARTESIAN_POINT('Ctrl Pts',(210.450653994806,-4.67374088555024,2.16444343357384));
#38969=CARTESIAN_POINT('Ctrl Pts',(210.529843565863,-5.1400993619923,-0.328706189953541));
#38970=CARTESIAN_POINT('Ctrl Pts',(210.609033136921,-4.35996765932188,-2.74214355389897));
#38971=CARTESIAN_POINT('Ctrl Pts',(210.688222707978,-2.52253014271629,-4.4906025102721));
#38972=CARTESIAN_POINT('Ctrl Pts',(210.767412279036,-0.0733711704623997,
-5.15007630184713));
#38973=CARTESIAN_POINT('Ctrl Pts',(210.846601850093,2.39358054145771,-4.56064046251547));
#38974=CARTESIAN_POINT('Ctrl Pts',(210.925791421151,4.28008147695276,-2.86523503209533));
#38975=CARTESIAN_POINT('Ctrl Pts',(211.004980992208,5.12864925304842,-0.475001134495899));
#38976=CARTESIAN_POINT('Ctrl Pts',(211.084170563266,4.73350352671038,2.03042202528198));
#38977=CARTESIAN_POINT('Ctrl Pts',(211.163360134324,3.19046837399552,4.04346148652501));
#38978=CARTESIAN_POINT('Ctrl Pts',(211.242549705381,0.873734650797867,5.07594887664184));
#38979=CARTESIAN_POINT('Ctrl Pts',(211.321739276439,-1.65488246098097,4.87750277075313));
#38980=CARTESIAN_POINT('Ctrl Pts',(211.400928847496,-3.78218539432946,3.49624697086225));
#38981=CARTESIAN_POINT('Ctrl Pts',(211.480118418554,-4.99229652704541,1.26714033334719));
#38982=CARTESIAN_POINT('Ctrl Pts',(211.559307989611,-4.99176012043676,-1.26925180258506));
#38983=CARTESIAN_POINT('Ctrl Pts',(211.638497560669,-3.78070625478386,-3.49784640219995));
#38984=CARTESIAN_POINT('Ctrl Pts',(211.717687131727,-1.65281928447252,-4.87820229707857));
#38985=CARTESIAN_POINT('Ctrl Pts',(211.796876702784,0.875881537511563,-5.07557886064165));
#38986=CARTESIAN_POINT('Ctrl Pts',(211.876066273842,3.1921783441522,-4.04211165821431));
#38987=CARTESIAN_POINT('Ctrl Pts',(211.955255844899,4.73436190721831,-2.02841972230267));
#38988=CARTESIAN_POINT('Ctrl Pts',(212.034445415957,5.12844788389286,0.47717034750827));
#38989=CARTESIAN_POINT('Ctrl Pts',(212.113634987014,4.27886919089879,2.86704511396724));
#38990=CARTESIAN_POINT('Ctrl Pts',(212.192824558072,2.39165132142645,4.56165246320512));
#38991=CARTESIAN_POINT('Ctrl Pts',(212.272014129129,-0.0755494820572054,
5.15004480699995));
#38992=CARTESIAN_POINT('Ctrl Pts',(212.351203700187,-2.52442929958692,4.48953515964998));
#38993=CARTESIAN_POINT('Ctrl Pts',(212.430393271245,-4.36112710765662,2.74029917877754));
#38994=CARTESIAN_POINT('Ctrl Pts',(212.509582842302,-5.14023793687424,0.326532066825224));
#38995=CARTESIAN_POINT('Ctrl Pts',(212.588772413359,-4.67282497165909,-2.16642009374577));
#38996=CARTESIAN_POINT('Ctrl Pts',(212.667961984417,-3.0722373196055,-4.13400859824571));
#38997=CARTESIAN_POINT('Ctrl Pts',(212.747151555475,-0.726622497980572,
-5.09908707356275));
#38998=CARTESIAN_POINT('Ctrl Pts',(212.826341126532,1.79520055455238,-4.82762096764867));
#38999=CARTESIAN_POINT('Ctrl Pts',(212.90553069759,3.88168185160442,-3.38544166118265));
#39000=CARTESIAN_POINT('Ctrl Pts',(212.984720268647,5.0268431456013,-1.1222821516301));
#39001=CARTESIAN_POINT('Ctrl Pts',(213.063909839705,4.95297923710267,1.41303429370134));
#39002=CARTESIAN_POINT('Ctrl Pts',(213.143099410763,3.67800235519679,3.60568549841956));
#39003=CARTESIAN_POINT('Ctrl Pts',(213.22228898182,1.51109838586108,4.92394667990976));
#39004=CARTESIAN_POINT('Ctrl Pts',(213.301478552878,-1.02225167348779,5.0481353740166));
#39005=CARTESIAN_POINT('Ctrl Pts',(213.380668123935,-3.30770250121545,3.94813543356853));
#39006=CARTESIAN_POINT('Ctrl Pts',(213.459857694993,-4.79102511555983,1.89070028836437));
#39007=CARTESIAN_POINT('Ctrl Pts',(213.53904726605,-5.11250913807012,-0.625235596791949));
#39008=CARTESIAN_POINT('Ctrl Pts',(213.618236837108,-4.19419368668006,-2.98954989203382));
#39009=CARTESIAN_POINT('Ctrl Pts',(213.697426408165,-2.25877313371456,-4.62888897779538));
#39010=CARTESIAN_POINT('Ctrl Pts',(213.776615979223,0.224406976683579,-5.14570799279964));
#39011=CARTESIAN_POINT('Ctrl Pts',(213.85580555028,2.65316769258906,-4.41467670768176));
#39012=CARTESIAN_POINT('Ctrl Pts',(213.934995121338,4.43852693563516,-2.6130724980351));
#39013=CARTESIAN_POINT('Ctrl Pts',(214.014184692395,5.14752949919566,-0.177790025751574));
#39014=CARTESIAN_POINT('Ctrl Pts',(214.093374263453,4.60824004162965,2.30060708445997));
#39015=CARTESIAN_POINT('Ctrl Pts',(214.172563834511,2.95143794498097,4.2210997731957));
#39016=CARTESIAN_POINT('Ctrl Pts',(214.251753405568,0.578902905345666,5.11796255012955));
#39017=CARTESIAN_POINT('Ctrl Pts',(214.330942976626,-1.9340179014548,4.77370338366332));
#39018=CARTESIAN_POINT('Ctrl Pts',(214.410132547683,-3.97793331149569,3.27180619958444));
#39019=CARTESIAN_POINT('Ctrl Pts',(214.489322118741,-5.05718743808221,0.976485767663708));
#39020=CARTESIAN_POINT('Ctrl Pts',(214.568511689798,-4.91005777623474,-1.55563552041699));
#39021=CARTESIAN_POINT('Ctrl Pts',(214.647701260856,-3.57222372963305,-3.71051032390327));
#39022=CARTESIAN_POINT('Ctrl Pts',(214.726890831913,-1.36811424350713,-4.96557475576184));
#39023=CARTESIAN_POINT('Ctrl Pts',(214.806080402971,1.16776723040952,-5.0164717615001));
#39024=CARTESIAN_POINT('Ctrl Pts',(214.885269974028,3.42046149452369,-3.85085865786152));
#39025=CARTESIAN_POINT('Ctrl Pts',(214.964459545086,4.84368313631455,-1.75140027216177));
#39026=CARTESIAN_POINT('Ctrl Pts',(215.043649116144,5.09229645135928,0.772778163394885));
#39027=CARTESIAN_POINT('Ctrl Pts',(215.122838687201,4.10601193231954,3.10955547466126));
#39028=CARTESIAN_POINT('Ctrl Pts',(215.202028258259,2.12400666324514,4.69225584690738));
#39029=CARTESIAN_POINT('Ctrl Pts',(215.281217829316,-0.373076872202056,
5.1370694842268));
#39030=CARTESIAN_POINT('Ctrl Pts',(215.360407400374,-2.77968809798898,4.33612768680129));
#39031=CARTESIAN_POINT('Ctrl Pts',(215.439596971431,-4.51221625645552,2.48366134835748));
#39032=CARTESIAN_POINT('Ctrl Pts',(215.518786542489,-5.15051784440682,0.0288993562764492));
#39033=CARTESIAN_POINT('Ctrl Pts',(215.597976113546,-4.53980272816102,-2.43287082018918));
#39034=CARTESIAN_POINT('Ctrl Pts',(215.677165684604,-2.82817123563468,-4.30466220513002));
#39035=CARTESIAN_POINT('Ctrl Pts',(215.756355255662,-0.430699363101971,
-5.13255952688031));
#39036=CARTESIAN_POINT('Ctrl Pts',(215.835544826719,2.07121845355762,-4.71579509266345));
#39037=CARTESIAN_POINT('Ctrl Pts',(215.914734397777,4.07085930998026,-3.15543558271965));
#39038=CARTESIAN_POINT('Ctrl Pts',(215.993923968834,5.08330403735285,-0.829873063894976));
#39039=CARTESIAN_POINT('Ctrl Pts',(216.073113539892,4.86303161919394,1.69693627136268));
#39040=CARTESIAN_POINT('Ctrl Pts',(216.152303110949,3.46345880660808,3.81223324749093));
#39041=CARTESIAN_POINT('Ctrl Pts',(216.231492682007,1.22398638888836,5.00305172451398));
#39042=CARTESIAN_POINT('Ctrl Pts',(216.310682253064,-1.3123065605943,4.98061449314915));
#39043=CARTESIAN_POINT('Ctrl Pts',(216.389871824122,-3.53036106013357,3.75036265225628));
#39044=CARTESIAN_POINT('Ctrl Pts',(216.469061395179,-4.8922919485796,1.61063612532735));
#39045=CARTESIAN_POINT('Ctrl Pts',(216.548250966237,-5.06782672110485,-0.919674705100661));
#39046=CARTESIAN_POINT('Ctrl Pts',(216.627440537294,-4.01439764575017,-3.22696153992293));
#39047=CARTESIAN_POINT('Ctrl Pts',(216.706630108352,-1.98746457170991,-4.75170009728562));
#39048=CARTESIAN_POINT('Ctrl Pts',(216.78581967941,0.521434883975116,-5.12413650287735));
#39049=CARTESIAN_POINT('Ctrl Pts',(216.865009250467,2.90388474761705,-4.25395376219621));
#39050=CARTESIAN_POINT('Ctrl Pts',(216.944198821525,4.58213346752824,-2.35217391451056));
#39051=CARTESIAN_POINT('Ctrl Pts',(217.023388392582,5.14920047431936,0.120015472400531));
#39052=CARTESIAN_POINT('Ctrl Pts',(217.10257796364,4.46757024328443,2.56310073147072));
#39053=CARTESIAN_POINT('Ctrl Pts',(217.181767534698,2.70254023972065,4.38462603776387));
#39054=CARTESIAN_POINT('Ctrl Pts',(217.260957105755,0.282135766026347,5.1428658010758));
#39055=CARTESIAN_POINT('Ctrl Pts',(217.340146676812,-2.20668751433244,4.65394450465791));
#39056=CARTESIAN_POINT('Ctrl Pts',(217.41933624787,-4.16038216304547,3.03642709376651));
#39057=CARTESIAN_POINT('Ctrl Pts',(217.498525818927,-5.10517111053266,0.682566605196131));
#39058=CARTESIAN_POINT('Ctrl Pts',(217.577715389985,-4.81194007877364,-1.83681842233742));
#39059=CARTESIAN_POINT('Ctrl Pts',(217.656904961043,-3.35179851111375,-3.91076923114136));
#39060=CARTESIAN_POINT('Ctrl Pts',(217.7360945321,-1.0788353096,-5.03634625627613));
#39061=CARTESIAN_POINT('Ctrl Pts',(217.815284103158,1.45574883246274,-4.94059354482127));
#39062=CARTESIAN_POINT('Ctrl Pts',(217.894473674215,3.63730932451793,-3.64673142911857));
#39063=CARTESIAN_POINT('Ctrl Pts',(217.973663245273,4.93681091649799,-1.46852552347328));
#39064=CARTESIAN_POINT('Ctrl Pts',(218.05285281633,5.03912040344251,1.06580241975503));
#39065=CARTESIAN_POINT('Ctrl Pts',(218.132042387388,3.91942741442336,3.34166993902942));
#39066=CARTESIAN_POINT('Ctrl Pts',(218.211231958445,1.84926100517927,4.80717203489428));
#39067=CARTESIAN_POINT('Ctrl Pts',(218.290421529503,-0.669356988092899,
5.10691986042834));
#39068=CARTESIAN_POINT('Ctrl Pts',(218.369611100561,-3.02565381591041,4.16822362939094));
#39069=CARTESIAN_POINT('Ctrl Pts',(218.448800671618,-4.64822011966157,2.2187201169863));
#39070=CARTESIAN_POINT('Ctrl Pts',(218.527990242676,-5.1435784902246,-0.268829970883292));
#39071=CARTESIAN_POINT('Ctrl Pts',(218.607179813733,-4.3916029717077,-2.69118794907274));
#39072=CARTESIAN_POINT('Ctrl Pts',(218.686369384791,-2.57464998188252,-4.46092442315924));
#39073=CARTESIAN_POINT('Ctrl Pts',(218.765558955848,-0.13333630989329,-5.14887275690614));
#39074=CARTESIAN_POINT('Ctrl Pts',(218.844748526906,2.34031183473807,-4.58820332532585));
#39075=CARTESIAN_POINT('Ctrl Pts',(218.923938097963,4.24642703163054,-2.91488022110407));
#39076=CARTESIAN_POINT('Ctrl Pts',(219.003127669021,5.12277037724782,-0.534689536402703));
#39077=CARTESIAN_POINT('Ctrl Pts',(219.082317240078,4.75682586633489,1.97516503505748));
#39078=CARTESIAN_POINT('Ctrl Pts',(219.161506811136,3.2373361886071,4.0060359010225));
#39079=CARTESIAN_POINT('Ctrl Pts',(219.240696382194,0.93278234862948,5.06543051758008));
#39080=CARTESIAN_POINT('Ctrl Pts',(219.319885953251,-1.59797413155131,4.8964423731153));
#39081=CARTESIAN_POINT('Ctrl Pts',(219.399075524309,-3.74121688137005,3.54005162178436));
#39082=CARTESIAN_POINT('Ctrl Pts',(219.478265095366,-4.97720282322922,1.32518726781742));
#39083=CARTESIAN_POINT('Ctrl Pts',(219.557454666424,-5.00620149619827,-1.21103914792564));
#39084=CARTESIAN_POINT('Ctrl Pts',(219.636644237481,-3.82118063128369,-3.45358477837864));
#39085=CARTESIAN_POINT('Ctrl Pts',(219.715833808539,-1.70951149867879,-4.85862528646028));
#39086=CARTESIAN_POINT('Ctrl Pts',(219.795023379597,0.816719525054341,-5.08543394959972));
#39087=CARTESIAN_POINT('Ctrl Pts',(219.874212950654,3.14489350670873,-4.07900895681872));
#39088=CARTESIAN_POINT('Ctrl Pts',(219.953402521712,4.71042096592359,-2.08341152011178));
#39089=CARTESIAN_POINT('Ctrl Pts',(220.032592092769,5.1336565919727,0.417419733649592));
#39090=CARTESIAN_POINT('Ctrl Pts',(220.111781663827,4.31196442033532,2.81702539500632));
#39091=CARTESIAN_POINT('Ctrl Pts',(220.190971234884,2.44460737545468,4.53349357760849));
#39092=CARTESIAN_POINT('Ctrl Pts',(220.270160805942,-0.0155746123486556,
5.1505753726931));
#39093=CARTESIAN_POINT('Ctrl Pts',(220.349350376999,-2.47197970789699,4.51862651279263));
#39094=CARTESIAN_POINT('Ctrl Pts',(220.428539948057,-4.32892198418446,2.79089657514049));
#39095=CARTESIAN_POINT('Ctrl Pts',(220.507729519114,-5.13608712492566,0.386365479370735));
#39096=CARTESIAN_POINT('Ctrl Pts',(220.586919090172,-4.69773505607432,-2.11186045492126));
#39097=CARTESIAN_POINT('Ctrl Pts',(220.66610866123,-3.12016752703196,-4.09795361635802));
#39098=CARTESIAN_POINT('Ctrl Pts',(220.745298232287,-0.785949602798,-5.09028019468105));
#39099=CARTESIAN_POINT('Ctrl Pts',(220.824487803345,1.73886356050538,-4.84819788733142));
#39100=CARTESIAN_POINT('Ctrl Pts',(220.903677374402,3.84199686688144,-3.43041241228741));
#39101=CARTESIAN_POINT('Ctrl Pts',(220.98286694546,5.01343390092321,-1.18074118554751));
#39102=CARTESIAN_POINT('Ctrl Pts',(221.062056516517,4.96909752124399,1.35526347434335));
#39103=CARTESIAN_POINT('Ctrl Pts',(221.141246087575,3.71973942326616,3.56261250116638));
#39104=CARTESIAN_POINT('Ctrl Pts',(221.220435658633,1.56833289050138,4.90601683517051));
#39105=CARTESIAN_POINT('Ctrl Pts',(221.29962522969,-0.963399326280619,5.05969673864025));
#39106=CARTESIAN_POINT('Ctrl Pts',(221.378814800748,-3.26150408922802,3.98638431206907));
#39107=CARTESIAN_POINT('Ctrl Pts',(221.458004371805,-4.76868411213275,1.94636126816844));
#39108=CARTESIAN_POINT('Ctrl Pts',(221.537193942863,-5.11944285257571,-0.565660605443682));
#39109=CARTESIAN_POINT('Ctrl Pts',(221.61638351392,-4.22872163540365,-2.94050773958088));
#39110=CARTESIAN_POINT('Ctrl Pts',(221.695573084978,-2.31252013462662,-4.60227311630824));
#39111=CARTESIAN_POINT('Ctrl Pts',(221.774762656035,0.164470394917766,-5.14797162841751));
#39112=CARTESIAN_POINT('Ctrl Pts',(221.853952227093,2.60158556523968,-4.44527350328976));
#39113=CARTESIAN_POINT('Ctrl Pts',(221.93314179815,4.40778851090815,-2.6645771347152));
#39114=CARTESIAN_POINT('Ctrl Pts',(222.012331369208,5.1451305867893,-0.237724303700579));
#39115=CARTESIAN_POINT('Ctrl Pts',(222.091520940265,4.63467444150074,2.24680150964327));
#39116=CARTESIAN_POINT('Ctrl Pts',(222.170710511323,3.00048534671845,4.18641270900455));
#39117=CARTESIAN_POINT('Ctrl Pts',(222.24990008238,0.638283697933631,5.11088637052273));
#39118=CARTESIAN_POINT('Ctrl Pts',(222.302693129752,-1.03902234995174,4.90057399389068));
#39119=CARTESIAN_POINT('Ctrl Pts',(222.329089653438,-1.80222833897997,4.6016667647905));
#39120=CARTESIAN_POINT('',(222.,4.90426805507063,-0.609523456491791));
#39121=CARTESIAN_POINT('Ctrl Pts',(222.,4.90448285458831,-0.609441531220142));
#39122=CARTESIAN_POINT('Ctrl Pts',(222.,4.91326917733984,-0.482075978558733));
#39123=CARTESIAN_POINT('Ctrl Pts',(222.,4.91707785477246,-0.354546138090381));
#39124=CARTESIAN_POINT('Ctrl Pts',(222.,4.91582655810574,-0.227126274667179));
#39125=CARTESIAN_POINT('Ctrl Pts',(222.,4.9143947739523,-0.0813273237593178));
#39126=CARTESIAN_POINT('Ctrl Pts',(222.,4.90633894433518,0.0643283824542994));
#39127=CARTESIAN_POINT('Ctrl Pts',(222.,4.89177207858516,0.209411418078174));
#39128=CARTESIAN_POINT('Ctrl Pts',(222.,4.88353154766168,0.291485438807731));
#39129=CARTESIAN_POINT('Ctrl Pts',(222.,4.87320640955617,0.373376035009041));
#39130=CARTESIAN_POINT('Ctrl Pts',(222.,4.86081007005833,0.455003302996157));
#39131=CARTESIAN_POINT('Ctrl Pts',(222.,4.85194006741065,0.513410390289533));
#39132=CARTESIAN_POINT('Ctrl Pts',(222.,4.84200952702687,0.571682622382685));
#39133=CARTESIAN_POINT('Ctrl Pts',(222.,4.8310218344987,0.629789994814728));
#39134=CARTESIAN_POINT('Ctrl Pts',(222.,4.82673488428677,0.652461125438654));
#39135=CARTESIAN_POINT('Ctrl Pts',(222.,4.8222869719834,0.675106928971051));
#39136=CARTESIAN_POINT('Ctrl Pts',(222.,4.81768123655949,0.697711955872851));
#39137=CARTESIAN_POINT('Ctrl Pts',(222.,4.78883957014647,0.83926733957451));
#39138=CARTESIAN_POINT('Ctrl Pts',(222.,4.75378779279869,0.979361892009339));
#39139=CARTESIAN_POINT('Ctrl Pts',(222.,4.71263944483955,1.11757740639638));
#39140=CARTESIAN_POINT('Ctrl Pts',(222.,4.67174027328832,1.25495594804698));
#39141=CARTESIAN_POINT('Ctrl Pts',(222.,4.62481784578113,1.3904788562509));
#39142=CARTESIAN_POINT('Ctrl Pts',(222.,4.57193686941057,1.52371480352769));
#39143=CARTESIAN_POINT('Ctrl Pts',(222.,4.53175843227578,1.62494614415654));
#39144=CARTESIAN_POINT('Ctrl Pts',(222.,4.48813926663806,1.72485692666779));
#39145=CARTESIAN_POINT('Ctrl Pts',(222.,4.44109105421273,1.82324608763217));
#39146=CARTESIAN_POINT('Ctrl Pts',(222.,4.43330321241965,1.83953234337379));
#39147=CARTESIAN_POINT('Ctrl Pts',(222.,4.42542221910461,1.85577505560334));
#39148=CARTESIAN_POINT('Ctrl Pts',(222.,4.41745220772723,1.87196530421876));
#39149=CARTESIAN_POINT('Ctrl Pts',(222.,4.38168626708121,1.94462009021658));
#39150=CARTESIAN_POINT('Ctrl Pts',(222.,4.34410598143193,2.016264933338));
#39151=CARTESIAN_POINT('Ctrl Pts',(222.,4.30473188164448,2.08682740943665));
#39152=CARTESIAN_POINT('Ctrl Pts',(222.,4.23575714136261,2.21043730753777));
#39153=CARTESIAN_POINT('Ctrl Pts',(222.,4.16128012266586,2.33072748027458));
#39154=CARTESIAN_POINT('Ctrl Pts',(222.,4.08162279945473,2.44740940981428));
#39155=CARTESIAN_POINT('Ctrl Pts',(222.,4.00157270449037,2.56466667083873));
#39156=CARTESIAN_POINT('Ctrl Pts',(222.,3.91629052773537,2.67828059710419));
#39157=CARTESIAN_POINT('Ctrl Pts',(222.,3.82606285547984,2.78792472525375));
#39158=CARTESIAN_POINT('Ctrl Pts',(222.,3.74674547067526,2.88431073728974));
#39159=CARTESIAN_POINT('Ctrl Pts',(222.,3.66360545427877,2.97762870520231));
#39160=CARTESIAN_POINT('Ctrl Pts',(222.,3.57681726235579,3.06763019115416));
#39161=CARTESIAN_POINT('Ctrl Pts',(222.,3.51172611841355,3.13513130561804));
#39162=CARTESIAN_POINT('Ctrl Pts',(222.,3.44458246403701,3.20076641165242));
#39163=CARTESIAN_POINT('Ctrl Pts',(222.,3.37545454247196,3.26441991676624));
#39164=CARTESIAN_POINT('Ctrl Pts',(222.,3.36073243108146,3.27797614660021));
#39165=CARTESIAN_POINT('Ctrl Pts',(222.,3.34591878431476,3.29144382870828));
#39166=CARTESIAN_POINT('Ctrl Pts',(222.,3.33101906241501,3.30481746426802));
#39167=CARTESIAN_POINT('Ctrl Pts',(222.,3.22694638125945,3.39823062451785));
#39168=CARTESIAN_POINT('Ctrl Pts',(222.,3.1189736864245,3.48679412040944));
#39169=CARTESIAN_POINT('Ctrl Pts',(222.,3.00739305624753,3.57022036306246));
#39170=CARTESIAN_POINT('Ctrl Pts',(222.,2.90992116374936,3.64309783061666));
#39171=CARTESIAN_POINT('Ctrl Pts',(222.,2.80969522479396,3.71205475252624));
#39172=CARTESIAN_POINT('Ctrl Pts',(222.,2.7068907197599,3.77687313241435));
#39173=CARTESIAN_POINT('Ctrl Pts',(222.,2.58891295229675,3.85125827484798));
#39174=CARTESIAN_POINT('Ctrl Pts',(222.,2.46753906543956,3.92019422568834));
#39175=CARTESIAN_POINT('Ctrl Pts',(222.,2.34317914443504,3.98353319537002));
#39176=CARTESIAN_POINT('Ctrl Pts',(222.,2.21947820439344,4.04653653300165));
#39177=CARTESIAN_POINT('Ctrl Pts',(222.,2.09282200300289,4.10400221753901));
#39178=CARTESIAN_POINT('Ctrl Pts',(222.,1.96360433617035,4.15573443747871));
#39179=CARTESIAN_POINT('Ctrl Pts',(222.,1.91350917960701,4.1757900051172));
#39180=CARTESIAN_POINT('Ctrl Pts',(222.,1.86302900287319,4.19498330383357));
#39181=CARTESIAN_POINT('Ctrl Pts',(222.,1.81218673898867,4.21330078673186));
#39182=CARTESIAN_POINT('Ctrl Pts',(222.,1.79518182048063,4.21942732949686));
#39183=CARTESIAN_POINT('Ctrl Pts',(222.,1.77813690967813,4.2254556476935));
#39184=CARTESIAN_POINT('Ctrl Pts',(222.,1.76106556469781,4.23138098370753));
#39185=CARTESIAN_POINT('Ctrl Pts',(222.,1.63109802355043,4.27649174405501));
#39186=CARTESIAN_POINT('Ctrl Pts',(222.,1.49941025889044,4.31570662400781));
#39187=CARTESIAN_POINT('Ctrl Pts',(222.,1.36640605860325,4.34892093575254));
#39188=CARTESIAN_POINT('Ctrl Pts',(222.,1.23393413223417,4.38200232604207));
#39189=CARTESIAN_POINT('Ctrl Pts',(222.,1.10015550342008,4.40913122338652));
#39190=CARTESIAN_POINT('Ctrl Pts',(222.,0.965458418930057,4.43015396750657));
#39191=CARTESIAN_POINT('Ctrl Pts',(222.,0.830761334440031,4.45117671162661));
#39192=CARTESIAN_POINT('Ctrl Pts',(222.,0.695145040010488,4.46609348868625));
#39193=CARTESIAN_POINT('Ctrl Pts',(222.,0.558998530275823,4.47469779566404));
#39194=CARTESIAN_POINT('Ctrl Pts',(222.,0.467028797805401,4.48051017978159));
#39195=CARTESIAN_POINT('Ctrl Pts',(222.,0.374817124048172,4.48344078212688));
#39196=CARTESIAN_POINT('Ctrl Pts',(222.,0.282495436056599,4.48349800210454));
#39197=CARTESIAN_POINT('Ctrl Pts',(222.,0.239680782870147,4.48352453816071));
#39198=CARTESIAN_POINT('Ctrl Pts',(222.,0.196842516440346,4.48293295657145));
#39199=CARTESIAN_POINT('Ctrl Pts',(222.,0.153994089551905,4.48172336523466));
#39200=CARTESIAN_POINT('Ctrl Pts',(222.,0.12621552348811,4.48093918912134));
#39201=CARTESIAN_POINT('Ctrl Pts',(222.,0.0984326912053478,4.4798952598853));
#39202=CARTESIAN_POINT('Ctrl Pts',(222.,0.0706493101151461,4.47859150531125));
#39203=CARTESIAN_POINT('Ctrl Pts',(222.,0.0514392659198498,4.47769006056246));
#39204=CARTESIAN_POINT('Ctrl Pts',(222.,0.032237116105233,4.47666475864222));
#39205=CARTESIAN_POINT('Ctrl Pts',(222.,0.0130498828690303,4.47551629094421));
#39206=CARTESIAN_POINT('Ctrl Pts',(222.,-0.126040864975259,4.46719089931406));
#39207=CARTESIAN_POINT('Ctrl Pts',(222.,-0.264445813962418,4.45239355914002));
#39208=CARTESIAN_POINT('Ctrl Pts',(222.,-0.401723720439985,4.43124956761349));
#39209=CARTESIAN_POINT('Ctrl Pts',(222.,-0.534675001036407,4.4107719771366));
#39210=CARTESIAN_POINT('Ctrl Pts',(222.,-0.666569928590543,4.38434097588717));
#39211=CARTESIAN_POINT('Ctrl Pts',(222.,-0.796997369050306,4.35201860521038));
#39212=CARTESIAN_POINT('Ctrl Pts',(222.,-0.926299184341642,4.31997518560255));
#39213=CARTESIAN_POINT('Ctrl Pts',(222.,-1.0541594515063,4.28214138070619));
#39214=CARTESIAN_POINT('Ctrl Pts',(222.,-1.18015635582318,4.23853132977908));
#39215=CARTESIAN_POINT('Ctrl Pts',(222.,-1.30349968543307,4.1958397341802));
#39216=CARTESIAN_POINT('Ctrl Pts',(222.,-1.4250578919995,4.14761231940487));
#39217=CARTESIAN_POINT('Ctrl Pts',(222.,-1.54440537989462,4.0938221719545));
#39218=CARTESIAN_POINT('Ctrl Pts',(222.,-1.5611016741838,4.08629711929081));
#39219=CARTESIAN_POINT('Ctrl Pts',(222.,-1.57775464564182,4.07866313700196));
#39220=CARTESIAN_POINT('Ctrl Pts',(222.,-1.59436307123033,4.07092009220237));
#39221=CARTESIAN_POINT('Ctrl Pts',(221.519679545343,-4.94203042585278,-0.000125883567849882));
#39222=CARTESIAN_POINT('Ctrl Pts',(221.52551767785,-4.94221599753283,-0.181402702505943));
#39223=CARTESIAN_POINT('Ctrl Pts',(221.531355810356,-4.93243348869434,-0.362659600138765));
#39224=CARTESIAN_POINT('Ctrl Pts',(221.537193942863,-4.91252952630654,-0.542798148864529));
#39225=CARTESIAN_POINT('Ctrl Pts',(221.563590466548,-4.82253578018502,-1.35727631682275));
#39226=CARTESIAN_POINT('Ctrl Pts',(221.589986990234,-4.52562870779433,-2.14889202820181));
#39227=CARTESIAN_POINT('Ctrl Pts',(221.61638351392,-4.05780825480282,-2.82166078001257));
#39228=CARTESIAN_POINT('Ctrl Pts',(221.642780037606,-3.58998780181129,-3.49442953182335));
#39229=CARTESIAN_POINT('Ctrl Pts',(221.669176561292,-2.95125396821893,-4.04835132406582));
#39230=CARTESIAN_POINT('Ctrl Pts',(221.695573084978,-2.21905529649866,-4.41626197220526));
#39231=CARTESIAN_POINT('Ctrl Pts',(221.721969608664,-1.48685662477844,-4.78417262034468));
#39232=CARTESIAN_POINT('Ctrl Pts',(221.748366132349,-0.661193114930324,
-4.96607212438109));
#39233=CARTESIAN_POINT('Ctrl Pts',(221.774762656035,0.157824501714043,-4.93990552221134));
#39234=CARTESIAN_POINT('Ctrl Pts',(221.801159179721,0.976842118358411,-4.91373892004159));
#39235=CARTESIAN_POINT('Ctrl Pts',(221.827555703407,1.78921384179903,-4.67950621166568));
#39236=CARTESIAN_POINT('Ctrl Pts',(221.853952227093,2.49643352779742,-4.26560712938197));
#39237=CARTESIAN_POINT('Ctrl Pts',(221.880348750779,3.20365321379582,-3.85170804709825));
#39238=CARTESIAN_POINT('Ctrl Pts',(221.906745274465,3.80572086235198,-3.25814259090672));
#39239=CARTESIAN_POINT('Ctrl Pts',(221.93314179815,4.22964503261026,-2.55688439097519));
#39240=CARTESIAN_POINT('Ctrl Pts',(221.955427865434,4.58755589594206,-1.9648258452143));
#39241=CARTESIAN_POINT('Ctrl Pts',(221.977713932717,4.81848441783212,-1.29600290208645));
#39242=CARTESIAN_POINT('Ctrl Pts',(222.,4.90448285458833,-0.609441531219933));
#39243=CARTESIAN_POINT('',(209.342,-2.53854069360603,-3.55974239505386));
#39244=CARTESIAN_POINT('Ctrl Pts',(209.342,-2.53854069360617,-3.55974239505377));
#39245=CARTESIAN_POINT('Ctrl Pts',(209.342,-2.6349877013993,-3.49987489435206));
#39246=CARTESIAN_POINT('Ctrl Pts',(209.342,-2.72895943133216,-3.43630922016219));
#39247=CARTESIAN_POINT('Ctrl Pts',(209.342,-2.82022491817566,-3.36916885592227));
#39248=CARTESIAN_POINT('Ctrl Pts',(209.342,-2.92748910751928,-3.29025888686925));
#39249=CARTESIAN_POINT('Ctrl Pts',(209.342,-3.03101625922222,-3.20641213996167));
#39250=CARTESIAN_POINT('Ctrl Pts',(209.342,-3.13058845059508,-3.11799396863395));
#39251=CARTESIAN_POINT('Ctrl Pts',(209.342,-3.18739359422047,-3.06755210477501));
#39252=CARTESIAN_POINT('Ctrl Pts',(209.342,-3.24291112510208,-3.01562153815868));
#39253=CARTESIAN_POINT('Ctrl Pts',(209.342,-3.29709651834796,-2.96226376957147));
#39254=CARTESIAN_POINT('Ctrl Pts',(209.342,-3.33383376776623,-2.92608764284123));
#39255=CARTESIAN_POINT('Ctrl Pts',(209.342,-3.3699586062124,-2.88925537752558));
#39256=CARTESIAN_POINT('Ctrl Pts',(209.342,-3.40545624307948,-2.85178508415988));
#39257=CARTESIAN_POINT('Ctrl Pts',(209.342,-3.41889230282954,-2.83760236257764));
#39258=CARTESIAN_POINT('Ctrl Pts',(209.342,-3.43223749900502,-2.8233292174573));
#39259=CARTESIAN_POINT('Ctrl Pts',(209.342,-3.44548459322086,-2.80897381138868));
#39260=CARTESIAN_POINT('Ctrl Pts',(209.342,-3.53764467726692,-2.70910319763421));
#39261=CARTESIAN_POINT('Ctrl Pts',(209.342,-3.62514721021095,-2.60516218242286));
#39262=CARTESIAN_POINT('Ctrl Pts',(209.342,-3.70776805623344,-2.49753092189412));
#39263=CARTESIAN_POINT('Ctrl Pts',(209.342,-3.79069451449376,-2.38950153629195));
#39264=CARTESIAN_POINT('Ctrl Pts',(209.342,-3.86870367845508,-2.27775398082505));
#39265=CARTESIAN_POINT('Ctrl Pts',(209.342,-3.9415356848087,-2.1626319845035));
#39266=CARTESIAN_POINT('Ctrl Pts',(209.342,-3.97091706474444,-2.11619027182486));
#39267=CARTESIAN_POINT('Ctrl Pts',(209.342,-3.99945547881667,-2.06919898329292));
#39268=CARTESIAN_POINT('Ctrl Pts',(209.342,-4.02713201378103,-2.02167914966254));
#39269=CARTESIAN_POINT('Ctrl Pts',(209.342,-4.04218110507543,-1.99584028235061));
#39270=CARTESIAN_POINT('Ctrl Pts',(209.342,-4.05697535079495,-1.96984512974782));
#39271=CARTESIAN_POINT('Ctrl Pts',(209.342,-4.07151156318289,-1.94369697898506));
#39272=CARTESIAN_POINT('Ctrl Pts',(209.342,-4.08507675832336,-1.91929552156319));
#39273=CARTESIAN_POINT('Ctrl Pts',(209.342,-4.09841961397682,-1.89475615326754));
#39274=CARTESIAN_POINT('Ctrl Pts',(209.342,-4.11152305824316,-1.87010919482169));
#39275=CARTESIAN_POINT('Ctrl Pts',(209.342,-4.14743612631779,-1.80255841362961));
#39276=CARTESIAN_POINT('Ctrl Pts',(209.342,-4.18157046256384,-1.73416632118921));
#39277=CARTESIAN_POINT('Ctrl Pts',(209.342,-4.2138886632462,-1.66499821702773));
#39278=CARTESIAN_POINT('Ctrl Pts',(209.342,-4.27122750314795,-1.54228040579181));
#39279=CARTESIAN_POINT('Ctrl Pts',(209.342,-4.32285214674876,-1.41712175506451));
#39280=CARTESIAN_POINT('Ctrl Pts',(209.342,-4.36877501690254,-1.289957099055));
#39281=CARTESIAN_POINT('Ctrl Pts',(209.342,-4.41534596983229,-1.16099784216372));
#39282=CARTESIAN_POINT('Ctrl Pts',(209.342,-4.45605337158386,-1.029974895541));
#39283=CARTESIAN_POINT('Ctrl Pts',(209.342,-4.49086552156863,-0.89731224357485));
#39284=CARTESIAN_POINT('Ctrl Pts',(209.342,-4.52200890075814,-0.778630597187785));
#39285=CARTESIAN_POINT('Ctrl Pts',(209.342,-4.54843362771313,-0.658635879371086));
#39286=CARTESIAN_POINT('Ctrl Pts',(209.342,-4.57008457584423,-0.537618862846069));
#39287=CARTESIAN_POINT('Ctrl Pts',(209.342,-4.58632278694256,-0.446856100452307));
#39288=CARTESIAN_POINT('Ctrl Pts',(209.342,-4.59987513097013,-0.355518010485838));
#39289=CARTESIAN_POINT('Ctrl Pts',(209.342,-4.61070640337213,-0.263725114165152));
#39290=CARTESIAN_POINT('Ctrl Pts',(209.342,-4.61385708563983,-0.237023703656357));
#39291=CARTESIAN_POINT('Ctrl Pts',(209.342,-4.61677798423051,-0.210277609469452));
#39292=CARTESIAN_POINT('Ctrl Pts',(209.342,-4.61946488160656,-0.183524245181616));
#39293=CARTESIAN_POINT('Ctrl Pts',(209.342,-4.63351223708837,-0.0436551077019361));
#39294=CARTESIAN_POINT('Ctrl Pts',(209.342,-4.64118722474554,0.0965531284597916));
#39295=CARTESIAN_POINT('Ctrl Pts',(209.342,-4.64248214861728,0.2366538474554));
#39296=CARTESIAN_POINT('Ctrl Pts',(209.342,-4.64349398598631,0.346126802585117));
#39297=CARTESIAN_POINT('Ctrl Pts',(209.342,-4.64060947998757,0.455534806659313));
#39298=CARTESIAN_POINT('Ctrl Pts',(209.342,-4.63380417679374,0.564672361043244));
#39299=CARTESIAN_POINT('Ctrl Pts',(209.342,-4.62513626605827,0.703680800835413));
#39300=CARTESIAN_POINT('Ctrl Pts',(209.342,-4.61010947807627,0.84225083434342));
#39301=CARTESIAN_POINT('Ctrl Pts',(209.342,-4.5889023314112,0.979995389180269));
#39302=CARTESIAN_POINT('Ctrl Pts',(209.342,-4.56757070635119,1.11854845547648));
#39303=CARTESIAN_POINT('Ctrl Pts',(209.342,-4.5399858294126,1.25626708770862));
#39304=CARTESIAN_POINT('Ctrl Pts',(209.342,-4.50627697501283,1.39275336470125));
#39305=CARTESIAN_POINT('Ctrl Pts',(209.342,-4.49324560349942,1.44551704990042));
#39306=CARTESIAN_POINT('Ctrl Pts',(209.342,-4.47929846871971,1.49809645764725));
#39307=CARTESIAN_POINT('Ctrl Pts',(209.342,-4.46444102040819,1.55046805929348));
#39308=CARTESIAN_POINT('Ctrl Pts',(209.342,-4.45834510918231,1.5719557756024));
#39309=CARTESIAN_POINT('Ctrl Pts',(209.342,-4.45209528668334,1.59341042954444));
#39310=CARTESIAN_POINT('Ctrl Pts',(209.342,-4.44569855505466,1.61480883852867));
#39311=CARTESIAN_POINT('Ctrl Pts',(209.342,-4.40499058452271,1.75098553827577));
#39312=CARTESIAN_POINT('Ctrl Pts',(209.342,-4.35828425914468,1.88507637301277));
#39313=CARTESIAN_POINT('Ctrl Pts',(209.342,-4.30579956169708,2.01668804744628));
#39314=CARTESIAN_POINT('Ctrl Pts',(209.342,-4.25229708069577,2.15085193622469));
#39315=CARTESIAN_POINT('Ctrl Pts',(209.342,-4.19278989677581,2.28244039276155));
#39316=CARTESIAN_POINT('Ctrl Pts',(209.342,-4.12745611479573,2.41103351755446));
#39317=CARTESIAN_POINT('Ctrl Pts',(209.342,-4.06212233281564,2.53962664234737));
#39318=CARTESIAN_POINT('Ctrl Pts',(209.342,-3.99096173488706,2.66522526969368));
#39319=CARTESIAN_POINT('Ctrl Pts',(209.342,-3.91410031164534,2.78739382776747));
#39320=CARTESIAN_POINT('Ctrl Pts',(209.342,-3.86029917566832,2.87290886154941));
#39321=CARTESIAN_POINT('Ctrl Pts',(209.342,-3.80370370371757,2.95674294064152));
#39322=CARTESIAN_POINT('Ctrl Pts',(209.342,-3.74442332099379,3.03879836555337));
#39323=CARTESIAN_POINT('Ctrl Pts',(209.342,-3.71848815355214,3.07469761395231));
#39324=CARTESIAN_POINT('Ctrl Pts',(209.342,-3.69203893552856,3.110256321026));
#39325=CARTESIAN_POINT('Ctrl Pts',(209.342,-3.66508419824396,3.14546582364801));
#39326=CARTESIAN_POINT('Ctrl Pts',(209.342,-3.64819963435168,3.16752120821214));
#39327=CARTESIAN_POINT('Ctrl Pts',(209.342,-3.6311167062146,3.18943956499776));
#39328=CARTESIAN_POINT('Ctrl Pts',(209.342,-3.61383743942568,3.21121869963276));
#39329=CARTESIAN_POINT('Ctrl Pts',(209.342,-3.60229869835278,3.22576236044978));
#39330=CARTESIAN_POINT('Ctrl Pts',(209.342,-3.59067553940754,3.24023993544928));
#39331=CARTESIAN_POINT('Ctrl Pts',(209.342,-3.57897369494969,3.25464484972412));
#39332=CARTESIAN_POINT('Ctrl Pts',(209.342,-3.48891908829218,3.36550163761165));
#39333=CARTESIAN_POINT('Ctrl Pts',(209.342,-3.39412108048915,3.47216689410339));
#39334=CARTESIAN_POINT('Ctrl Pts',(209.342,-3.29496106328392,3.57441629318392));
#39335=CARTESIAN_POINT('Ctrl Pts',(209.342,-3.19397353135956,3.67855014415453));
#39336=CARTESIAN_POINT('Ctrl Pts',(209.342,-3.08846133700036,3.77810448924538));
#39337=CARTESIAN_POINT('Ctrl Pts',(209.342,-2.9787792577949,3.87281847405827));
#39338=CARTESIAN_POINT('Ctrl Pts',(209.342,-2.86895681661178,3.96765366592994));
#39339=CARTESIAN_POINT('Ctrl Pts',(209.342,-2.75495327666192,4.05763668470962));
#39340=CARTESIAN_POINT('Ctrl Pts',(209.342,-2.6370841846052,4.14247293811633));
#39341=CARTESIAN_POINT('Ctrl Pts',(209.342,-2.52058663017021,4.2263220276177));
#39342=CARTESIAN_POINT('Ctrl Pts',(209.342,-2.4003123772207,4.30514392692405));
#39343=CARTESIAN_POINT('Ctrl Pts',(209.342,-2.27653488851178,4.37861434524912));
#39344=CARTESIAN_POINT('Ctrl Pts',(209.342,-2.24103337778535,4.39968692372401));
#39345=CARTESIAN_POINT('Ctrl Pts',(209.342,-2.20524350840695,4.42031898826745));
#39346=CARTESIAN_POINT('Ctrl Pts',(209.342,-2.16917135428551,4.44050218283329));
#39347=CARTESIAN_POINT('Ctrl Pts',(209.342,-2.53854069360603,-3.55974239505386));
#39348=CARTESIAN_POINT('Ctrl Pts',(209.364286067283,-2.03981491325066,-3.91465767403852));
#39349=CARTESIAN_POINT('Ctrl Pts',(209.412968658252,-0.786126241680141,
-4.46051691609693));
#39350=CARTESIAN_POINT('Ctrl Pts',(209.488047772907,1.33865191662591,-4.35546678832985));
#39351=CARTESIAN_POINT('Ctrl Pts',(209.567237343965,3.25513899273275,-3.1884349607263));
#39352=CARTESIAN_POINT('Ctrl Pts',(209.646426915022,4.38224084314362,-1.24820523943406));
#39353=CARTESIAN_POINT('Ctrl Pts',(209.72561648608,4.4466373711158,0.994721723380339));
#39354=CARTESIAN_POINT('Ctrl Pts',(209.804806057137,3.43270956435134,2.99642387551628));
#39355=CARTESIAN_POINT('Ctrl Pts',(209.883995628195,1.58633933997099,4.27148464599025));
#39356=CARTESIAN_POINT('Ctrl Pts',(209.963185199253,-0.644723329766792,
4.51069664301433));
#39357=CARTESIAN_POINT('Ctrl Pts',(210.04237477031,-2.71943848460081,3.6560507558529));
#39358=CARTESIAN_POINT('Ctrl Pts',(210.118176334528,-4.07413229445598,1.98929778409173));
#39359=CARTESIAN_POINT('Ctrl Pts',(210.167581375059,-4.3716724462746,0.631855615331185));
#39360=CARTESIAN_POINT('Ctrl Pts',(210.190589891905,-4.37223008469844,-8.48050595506078E-5));
#39361=CARTESIAN_POINT('Origin',(209.342,-4.51336705371395E-16,0.));
#39362=CARTESIAN_POINT('',(209.342,-4.94200000000001,-6.05220448138623E-16));
#39363=CARTESIAN_POINT('Origin',(209.342,0.,0.));
#39364=CARTESIAN_POINT('Origin',(209.342,0.,0.));
#39365=CARTESIAN_POINT('',(209.342,2.5383587572263,-3.55965150255085));
#39366=CARTESIAN_POINT('Ctrl Pts',(209.342,2.16935732978974,4.44063731407447));
#39367=CARTESIAN_POINT('Ctrl Pts',(209.342,2.28083034847072,4.37840428778324));
#39368=CARTESIAN_POINT('Ctrl Pts',(209.342,2.38972120560265,4.31191257789851));
#39369=CARTESIAN_POINT('Ctrl Pts',(209.342,2.4957552127191,4.24124308848005));
#39370=CARTESIAN_POINT('Ctrl Pts',(209.342,2.61708360362285,4.16038020618121));
#39371=CARTESIAN_POINT('Ctrl Pts',(209.342,2.73467268219725,4.07404776792419));
#39372=CARTESIAN_POINT('Ctrl Pts',(209.342,2.84822453982244,3.98257505818366));
#39373=CARTESIAN_POINT('Ctrl Pts',(209.342,2.91246125417312,3.9308286011078));
#39374=CARTESIAN_POINT('Ctrl Pts',(209.342,2.97540532777855,3.87743644914975));
#39375=CARTESIAN_POINT('Ctrl Pts',(209.342,3.03699716389969,3.82245348897652));
#39376=CARTESIAN_POINT('Ctrl Pts',(209.342,3.08106821799472,3.78311131045575));
#39377=CARTESIAN_POINT('Ctrl Pts',(209.342,3.12444685526241,3.74295458595479));
#39378=CARTESIAN_POINT('Ctrl Pts',(209.342,3.16710979599021,3.70200254527677));
#39379=CARTESIAN_POINT('Ctrl Pts',(209.342,3.18375513858242,3.68602472623038));
#39380=CARTESIAN_POINT('Ctrl Pts',(209.342,3.20029132024471,3.66992593549385));
#39381=CARTESIAN_POINT('Ctrl Pts',(209.342,3.21670711667039,3.65371724358499));
#39382=CARTESIAN_POINT('Ctrl Pts',(209.342,3.31950479669339,3.55221647680933));
#39383=CARTESIAN_POINT('Ctrl Pts',(209.342,3.41768582005176,3.44631275793146));
#39384=CARTESIAN_POINT('Ctrl Pts',(209.342,3.51096196457959,3.33632968608582));
#39385=CARTESIAN_POINT('Ctrl Pts',(209.342,3.60367326944256,3.22701262377301));
#39386=CARTESIAN_POINT('Ctrl Pts',(209.342,3.69153935620988,3.11366482343842));
#39387=CARTESIAN_POINT('Ctrl Pts',(209.342,3.77423433156167,2.996576154091));
#39388=CARTESIAN_POINT('Ctrl Pts',(209.342,3.83706514758663,2.90761335301298));
#39389=CARTESIAN_POINT('Ctrl Pts',(209.342,3.89690996444767,2.81649039091281));
#39390=CARTESIAN_POINT('Ctrl Pts',(209.342,3.95360676868133,2.72332691152732));
#39391=CARTESIAN_POINT('Ctrl Pts',(209.342,3.96299173203349,2.70790565716191));
#39392=CARTESIAN_POINT('Ctrl Pts',(209.342,3.97228932900057,2.69243017771718));
#39393=CARTESIAN_POINT('Ctrl Pts',(209.342,3.98149434724664,2.67690880897368));
#39394=CARTESIAN_POINT('Ctrl Pts',(209.342,4.02280245884576,2.60725566814465));
#39395=CARTESIAN_POINT('Ctrl Pts',(209.342,4.06227336715778,2.53663478972804));
#39396=CARTESIAN_POINT('Ctrl Pts',(209.342,4.0998576328727,2.46510294105804));
#39397=CARTESIAN_POINT('Ctrl Pts',(209.342,4.16569698017407,2.33979491286836));
#39398=CARTESIAN_POINT('Ctrl Pts',(209.342,4.22574955040824,2.21169245175744));
#39399=CARTESIAN_POINT('Ctrl Pts',(209.342,4.27994962666695,2.08122286415638));
#39400=CARTESIAN_POINT('Ctrl Pts',(209.342,4.33441695131631,1.95010996035133));
#39401=CARTESIAN_POINT('Ctrl Pts',(209.342,4.3829741009233,1.81660573893223));
#39402=CARTESIAN_POINT('Ctrl Pts',(209.342,4.42550424254866,1.68112860143975));
#39403=CARTESIAN_POINT('Ctrl Pts',(209.342,4.46289165918603,1.56203329654074));
#39404=CARTESIAN_POINT('Ctrl Pts',(209.342,4.49562083867352,1.44141279236264));
#39405=CARTESIAN_POINT('Ctrl Pts',(209.342,4.52357902926892,1.31954894560292));
#39406=CARTESIAN_POINT('Ctrl Pts',(209.342,4.54454767221548,1.22815106053312));
#39407=CARTESIAN_POINT('Ctrl Pts',(209.342,4.56283200080972,1.13605371672259));
#39408=CARTESIAN_POINT('Ctrl Pts',(209.342,4.57837249086842,1.04337722880969));
#39409=CARTESIAN_POINT('Ctrl Pts',(209.342,4.58168213497945,1.02364000100714));
#39410=CARTESIAN_POINT('Ctrl Pts',(209.342,4.58486760349077,1.00387449172836));
#39411=CARTESIAN_POINT('Ctrl Pts',(209.342,4.58792727443095,0.984088278604412));
#39412=CARTESIAN_POINT('Ctrl Pts',(209.342,4.60929869169466,0.845884064815334));
#39413=CARTESIAN_POINT('Ctrl Pts',(209.342,4.62447743383398,0.707063308822669));
#39414=CARTESIAN_POINT('Ctrl Pts',(209.342,4.63338222718942,0.568027771136266));
#39415=CARTESIAN_POINT('Ctrl Pts',(209.342,4.6411610596881,0.446572492405312));
#39416=CARTESIAN_POINT('Ctrl Pts',(209.342,4.64415153042464,0.324952785915422));
#39417=CARTESIAN_POINT('Ctrl Pts',(209.342,4.64226694290985,0.203434733211828));
#39418=CARTESIAN_POINT('Ctrl Pts',(209.342,4.64010420278125,0.0639814221460967));
#39419=CARTESIAN_POINT('Ctrl Pts',(209.342,4.63152199228626,-0.075338827690575));
#39420=CARTESIAN_POINT('Ctrl Pts',(209.342,4.61662060143202,-0.214101806503654));
#39421=CARTESIAN_POINT('Ctrl Pts',(209.342,4.60179817353413,-0.352129475764245));
#39422=CARTESIAN_POINT('Ctrl Pts',(209.342,4.58072306891116,-0.489606517490044));
#39423=CARTESIAN_POINT('Ctrl Pts',(209.342,4.55344645744459,-0.626096125820327));
#39424=CARTESIAN_POINT('Ctrl Pts',(209.342,4.5428718464784,-0.679010488397532));
#39425=CARTESIAN_POINT('Ctrl Pts',(209.342,4.53136468778828,-0.731776177221943));
#39426=CARTESIAN_POINT('Ctrl Pts',(209.342,4.51892616592192,-0.784366583247235));
#39427=CARTESIAN_POINT('Ctrl Pts',(209.342,4.51476592663783,-0.801956187177935));
#39428=CARTESIAN_POINT('Ctrl Pts',(209.342,4.51050156997105,-0.81952561642285));
#39429=CARTESIAN_POINT('Ctrl Pts',(209.342,4.50613651936222,-0.83706091614901));
#39430=CARTESIAN_POINT('Ctrl Pts',(209.342,4.47290452011878,-0.970560643747779));
#39431=CARTESIAN_POINT('Ctrl Pts',(209.342,4.43379463524881,-1.10227963075694));
#39432=CARTESIAN_POINT('Ctrl Pts',(209.342,4.38893981285202,-1.23182249216731));
#39433=CARTESIAN_POINT('Ctrl Pts',(209.342,4.34426449583392,-1.3608469335026));
#39434=CARTESIAN_POINT('Ctrl Pts',(209.342,4.29388982367071,-1.48771336542518));
#39435=CARTESIAN_POINT('Ctrl Pts',(209.342,4.2378992370765,-1.61201266075259));
#39436=CARTESIAN_POINT('Ctrl Pts',(209.342,4.18190865048229,-1.73631195607999));
#39437=CARTESIAN_POINT('Ctrl Pts',(209.342,4.12030189324976,-1.85804484824877));
#39438=CARTESIAN_POINT('Ctrl Pts',(209.342,4.05311855743346,-1.97677271072609));
#39439=CARTESIAN_POINT('Ctrl Pts',(209.342,4.00773484962232,-2.05697579314588));
#39440=CARTESIAN_POINT('Ctrl Pts',(209.342,3.95980537285593,-2.13580691803772));
#39441=CARTESIAN_POINT('Ctrl Pts',(209.342,3.90940924621182,-2.21316018241094));
#39442=CARTESIAN_POINT('Ctrl Pts',(209.342,3.88603778600824,-2.24903315242473));
#39443=CARTESIAN_POINT('Ctrl Pts',(209.342,3.86213573272516,-2.2845881630747));
#39444=CARTESIAN_POINT('Ctrl Pts',(209.342,3.83771052726995,-2.31981400625445));
#39445=CARTESIAN_POINT('Ctrl Pts',(209.342,3.82187570579579,-2.34265086382156));
#39446=CARTESIAN_POINT('Ctrl Pts',(209.342,3.80582100272928,-2.3653493667811));
#39447=CARTESIAN_POINT('Ctrl Pts',(209.342,3.78954838876465,-2.38790636224504));
#39448=CARTESIAN_POINT('Ctrl Pts',(209.342,3.77829714314839,-2.40350276838367));
#39449=CARTESIAN_POINT('Ctrl Pts',(209.342,3.76694647710257,-2.419024887875));
#39450=CARTESIAN_POINT('Ctrl Pts',(209.342,3.75550080658077,-2.4344672172057));
#39451=CARTESIAN_POINT('Ctrl Pts',(209.342,3.67252965594557,-2.54641066609451));
#39452=CARTESIAN_POINT('Ctrl Pts',(209.342,3.58451278293967,-2.65424350219139));
#39453=CARTESIAN_POINT('Ctrl Pts',(209.342,3.49179622102669,-2.75766463405047));
#39454=CARTESIAN_POINT('Ctrl Pts',(209.342,3.40200182763164,-2.85782621907811));
#39455=CARTESIAN_POINT('Ctrl Pts',(209.342,3.30779847052118,-2.95385016824527));
#39456=CARTESIAN_POINT('Ctrl Pts',(209.342,3.20946275289611,-3.04542604497319));
#39457=CARTESIAN_POINT('Ctrl Pts',(209.342,3.11197569393019,-3.1362116019411));
#39458=CARTESIAN_POINT('Ctrl Pts',(209.342,3.01042667809337,-3.22262598770536));
#39459=CARTESIAN_POINT('Ctrl Pts',(209.342,2.90505802513543,-3.30432364681823));
#39460=CARTESIAN_POINT('Ctrl Pts',(209.342,2.80190849661856,-3.38430070623636));
#39461=CARTESIAN_POINT('Ctrl Pts',(209.342,2.69509794498561,-3.45975793435593));
#39462=CARTESIAN_POINT('Ctrl Pts',(209.342,2.58483637303122,-3.53032417801676));
#39463=CARTESIAN_POINT('Ctrl Pts',(209.342,2.56941120866939,-3.5401961205945));
#39464=CARTESIAN_POINT('Ctrl Pts',(209.342,2.55391848441358,-3.54997226108128));
#39465=CARTESIAN_POINT('Ctrl Pts',(209.342,2.53835875722666,-3.5596515025506));
#39466=CARTESIAN_POINT('Origin',(209.342,0.,0.));
#39467=CARTESIAN_POINT('Origin',(207.493410108095,0.,0.));
#39468=CARTESIAN_POINT('Ctrl Pts',(209.342,2.5383587572263,-3.55965150255085));
#39469=CARTESIAN_POINT('Ctrl Pts',(209.368396523686,3.12874208667276,-3.13865391518958));
#39470=CARTESIAN_POINT('Ctrl Pts',(209.421189571058,4.09533550545485,-1.99754846162188));
#39471=CARTESIAN_POINT('Ctrl Pts',(209.500379142115,4.55219349719505,0.199542953564506));
#39472=CARTESIAN_POINT('Ctrl Pts',(209.579568713173,3.90500385774559,2.34791981561545));
#39473=CARTESIAN_POINT('Ctrl Pts',(209.65875828423,2.31088729255791,3.92708782806959));
#39474=CARTESIAN_POINT('Ctrl Pts',(209.737947855288,0.156348682839113,4.55384789993644));
#39475=CARTESIAN_POINT('Ctrl Pts',(209.817137426345,-2.03609361756371,4.07632219349179));
#39476=CARTESIAN_POINT('Ctrl Pts',(209.896326997403,-3.73478222633324,2.61025841618883));
#39477=CARTESIAN_POINT('Ctrl Pts',(209.955084557986,-4.32316955247597,1.05279137782476));
#39478=CARTESIAN_POINT('Ctrl Pts',(209.987445594884,-4.37218337323086,0.16395346347465));
#39479=CARTESIAN_POINT('Ctrl Pts',(209.993410108095,-4.37201596611874,0.000111980929712943));
#39480=CARTESIAN_POINT('Ctrl Pts',(209.012910346562,2.86929757049685,-4.02374147429241));
#39481=CARTESIAN_POINT('Ctrl Pts',(209.039306870248,3.53665219403857,-3.5478562783319));
#39482=CARTESIAN_POINT('Ctrl Pts',(209.09209991762,4.62926534033801,-2.25797907075377));
#39483=CARTESIAN_POINT('Ctrl Pts',(209.171289488677,5.14568624499954,0.225558388955994));
#39484=CARTESIAN_POINT('Ctrl Pts',(209.250479059734,4.41411918229158,2.6540301300941));
#39485=CARTESIAN_POINT('Ctrl Pts',(209.329668630792,2.61216948760781,4.43908235277214));
#39486=CARTESIAN_POINT('Ctrl Pts',(209.40885820185,0.176732660244985,5.14755634068753));
#39487=CARTESIAN_POINT('Ctrl Pts',(209.488047772907,-2.30154955580963,4.60777316565336));
#39488=CARTESIAN_POINT('Ctrl Pts',(209.567237343965,-4.22170488621655,2.95057115571943));
#39489=CARTESIAN_POINT('Ctrl Pts',(209.646426915022,-5.11808070198921,0.577855556617751));
#39490=CARTESIAN_POINT('Ctrl Pts',(209.72561648608,-4.77330727068225,-1.93499613460064));
#39491=CARTESIAN_POINT('Ctrl Pts',(209.804806057137,-3.27099124539652,-3.97860317407427));
#39492=CARTESIAN_POINT('Ctrl Pts',(209.883995628195,-0.975449900320081,
-5.0573874425955));
#39493=CARTESIAN_POINT('Ctrl Pts',(209.963185199253,1.55664124071889,-4.90973897055166));
#39494=CARTESIAN_POINT('Ctrl Pts',(210.04237477031,3.71124194048778,-3.57146363727227));
#39495=CARTESIAN_POINT('Ctrl Pts',(210.121564341368,4.96585488056877,-1.367097089327));
#39496=CARTESIAN_POINT('Ctrl Pts',(210.200753912425,5.01623244866681,1.16879473627364));
#39497=CARTESIAN_POINT('Ctrl Pts',(210.279943483483,3.85015794843245,3.42125020084859));
#39498=CARTESIAN_POINT('Ctrl Pts',(210.35913305454,1.75040808710203,4.84404176890668));
#39499=CARTESIAN_POINT('Ctrl Pts',(210.438322625598,-0.773821214563635,
5.09213804560949));
#39500=CARTESIAN_POINT('Ctrl Pts',(210.517512196655,-3.11039644948909,4.10537489980206));
#39501=CARTESIAN_POINT('Ctrl Pts',(210.596701767713,-4.69269080602413,2.12304548743095));
#39502=CARTESIAN_POINT('Ctrl Pts',(210.67589133877,-5.13699294884545,-0.374129103682252));
#39503=CARTESIAN_POINT('Ctrl Pts',(210.755080909828,-4.33555821691576,-2.78057621546455));
#39504=CARTESIAN_POINT('Ctrl Pts',(210.834270480886,-2.48273704223376,-4.51272488877181));
#39505=CARTESIAN_POINT('Ctrl Pts',(210.913460051943,-0.0278443610268617,
-5.15052364658087));
#39506=CARTESIAN_POINT('Ctrl Pts',(210.992649623001,2.43380066490539,-4.53930429317273));
#39507=CARTESIAN_POINT('Ctrl Pts',(211.071839194058,4.30524140906143,-2.82728943551745));
#39508=CARTESIAN_POINT('Ctrl Pts',(211.151028765116,5.13264763125822,-0.429648037150878));
#39509=CARTESIAN_POINT('Ctrl Pts',(211.230218336173,4.71537073190118,2.07218435551025));
#39510=CARTESIAN_POINT('Ctrl Pts',(211.309407907231,3.15460166563038,4.0715055536853));
#39511=CARTESIAN_POINT('Ctrl Pts',(211.388597478288,0.828831817984134,5.08347390668895));
#39512=CARTESIAN_POINT('Ctrl Pts',(211.467787049346,-1.69793234070152,4.86268392031491));
#39513=CARTESIAN_POINT('Ctrl Pts',(211.546976620404,-3.81294259032423,3.46267785758093));
#39514=CARTESIAN_POINT('Ctrl Pts',(211.626166191461,-5.00330232298365,1.22296157229737));
#39515=CARTESIAN_POINT('Ctrl Pts',(211.705355762519,-4.98034557634164,-1.31332672351697));
#39516=CARTESIAN_POINT('Ctrl Pts',(211.784545333576,-3.74963943333942,-3.53112917668494));
#39517=CARTESIAN_POINT('Ctrl Pts',(211.863734904634,-1.60963398715295,-4.89262174809087));
#39518=CARTESIAN_POINT('Ctrl Pts',(211.942924475691,0.92071274088747,-5.06763822616188));
#39519=CARTESIAN_POINT('Ctrl Pts',(212.022114046749,3.22778374639364,-4.01373656696683));
#39520=CARTESIAN_POINT('Ctrl Pts',(212.101303617806,4.75210708679663,-1.98649122276108));
#39521=CARTESIAN_POINT('Ctrl Pts',(212.180493188864,5.1240295791979,0.522484462921665));
#39522=CARTESIAN_POINT('Ctrl Pts',(212.259682759921,4.25335885465338,2.9047560303804));
#39523=CARTESIAN_POINT('Ctrl Pts',(212.338872330979,2.3512352900462,4.5826151653102));
#39524=CARTESIAN_POINT('Ctrl Pts',(212.418061902037,-0.121070194414848,
5.14917577389955));
#39525=CARTESIAN_POINT('Ctrl Pts',(212.497251473094,-2.56401577764407,4.46704513459198));
#39526=CARTESIAN_POINT('Ctrl Pts',(212.576441044152,-4.38517950653409,2.70164206325766));
#39527=CARTESIAN_POINT('Ctrl Pts',(212.655630615209,-5.1429234745331,0.281082332397397));
#39528=CARTESIAN_POINT('Ctrl Pts',(212.734820186267,-4.65349239680834,-2.20764074417387));
#39529=CARTESIAN_POINT('Ctrl Pts',(212.814009757324,-3.03557484217919,-4.16100402787818));
#39530=CARTESIAN_POINT('Ctrl Pts',(212.893199328382,-0.68152088354947,-5.10531080618757));
#39531=CARTESIAN_POINT('Ctrl Pts',(212.972388899439,1.83780402326983,-4.81156372861701));
#39532=CARTESIAN_POINT('Ctrl Pts',(213.051578470497,3.91145570004733,-3.35099738123695));
#39533=CARTESIAN_POINT('Ctrl Pts',(213.130768041555,5.03656712229653,-1.07780367650663));
#39534=CARTESIAN_POINT('Ctrl Pts',(213.209957612612,4.94029524725464,1.45676079451735));
#39535=CARTESIAN_POINT('Ctrl Pts',(213.28914718367,3.64598630605882,3.638056211567));
#39536=CARTESIAN_POINT('Ctrl Pts',(213.368336754727,1.46751426959545,4.93711160609353));
#39537=CARTESIAN_POINT('Ctrl Pts',(213.447526325785,-1.06683457221922,5.03890197741606));
#39538=CARTESIAN_POINT('Ctrl Pts',(213.526715896842,-3.34247268987556,3.91874284177026));
#39539=CARTESIAN_POINT('Ctrl Pts',(213.6059054679,-4.80755071452867,1.84827629691139));
#39540=CARTESIAN_POINT('Ctrl Pts',(213.685095038957,-5.10678263785396,-0.670403037137365));
#39541=CARTESIAN_POINT('Ctrl Pts',(213.764284610015,-4.16760378151171,-3.02650753556288));
#39542=CARTESIAN_POINT('Ctrl Pts',(213.843474181072,-2.21776795885376,-4.64867448023318));
#39543=CARTESIAN_POINT('Ctrl Pts',(213.92266375213,0.269883537940656,-5.14352330785409));
#39544=CARTESIAN_POINT('Ctrl Pts',(214.001853323188,2.69208743174467,-4.39105162829271));
#39545=CARTESIAN_POINT('Ctrl Pts',(214.081042894245,4.46145169408141,-2.5737361799275));
#39546=CARTESIAN_POINT('Ctrl Pts',(214.160232465303,5.14889995122897,-0.132281649233546));
#39547=CARTESIAN_POINT('Ctrl Pts',(214.23942203636,4.58772384834088,2.34125159559026));
#39548=CARTESIAN_POINT('Ctrl Pts',(214.318611607418,2.91401034748148,4.24702399772599));
#39549=CARTESIAN_POINT('Ctrl Pts',(214.397801178475,0.533640213219658,5.12287978243923));
#39550=CARTESIAN_POINT('Ctrl Pts',(214.476990749533,-1.97613934364353,4.75642117952077));
#39551=CARTESIAN_POINT('Ctrl Pts',(214.55618032059,-4.00669892212876,3.236515547607));
#39552=CARTESIAN_POINT('Ctrl Pts',(214.635369891648,-5.06562146651227,0.931744761455457));
#39553=CARTESIAN_POINT('Ctrl Pts',(214.714559462705,-4.89611494415949,-1.59897704676074));
#39554=CARTESIAN_POINT('Ctrl Pts',(214.793749033763,-3.53928521748753,-3.74194191453633));
#39555=CARTESIAN_POINT('Ctrl Pts',(214.87293860482,-1.3241677436213,-4.97747415153937));
#39556=CARTESIAN_POINT('Ctrl Pts',(214.952128175878,1.21206455421126,-5.00595332168752));
#39557=CARTESIAN_POINT('Ctrl Pts',(215.031317746935,3.45436740251883,-3.82047313704794));
#39558=CARTESIAN_POINT('Ctrl Pts',(215.110507317993,4.85897533965053,-1.70851625428545));
#39559=CARTESIAN_POINT('Ctrl Pts',(215.189696889051,5.08526654284531,0.817761169723606));
#39560=CARTESIAN_POINT('Ctrl Pts',(215.268886460108,4.07836468678181,3.14572894956014));
#39561=CARTESIAN_POINT('Ctrl Pts',(215.348076031166,2.08244662429357,4.7108476094497));
#39562=CARTESIAN_POINT('Ctrl Pts',(215.427265602223,-0.418471264991916,
5.13357097378284));
#39563=CARTESIAN_POINT('Ctrl Pts',(215.506455173281,-2.81790856222995,4.31138730310799));
#39564=CARTESIAN_POINT('Ctrl Pts',(215.585644744339,-4.53399420989599,2.44367871192578));
#39565=CARTESIAN_POINT('Ctrl Pts',(215.664834315396,-5.15057206514796,-0.0166296183682295));
#39566=CARTESIAN_POINT('Ctrl Pts',(215.744023886454,-4.51812006750333,-2.47290521413848));
#39567=CARTESIAN_POINT('Ctrl Pts',(215.823213457511,-2.79000980667881,-4.32949355249846));
#39568=CARTESIAN_POINT('Ctrl Pts',(215.902403028569,-0.385313431858017,
-5.1361661481809));
#39569=CARTESIAN_POINT('Ctrl Pts',(215.981592599626,2.11282265665386,-4.697302370938));
#39570=CARTESIAN_POINT('Ctrl Pts',(216.060782170684,4.09859263540988,-3.11932806088965));
#39571=CARTESIAN_POINT('Ctrl Pts',(216.139971741741,5.09044106686257,-0.784906929061443));
#39572=CARTESIAN_POINT('Ctrl Pts',(216.219161312799,4.8478416007807,1.73985659070789));
#39573=CARTESIAN_POINT('Ctrl Pts',(216.298350883857,3.42962536729897,3.84269943951761));
#39574=CARTESIAN_POINT('Ctrl Pts',(216.377540454914,1.1797142436527,5.01367564226213));
#39575=CARTESIAN_POINT('Ctrl Pts',(216.456730025972,-1.35628127791517,4.96881980330002));
#39576=CARTESIAN_POINT('Ctrl Pts',(216.535919597029,-3.56337434289889,3.71900960402894));
#39577=CARTESIAN_POINT('Ctrl Pts',(216.615109168087,-4.90633797234996,1.56732793108732));
#39578=CARTESIAN_POINT('Ctrl Pts',(216.694298739144,-5.05949928113605,-0.964435672646684));
#39579=CARTESIAN_POINT('Ctrl Pts',(216.773488310202,-3.98571617230891,-3.26232060599274));
#39580=CARTESIAN_POINT('Ctrl Pts',(216.852677881259,-1.94538441191105,-4.76908257764353));
#39581=CARTESIAN_POINT('Ctrl Pts',(216.931867452317,0.566709159622022,-5.11932709160981));
#39582=CARTESIAN_POINT('Ctrl Pts',(217.011057023375,2.94137398550808,-4.22811875659447));
#39583=CARTESIAN_POINT('Ctrl Pts',(217.090246594432,4.60274641009122,-2.31157838432574));
#39584=CARTESIAN_POINT('Ctrl Pts',(217.169436165489,5.14793841844104,0.165526983988809));
#39585=CARTESIAN_POINT('Ctrl Pts',(217.248625736547,4.44473924146695,2.60249154039997));
#39586=CARTESIAN_POINT('Ctrl Pts',(217.327815307605,2.66367688139153,4.4083437495311));
#39587=CARTESIAN_POINT('Ctrl Pts',(217.407004878662,0.236664537266517,5.14515879631426));
#39588=CARTESIAN_POINT('Ctrl Pts',(217.48619444972,-2.24773969817247,4.63425672484263));
#39589=CARTESIAN_POINT('Ctrl Pts',(217.565384020777,-4.18706001884488,2.99953288714764));
#39590=CARTESIAN_POINT('Ctrl Pts',(217.644573591835,-5.11100517472834,0.637412932399219));
#39591=CARTESIAN_POINT('Ctrl Pts',(217.723763162892,-4.79551557253093,-1.87928165427725));
#39592=CARTESIAN_POINT('Ctrl Pts',(217.80295273395,-3.3170984286237,-3.94024455552087));
#39593=CARTESIAN_POINT('Ctrl Pts',(217.882142305007,-1.03427452951688,-5.04568581464227));
#39594=CARTESIAN_POINT('Ctrl Pts',(217.961331876065,1.49936418144328,-4.92753246502694));
#39595=CARTESIAN_POINT('Ctrl Pts',(218.040521447122,3.66940238370292,-3.61443706390981));
#39596=CARTESIAN_POINT('Ctrl Pts',(218.11971101818,4.94959901854762,-1.42482935753097));
#39597=CARTESIAN_POINT('Ctrl Pts',(218.198900589237,5.02950239356853,1.11030392937163));
#39598=CARTESIAN_POINT('Ctrl Pts',(218.278090160295,3.88973569013542,3.37618503689836));
#39599=CARTESIAN_POINT('Ctrl Pts',(218.357279731353,1.80669590258578,4.82333070171115));
#39600=CARTESIAN_POINT('Ctrl Pts',(218.436469302411,-0.714473298336281,
5.10080356889521));
#39601=CARTESIAN_POINT('Ctrl Pts',(218.515658873468,-3.06238048730475,4.14131559935545));
#39602=CARTESIAN_POINT('Ctrl Pts',(218.594848444525,-4.66765081939779,2.17754562998453));
#39603=CARTESIAN_POINT('Ctrl Pts',(218.674038015583,-5.14100121277669,-0.3142859728308));
#39604=CARTESIAN_POINT('Ctrl Pts',(218.753227586641,-4.36764271492659,-2.72990224316519));
#39605=CARTESIAN_POINT('Ctrl Pts',(218.832417157698,-2.53511718306022,-4.48350867185984));
#39606=CARTESIAN_POINT('Ctrl Pts',(218.911606728756,-0.0878177965264293,
-5.14985020919084));
#39607=CARTESIAN_POINT('Ctrl Pts',(218.990796299813,2.38077768063373,-4.56733694595503));
#39608=CARTESIAN_POINT('Ctrl Pts',(219.069985870871,4.27202711572156,-2.8772301724105));
#39609=CARTESIAN_POINT('Ctrl Pts',(219.149175441928,5.12729659898502,-0.48938607308168));
#39610=CARTESIAN_POINT('Ctrl Pts',(219.228365012986,4.73918060277484,2.0171356812997));
#39611=CARTESIAN_POINT('Ctrl Pts',(219.307554584043,3.20179847141267,4.03449571705674));
#39612=CARTESIAN_POINT('Ctrl Pts',(219.386744155101,0.887970185493443,5.07347790890671));
#39613=CARTESIAN_POINT('Ctrl Pts',(219.465933726158,-1.64119365075591,4.88212582214021));
#39614=CARTESIAN_POINT('Ctrl Pts',(219.545123297216,-3.77236288791018,3.5068429369459));
#39615=CARTESIAN_POINT('Ctrl Pts',(219.624312868273,-4.9887223129969,1.28113965916958));
#39616=CARTESIAN_POINT('Ctrl Pts',(219.703502439331,-4.99530095685557,-1.25524399736708));
#39617=CARTESIAN_POINT('Ctrl Pts',(219.782692010389,-3.79050347775281,-3.48722705421306));
#39618=CARTESIAN_POINT('Ctrl Pts',(219.861881581446,-1.66649703674374,-4.87354663145974));
#39619=CARTESIAN_POINT('Ctrl Pts',(219.941071152504,0.861640153687791,-5.07801589088088));
#39620=CARTESIAN_POINT('Ctrl Pts',(220.020260723561,3.18082690895062,-4.05105039684845));
#39621=CARTESIAN_POINT('Ctrl Pts',(220.099450294619,4.72865317920565,-2.0416924972233));
#39622=CARTESIAN_POINT('Ctrl Pts',(220.178639865676,5.12976624751329,0.462782225775264));
#39623=CARTESIAN_POINT('Ctrl Pts',(220.257829436734,4.2868949387905,2.85503080999931));
#39624=CARTESIAN_POINT('Ctrl Pts',(220.337019007791,2.40443818471475,4.55492548331974));
#39625=CARTESIAN_POINT('Ctrl Pts',(220.416208578849,-0.0611023580090773,
5.15023646491014));
#39626=CARTESIAN_POINT('Ctrl Pts',(220.495398149907,-2.51182538706132,4.49659897765337));
#39627=CARTESIAN_POINT('Ctrl Pts',(220.574587720964,-4.35342289604155,2.75252215901591));
#39628=CARTESIAN_POINT('Ctrl Pts',(220.653777292022,-5.13930171919711,0.340950098053002));
#39629=CARTESIAN_POINT('Ctrl Pts',(220.732966863079,-4.67888378875926,-2.15330342868111));
#39630=CARTESIAN_POINT('Ctrl Pts',(220.812156434137,-3.08382187849219,-4.12537413289167));
#39631=CARTESIAN_POINT('Ctrl Pts',(220.891346005194,-0.740923529936072,
-5.09702869025692));
#39632=CARTESIAN_POINT('Ctrl Pts',(220.970535576252,1.78165114356852,-4.83263783619408));
#39633=CARTESIAN_POINT('Ctrl Pts',(221.049725147309,3.87216973211928,-3.39631716377015));
#39634=CARTESIAN_POINT('Ctrl Pts',(221.128914718367,5.02367525731088,-1.13637896919977));
#39635=CARTESIAN_POINT('Ctrl Pts',(221.208104289424,4.9569233337539,1.39913473529202));
#39636=CARTESIAN_POINT('Ctrl Pts',(221.287293860482,3.6881029769245,3.59535377575949));
#39637=CARTESIAN_POINT('Ctrl Pts',(221.36648343154,1.52490398573333,4.91968850138736));
#39638=CARTESIAN_POINT('Ctrl Pts',(221.445673002597,-1.00808450753534,5.05098286642663));
#39639=CARTESIAN_POINT('Ctrl Pts',(221.524862573655,-3.2966188845772,3.95739912490663));
#39640=CARTESIAN_POINT('Ctrl Pts',(221.604052144712,-4.78569263413133,1.90413148846678));
#39641=CARTESIAN_POINT('Ctrl Pts',(221.68324171577,-5.11426397585892,-0.610889148630078));
#39642=CARTESIAN_POINT('Ctrl Pts',(221.762431286827,-4.20251954963569,-2.97777660711001));
#39643=CARTESIAN_POINT('Ctrl Pts',(221.841620857885,-2.27184811611898,-4.62251767504382));
#39644=CARTESIAN_POINT('Ctrl Pts',(221.920810428943,0.210147207048501,-5.14630014929042));
#39645=CARTESIAN_POINT('Ctrl Pts',(221.973603476314,1.83010136182592,-4.66325228984448));
#39646=CARTESIAN_POINT('Ctrl Pts',(222.,2.53382212491006,-4.24300712223256));
#39647=CARTESIAN_POINT('Ctrl Pts',(209.122606897708,2.75898463274,-3.86904481704522));
#39648=CARTESIAN_POINT('Ctrl Pts',(209.149003421394,3.40068215824997,-3.41145549061779));
#39649=CARTESIAN_POINT('Ctrl Pts',(209.201796468766,4.45128872871029,-2.17116886770981));
#39650=CARTESIAN_POINT('Ctrl Pts',(209.280986039823,4.94785532906471,0.216886577158832));
#39651=CARTESIAN_POINT('Ctrl Pts',(209.360175610881,4.24441407410958,2.55199335860121));
#39652=CARTESIAN_POINT('Ctrl Pts',(209.439365181938,2.51174208925784,4.26841751120462));
#39653=CARTESIAN_POINT('Ctrl Pts',(209.518554752996,0.169938001109696,4.94965352710383));
#39654=CARTESIAN_POINT('Ctrl Pts',(209.597744324053,-2.21306424306099,4.43062284159951));
#39655=CARTESIAN_POINT('Ctrl Pts',(209.676933895111,-4.05939733292211,2.83713357587589));
#39656=CARTESIAN_POINT('Ctrl Pts',(209.756123466168,-4.92131110802362,0.555639337322439));
#39657=CARTESIAN_POINT('Ctrl Pts',(209.835313037226,-4.58979282684784,-1.86060332489322));
#39658=CARTESIAN_POINT('Ctrl Pts',(209.914502608283,-3.14523480334363,-3.82564190271164));
#39659=CARTESIAN_POINT('Ctrl Pts',(209.993692179341,-0.937947779506468,
-4.86295126005946));
#39660=CARTESIAN_POINT('Ctrl Pts',(210.072881750399,1.49679465315585,-4.72097927722814));
#39661=CARTESIAN_POINT('Ctrl Pts',(210.152071321456,3.56855963197046,-3.43415524166689));
#39662=CARTESIAN_POINT('Ctrl Pts',(210.231260892514,4.77493775646759,-1.31453771114566));
#39663=CARTESIAN_POINT('Ctrl Pts',(210.310450463571,4.8233785099281,1.12385928506119));
#39664=CARTESIAN_POINT('Ctrl Pts',(210.389640034629,3.70213487878409,3.2897169070078));
#39665=CARTESIAN_POINT('Ctrl Pts',(210.468829605686,1.6831119445384,4.65780786844285));
#39666=CARTESIAN_POINT('Ctrl Pts',(210.548019176744,-0.744070904817171,
4.89636584231815));
#39667=CARTESIAN_POINT('Ctrl Pts',(210.627208747802,-2.99081423067021,3.94753976605815));
#39668=CARTESIAN_POINT('Ctrl Pts',(210.706398318859,-4.51227574063673,2.04142293732736));
#39669=CARTESIAN_POINT('Ctrl Pts',(210.785587889917,-4.93949625514236,-0.359745346155024));
#39670=CARTESIAN_POINT('Ctrl Pts',(210.864777460974,-4.16887346151025,-2.67367425655354));
#39671=CARTESIAN_POINT('Ctrl Pts',(210.943967032032,-2.38728580022152,-4.33922878823222));
#39672=CARTESIAN_POINT('Ctrl Pts',(211.023156603089,-0.0267738574665273,
-4.95250675203405));
#39673=CARTESIAN_POINT('Ctrl Pts',(211.102346174147,2.34023082954886,-4.36478632156147));
#39674=CARTESIAN_POINT('Ctrl Pts',(211.181535745204,4.13972221284094,-2.71859154139596));
#39675=CARTESIAN_POINT('Ctrl Pts',(211.260725316262,4.93531799751903,-0.41312980019039));
#39676=CARTESIAN_POINT('Ctrl Pts',(211.339914887319,4.53408371468927,1.99251721112601));
#39677=CARTESIAN_POINT('Ctrl Pts',(211.419104458377,3.03331993425243,3.91497255991756));
#39678=CARTESIAN_POINT('Ctrl Pts',(211.498294029434,0.796966572047865,4.88803480465114));
#39679=CARTESIAN_POINT('Ctrl Pts',(211.577483600492,-1.63265367928241,4.67573330419596));
#39680=CARTESIAN_POINT('Ctrl Pts',(211.656673171549,-3.6663503013397,3.32955183715591));
#39681=CARTESIAN_POINT('Ctrl Pts',(211.735862742607,-4.8109454955116,1.17594362435392));
#39682=CARTESIAN_POINT('Ctrl Pts',(211.815052313665,-4.78887134333782,-1.26283459938339));
#39683=CARTESIAN_POINT('Ctrl Pts',(211.894241884722,-3.60548089583749,-3.39537147867399));
#39684=CARTESIAN_POINT('Ctrl Pts',(211.97343145578,-1.54775004187592,-4.70452014304488));
#39685=CARTESIAN_POINT('Ctrl Pts',(212.052621026837,0.885315043443409,-4.87280794227463));
#39686=CARTESIAN_POINT('Ctrl Pts',(212.131810597895,3.10368845869336,-3.85942455811946));
#39687=CARTESIAN_POINT('Ctrl Pts',(212.211000168952,4.56940770466565,-1.91011863426965));
#39688=CARTESIAN_POINT('Ctrl Pts',(212.29018974001,4.92703127485804,0.502397039215665));
#39689=CARTESIAN_POINT('Ctrl Pts',(212.369379311067,4.08983433373387,2.79307985762196));
#39690=CARTESIAN_POINT('Ctrl Pts',(212.448568882125,2.26083976088618,4.40643206506557));
#39691=CARTESIAN_POINT('Ctrl Pts',(212.527758453183,-0.116415532954153,
4.95121069962984));
#39692=CARTESIAN_POINT('Ctrl Pts',(212.60694802424,-2.46543969554121,4.29530523666149));
#39693=CARTESIAN_POINT('Ctrl Pts',(212.686137595298,-4.2165870123533,2.59777480465405));
#39694=CARTESIAN_POINT('Ctrl Pts',(212.765327166355,-4.94519877599783,0.270275848553698));
#39695=CARTESIAN_POINT('Ctrl Pts',(212.844516737413,-4.47458435241465,-2.12276584708909));
#39696=CARTESIAN_POINT('Ctrl Pts',(212.92370630847,-2.91886921287646,-4.00103017816211));
#39697=CARTESIAN_POINT('Ctrl Pts',(213.002895879528,-0.655319149863825,
-4.90903216329489));
#39698=CARTESIAN_POINT('Ctrl Pts',(213.082085450585,1.76714785887865,-4.62657847802267));
#39699=CARTESIAN_POINT('Ctrl Pts',(213.161275021643,3.76107597867765,-3.22216502542249));
#39700=CARTESIAN_POINT('Ctrl Pts',(213.240464592701,4.84293139723859,-1.0363664651476));
#39701=CARTESIAN_POINT('Ctrl Pts',(213.319654163758,4.75036078813315,1.40075420792119));
#39702=CARTESIAN_POINT('Ctrl Pts',(213.398843734816,3.50581281391976,3.49818759962898));
#39703=CARTESIAN_POINT('Ctrl Pts',(213.478033305873,1.41109425518363,4.74729954515509));
#39704=CARTESIAN_POINT('Ctrl Pts',(213.557222876931,-1.02581907875067,4.84517648658055));
#39705=CARTESIAN_POINT('Ctrl Pts',(213.636412447988,-3.21396807411751,3.76808295914452));
#39706=CARTESIAN_POINT('Ctrl Pts',(213.715602019046,-4.62271974816679,1.77721751576748));
#39707=CARTESIAN_POINT('Ctrl Pts',(213.794791590103,-4.91044740896034,-0.644628739877947));
#39708=CARTESIAN_POINT('Ctrl Pts',(213.873981161161,-4.00737619784371,-2.91015050768815));
#39709=CARTESIAN_POINT('Ctrl Pts',(213.953170732218,-2.13250371114387,-4.46995166533147));
#39710=CARTESIAN_POINT('Ctrl Pts',(214.032360303276,0.259507602649545,-4.94577554814299));
#39711=CARTESIAN_POINT('Ctrl Pts',(214.111549874334,2.58858751024904,-4.22223337467562));
#39712=CARTESIAN_POINT('Ctrl Pts',(214.190739445391,4.28992684141539,-2.47478638749806));
#39713=CARTESIAN_POINT('Ctrl Pts',(214.269929016449,4.95094548123029,-0.127195952480322));
#39714=CARTESIAN_POINT('Ctrl Pts',(214.349118587506,4.4113443398049,2.25123989928065));
#39715=CARTESIAN_POINT('Ctrl Pts',(214.428308158564,2.80197838349493,4.08374302654674));
#39716=CARTESIAN_POINT('Ctrl Pts',(214.507497729621,0.513123895835644,4.92592568315483));
#39717=CARTESIAN_POINT('Ctrl Pts',(214.586687300679,-1.90016474322018,4.57355593789613));
#39718=CARTESIAN_POINT('Ctrl Pts',(214.665876871736,-3.85265748238687,3.11208455731049));
#39719=CARTESIAN_POINT('Ctrl Pts',(214.745066442794,-4.87086871891265,0.895922927243278));
#39720=CARTESIAN_POINT('Ctrl Pts',(214.824256013852,-4.70787903979075,-1.5375028179294));
#39721=CARTESIAN_POINT('Ctrl Pts',(214.903445584909,-3.40321395254972,-3.59807931563672));
#39722=CARTESIAN_POINT('Ctrl Pts',(214.982635155967,-1.27325882591832,-4.7861103132568));
#39723=CARTESIAN_POINT('Ctrl Pts',(215.061824727024,1.16546555273411,-4.8134945739901));
#39724=CARTESIAN_POINT('Ctrl Pts',(215.141014298082,3.32156088562718,-3.6735913288652));
#39725=CARTESIAN_POINT('Ctrl Pts',(215.220203869139,4.67216730352476,-1.64283068400737));
#39726=CARTESIAN_POINT('Ctrl Pts',(215.299393440197,4.8897585211657,0.78632154563469));
#39727=CARTESIAN_POINT('Ctrl Pts',(215.378583011254,3.92156798696623,3.02478833838726));
#39728=CARTESIAN_POINT('Ctrl Pts',(215.457772582312,2.00238493699778,4.52973448808276));
#39729=CARTESIAN_POINT('Ctrl Pts',(215.53696215337,-0.402382729915348,4.93620584124162));
#39730=CARTESIAN_POINT('Ctrl Pts',(215.616151724427,-2.70957132491234,4.14563182200913));
#39731=CARTESIAN_POINT('Ctrl Pts',(215.695341295485,-4.35968038960457,2.34972910543732));
#39732=CARTESIAN_POINT('Ctrl Pts',(215.774530866542,-4.95255330910221,-0.0159902765046303));
#39733=CARTESIAN_POINT('Ctrl Pts',(215.8537204376,-4.34441654406633,-2.37783196632661));
#39734=CARTESIAN_POINT('Ctrl Pts',(215.932910008657,-2.68274516417193,-4.16304195901916));
#39735=CARTESIAN_POINT('Ctrl Pts',(216.012099579715,-0.370499681948449,
-4.93870124163409));
#39736=CARTESIAN_POINT('Ctrl Pts',(216.091289150772,2.0315931332293,-4.51671000944908));
#39737=CARTESIAN_POINT('Ctrl Pts',(216.17047872183,3.94101825242164,-2.99940245757741));
#39738=CARTESIAN_POINT('Ctrl Pts',(216.249668292887,4.89473410557081,-0.754730418231469));
#39739=CARTESIAN_POINT('Ctrl Pts',(216.328857863945,4.66146161208212,1.67296611069283));
#39740=CARTESIAN_POINT('Ctrl Pts',(216.408047435003,3.29777008203251,3.69496311950379));
#39741=CARTESIAN_POINT('Ctrl Pts',(216.48723700606,1.13435898135118,4.82092000243417));
#39742=CARTESIAN_POINT('Ctrl Pts',(216.566426577118,-1.3041377241305,4.7777886898587));
#39743=CARTESIAN_POINT('Ctrl Pts',(216.645616148175,-3.42637694808895,3.57602866012657));
#39744=CARTESIAN_POINT('Ctrl Pts',(216.724805719233,-4.71770903371247,1.50707048331179));
#39745=CARTESIAN_POINT('Ctrl Pts',(216.80399529029,-4.86498190691188,-0.927357004536036));
#39746=CARTESIAN_POINT('Ctrl Pts',(216.883184861348,-3.83248143480613,-3.13689751511079));
#39747=CARTESIAN_POINT('Ctrl Pts',(216.962374432405,-1.8705922147716,-4.58573055624486));
#39748=CARTESIAN_POINT('Ctrl Pts',(217.041564003463,0.544921474407914,-4.92250957898215));
#39749=CARTESIAN_POINT('Ctrl Pts',(217.120753574521,2.82828999982485,-4.06556461581078));
#39750=CARTESIAN_POINT('Ctrl Pts',(217.199943145578,4.42578934454745,-2.22270750350381));
#39751=CARTESIAN_POINT('Ctrl Pts',(217.279132716636,4.95002091550624,0.159163137983585));
#39752=CARTESIAN_POINT('Ctrl Pts',(217.358322287693,4.27385691530776,2.50243622014988));
#39753=CARTESIAN_POINT('Ctrl Pts',(217.437511858751,2.56126923115591,4.23886068348277));
#39754=CARTESIAN_POINT('Ctrl Pts',(217.516701429808,0.227565738788027,4.9473481586575));
#39755=CARTESIAN_POINT('Ctrl Pts',(217.595891000866,-2.1613231577733,4.45608821457955));
#39756=CARTESIAN_POINT('Ctrl Pts',(217.675080571923,-4.02608442119606,2.88421292588538));
#39757=CARTESIAN_POINT('Ctrl Pts',(217.754270142981,-4.91450760629484,0.61290697182538));
#39758=CARTESIAN_POINT('Ctrl Pts',(217.833459714038,-4.61114730891682,-1.80703084199222));
#39759=CARTESIAN_POINT('Ctrl Pts',(217.912649285096,-3.18956935103597,-3.7887580185826));
#39760=CARTESIAN_POINT('Ctrl Pts',(217.991838856153,-0.99451083858036,-4.85169951258196));
#39761=CARTESIAN_POINT('Ctrl Pts',(218.071028427211,1.4417196661713,-4.73808868349009));
#39762=CARTESIAN_POINT('Ctrl Pts',(218.150217998269,3.52832863766821,-3.47547651309174));
#39763=CARTESIAN_POINT('Ctrl Pts',(218.229407569326,4.75930686688351,-1.37005040610828));
#39764=CARTESIAN_POINT('Ctrl Pts',(218.308597140384,4.83613827888256,1.06761721415906));
#39765=CARTESIAN_POINT('Ctrl Pts',(218.387786711441,3.74019101568666,3.24638431714711));
#39766=CARTESIAN_POINT('Ctrl Pts',(218.466976282499,1.7372357201715,4.63789305838353));
#39767=CARTESIAN_POINT('Ctrl Pts',(218.546165853556,-0.68700467699192,4.90469821112708));
#39768=CARTESIAN_POINT('Ctrl Pts',(218.625355424614,-2.94464428888551,3.98209869043647));
#39769=CARTESIAN_POINT('Ctrl Pts',(218.704544995671,-4.4881984406674,2.09382776885602));
#39770=CARTESIAN_POINT('Ctrl Pts',(218.783734566729,-4.94335041746557,-0.302202942713887));
#39771=CARTESIAN_POINT('Ctrl Pts',(218.862924137787,-4.19972443976753,-2.62494849443971));
#39772=CARTESIAN_POINT('Ctrl Pts',(218.942113708844,-2.43765213555284,-4.3111358172153));
#39773=CARTESIAN_POINT('Ctrl Pts',(219.021303279902,-0.0844415558667597,
-4.95185920559993));
#39774=CARTESIAN_POINT('Ctrl Pts',(219.100492850959,2.28924636551427,-4.39174123172365));
#39775=CARTESIAN_POINT('Ctrl Pts',(219.179682422017,4.10778487533567,-2.76661225805234));
#39776=CARTESIAN_POINT('Ctrl Pts',(219.258871993074,4.93017269088968,-0.470571149187391));
#39777=CARTESIAN_POINT('Ctrl Pts',(219.338061564132,4.55697819190328,1.93958493677382));
#39778=CARTESIAN_POINT('Ctrl Pts',(219.417251135189,3.07870221290023,3.87938560247949));
#39779=CARTESIAN_POINT('Ctrl Pts',(219.496440706247,0.853831307459487,4.87842311273264));
#39780=CARTESIAN_POINT('Ctrl Pts',(219.575630277305,-1.57809636349497,4.69442774318297));
#39781=CARTESIAN_POINT('Ctrl Pts',(219.654819848362,-3.62733072508078,3.37201894705926));
#39782=CARTESIAN_POINT('Ctrl Pts',(219.73400941942,-4.79692602819937,1.23188499805217));
#39783=CARTESIAN_POINT('Ctrl Pts',(219.813198990477,-4.80325174969195,-1.20698492017167));
#39784=CARTESIAN_POINT('Ctrl Pts',(219.892388561535,-3.64477388229083,-3.35315721603005));
#39785=CARTESIAN_POINT('Ctrl Pts',(219.971578132592,-1.60242693618093,-4.68617838783826));
#39786=CARTESIAN_POINT('Ctrl Pts',(220.05076770365,0.828513559353387,-4.88278662757303));
#39787=CARTESIAN_POINT('Ctrl Pts',(220.129957274707,3.05853692256848,-3.89530382149409));
#39788=CARTESIAN_POINT('Ctrl Pts',(220.209146845765,4.54685550537946,-1.96319764200831));
#39789=CARTESIAN_POINT('Ctrl Pts',(220.288336416822,4.9325473913766,0.444990112683956));
#39790=CARTESIAN_POINT('Ctrl Pts',(220.36752598788,4.12208109047601,2.74526637173549));
#39791=CARTESIAN_POINT('Ctrl Pts',(220.446715558938,2.31199721848734,4.37980693984934));
#39792=CARTESIAN_POINT('Ctrl Pts',(220.525905129995,-0.0587532183851061,
4.95223061134216));
#39793=CARTESIAN_POINT('Ctrl Pts',(220.605094701053,-2.41525581532081,4.32372285346192));
#39794=CARTESIAN_POINT('Ctrl Pts',(220.68428427211,-4.18605131565955,2.64669876560978));
#39795=CARTESIAN_POINT('Ctrl Pts',(220.763473843168,-4.94171626257075,0.327841939689966));
#39796=CARTESIAN_POINT('Ctrl Pts',(220.842663414225,-4.49899954758883,-2.07051758257643));
#39797=CARTESIAN_POINT('Ctrl Pts',(220.921852985283,-2.96526134492004,-3.96677010916658));
#39798=CARTESIAN_POINT('Ctrl Pts',(221.00104255634,-0.712438003694083,-4.90106846137209));
#39799=CARTESIAN_POINT('Ctrl Pts',(221.080232127398,1.7131538312905,-4.64684237102271));
#39800=CARTESIAN_POINT('Ctrl Pts',(221.159421698455,3.72330039802324,-3.2657424448069));
#39801=CARTESIAN_POINT('Ctrl Pts',(221.238611269513,4.83053517254985,-1.09268977370239));
#39802=CARTESIAN_POINT('Ctrl Pts',(221.317800840571,4.76634959166299,1.34534363862965));
#39803=CARTESIAN_POINT('Ctrl Pts',(221.396990411628,3.54631026838228,3.45712690052796));
#39804=CARTESIAN_POINT('Ctrl Pts',(221.476179982686,1.46627756782774,4.73054628866709));
#39805=CARTESIAN_POINT('Ctrl Pts',(221.555369553743,-0.969327717484422,
4.8567929140549));
#39806=CARTESIAN_POINT('Ctrl Pts',(221.634559124801,-3.1698771629929,3.80525306385193));
#39807=CARTESIAN_POINT('Ctrl Pts',(221.713748695858,-4.60170202294458,1.83092530012021));
#39808=CARTESIAN_POINT('Ctrl Pts',(221.792938266916,-4.91764111964419,-0.587402920738604));
#39809=CARTESIAN_POINT('Ctrl Pts',(221.872127837973,-4.04094959527899,-2.86329308720899));
#39810=CARTESIAN_POINT('Ctrl Pts',(221.951317409031,-2.18450470412734,-4.44480048397577));
#39811=CARTESIAN_POINT('Ctrl Pts',(222.030506980089,0.202067893139325,-4.94844563120763));
#39812=CARTESIAN_POINT('Ctrl Pts',(222.08330002746,1.75974133375087,-4.48396901686381));
#39813=CARTESIAN_POINT('Ctrl Pts',(222.109696551146,2.43640686717375,-4.07988058374122));
#39814=CARTESIAN_POINT('Ctrl Pts',(209.232303448854,2.64867169498315,-3.71434815979804));
#39815=CARTESIAN_POINT('Ctrl Pts',(209.25869997254,3.26471212246136,-3.27505470290369));
#39816=CARTESIAN_POINT('Ctrl Pts',(209.311493019912,4.27331211708257,-2.08435866466584));
#39817=CARTESIAN_POINT('Ctrl Pts',(209.390682590969,4.75002441312988,0.208214765361669));
#39818=CARTESIAN_POINT('Ctrl Pts',(209.469872162027,4.07470896592758,2.44995658710833));
#39819=CARTESIAN_POINT('Ctrl Pts',(209.549061733084,2.41131469090788,4.09775266963711));
#39820=CARTESIAN_POINT('Ctrl Pts',(209.628251304142,0.163143341974401,4.75175071352013));
#39821=CARTESIAN_POINT('Ctrl Pts',(209.707440875199,-2.12457893031235,4.25347251754565));
#39822=CARTESIAN_POINT('Ctrl Pts',(209.786630446257,-3.89708977962767,2.72369599603236));
#39823=CARTESIAN_POINT('Ctrl Pts',(209.865820017314,-4.72454151405803,0.533423118027127));
#39824=CARTESIAN_POINT('Ctrl Pts',(209.945009588372,-4.40627838301343,-1.7862105151858));
#39825=CARTESIAN_POINT('Ctrl Pts',(210.02419915943,-3.01947836129074,-3.67268063134902));
#39826=CARTESIAN_POINT('Ctrl Pts',(210.103388730487,-0.900445658692855,
-4.66851507752341));
#39827=CARTESIAN_POINT('Ctrl Pts',(210.182578301545,1.43694806559282,-4.53221958390462));
#39828=CARTESIAN_POINT('Ctrl Pts',(210.261767872602,3.42587732345312,-3.29684684606151));
#39829=CARTESIAN_POINT('Ctrl Pts',(210.34095744366,4.5840206323664,-1.26197833296432));
#39830=CARTESIAN_POINT('Ctrl Pts',(210.420147014717,4.63052457118939,1.07892383384874));
#39831=CARTESIAN_POINT('Ctrl Pts',(210.499336585775,3.55411180913573,3.15818361316701));
#39832=CARTESIAN_POINT('Ctrl Pts',(210.578526156832,1.61581580197477,4.47157396797902));
#39833=CARTESIAN_POINT('Ctrl Pts',(210.65771572789,-0.714320595070703,4.7005936390268));
#39834=CARTESIAN_POINT('Ctrl Pts',(210.736905298947,-2.87123201185134,3.78970463231423));
#39835=CARTESIAN_POINT('Ctrl Pts',(210.816094870005,-4.33186067524932,1.95980038722377));
#39836=CARTESIAN_POINT('Ctrl Pts',(210.895284441062,-4.74199956143928,-0.345361588627793));
#39837=CARTESIAN_POINT('Ctrl Pts',(210.97447401212,-4.00218870610474,-2.56677229764253));
#39838=CARTESIAN_POINT('Ctrl Pts',(211.053663583178,-2.29183455820929,-4.16573268769264));
#39839=CARTESIAN_POINT('Ctrl Pts',(211.132853154235,-0.0257033539061957,
-4.75448985748724));
#39840=CARTESIAN_POINT('Ctrl Pts',(211.212042725293,2.24666099419233,-4.19026834995021));
#39841=CARTESIAN_POINT('Ctrl Pts',(211.29123229635,3.97420301662046,-2.60989364727448));
#39842=CARTESIAN_POINT('Ctrl Pts',(211.370421867408,4.73798836377985,-0.396611563229904));
#39843=CARTESIAN_POINT('Ctrl Pts',(211.449611438465,4.35279669747736,1.91285006674178));
#39844=CARTESIAN_POINT('Ctrl Pts',(211.528801009523,2.91203820287448,3.75843956614982));
#39845=CARTESIAN_POINT('Ctrl Pts',(211.60799058058,0.765101326111594,4.69259570261332));
#39846=CARTESIAN_POINT('Ctrl Pts',(211.687180151638,-1.5673750178633,4.48878268807701));
#39847=CARTESIAN_POINT('Ctrl Pts',(211.766369722695,-3.51975801235516,3.1964258167309));
#39848=CARTESIAN_POINT('Ctrl Pts',(211.845559293753,-4.61858866803955,1.12892567641046));
#39849=CARTESIAN_POINT('Ctrl Pts',(211.924748864811,-4.59739711033398,-1.21234247524981));
#39850=CARTESIAN_POINT('Ctrl Pts',(212.003938435868,-3.46132235833556,-3.25961378066305));
#39851=CARTESIAN_POINT('Ctrl Pts',(212.083128006926,-1.48586609659888,-4.5164185379989));
#39852=CARTESIAN_POINT('Ctrl Pts',(212.162317577983,0.849917345999346,-4.67797765838739));
#39853=CARTESIAN_POINT('Ctrl Pts',(212.241507149041,2.97959317099309,-3.70511254927208));
#39854=CARTESIAN_POINT('Ctrl Pts',(212.320696720098,4.38670832253466,-1.83374604577822));
#39855=CARTESIAN_POINT('Ctrl Pts',(212.399886291156,4.73003297051818,0.482309615509662));
#39856=CARTESIAN_POINT('Ctrl Pts',(212.479075862213,3.92630981281437,2.68140368486352));
#39857=CARTESIAN_POINT('Ctrl Pts',(212.558265433271,2.17044423172616,4.23024896482096));
#39858=CARTESIAN_POINT('Ctrl Pts',(212.637455004329,-0.111760871493455,
4.75324562536013));
#39859=CARTESIAN_POINT('Ctrl Pts',(212.716644575386,-2.36686361343836,4.12356533873099));
#39860=CARTESIAN_POINT('Ctrl Pts',(212.795834146444,-4.04799451817251,2.49390754605045));
#39861=CARTESIAN_POINT('Ctrl Pts',(212.875023717501,-4.74747407746257,0.259469364709995));
#39862=CARTESIAN_POINT('Ctrl Pts',(212.954213288559,-4.29567630802097,-2.03789095000431));
#39863=CARTESIAN_POINT('Ctrl Pts',(213.033402859616,-2.80216358357373,-3.84105632844604));
#39864=CARTESIAN_POINT('Ctrl Pts',(213.112592430674,-0.629117416178179,
-4.71275352040221));
#39865=CARTESIAN_POINT('Ctrl Pts',(213.191782001732,1.69649169448747,-4.44159322742832));
#39866=CARTESIAN_POINT('Ctrl Pts',(213.270971572789,3.61069625730797,-3.09333266960803));
#39867=CARTESIAN_POINT('Ctrl Pts',(213.350161143847,4.64929567218066,-0.994929253788572));
#39868=CARTESIAN_POINT('Ctrl Pts',(213.429350714904,4.56042632901166,1.34474762132502));
#39869=CARTESIAN_POINT('Ctrl Pts',(213.508540285962,3.3656393217807,3.35831898769097));
#39870=CARTESIAN_POINT('Ctrl Pts',(213.587729857019,1.35467424077182,4.55748748421665));
#39871=CARTESIAN_POINT('Ctrl Pts',(213.666919428077,-0.984803585282112,
4.65145099574505));
#39872=CARTESIAN_POINT('Ctrl Pts',(213.746108999134,-3.08546345835945,3.61742307651878));
#39873=CARTESIAN_POINT('Ctrl Pts',(213.825298570192,-4.4378887818049,1.70615873462357));
#39874=CARTESIAN_POINT('Ctrl Pts',(213.90448814125,-4.71411218006672,-0.618854442618533));
#39875=CARTESIAN_POINT('Ctrl Pts',(213.983677712307,-3.84714861417571,-2.79379347981342));
#39876=CARTESIAN_POINT('Ctrl Pts',(214.062867283365,-2.04723946343398,-4.29122885042975));
#39877=CARTESIAN_POINT('Ctrl Pts',(214.142056854422,0.249131667358439,-4.74802778843188));
#39878=CARTESIAN_POINT('Ctrl Pts',(214.22124642548,2.48508758875339,-4.05341512105853));
#39879=CARTESIAN_POINT('Ctrl Pts',(214.300435996537,4.11840198874938,-2.37583659506863));
#39880=CARTESIAN_POINT('Ctrl Pts',(214.379625567595,4.7529910112316,-0.122110255727096));
#39881=CARTESIAN_POINT('Ctrl Pts',(214.458815138652,4.23496483126893,2.16122820297104));
#39882=CARTESIAN_POINT('Ctrl Pts',(214.53800470971,2.68994641950838,3.92046205536747));
#39883=CARTESIAN_POINT('Ctrl Pts',(214.617194280768,0.492607578451629,4.72897158387045));
#39884=CARTESIAN_POINT('Ctrl Pts',(214.696383851825,-1.82419014279682,4.39069069627149));
#39885=CARTESIAN_POINT('Ctrl Pts',(214.775573422882,-3.69861604264498,2.98765356701397));
#39886=CARTESIAN_POINT('Ctrl Pts',(214.85476299394,-4.67611597131303,0.860101093031097));
#39887=CARTESIAN_POINT('Ctrl Pts',(214.933952564997,-4.51964313542201,-1.47602858909806));
#39888=CARTESIAN_POINT('Ctrl Pts',(215.013142136055,-3.2671426876119,-3.45421671673712));
#39889=CARTESIAN_POINT('Ctrl Pts',(215.092331707113,-1.22234990821534,-4.59474647497423));
#39890=CARTESIAN_POINT('Ctrl Pts',(215.17152127817,1.11886655125696,-4.62103582629268));
#39891=CARTESIAN_POINT('Ctrl Pts',(215.250710849228,3.18875436873553,-3.52670952068245));
#39892=CARTESIAN_POINT('Ctrl Pts',(215.329900420285,4.48535926739899,-1.57714511372928));
#39893=CARTESIAN_POINT('Ctrl Pts',(215.409089991343,4.69425049948609,0.754881921545774));
#39894=CARTESIAN_POINT('Ctrl Pts',(215.4882795624,3.76477128715065,2.90384772721438));
#39895=CARTESIAN_POINT('Ctrl Pts',(215.567469133458,1.92232324970198,4.34862136671582));
#39896=CARTESIAN_POINT('Ctrl Pts',(215.646658704516,-0.386294194838778,
4.73884070870039));
#39897=CARTESIAN_POINT('Ctrl Pts',(215.725848275573,-2.60123408759472,3.97987634091028));
#39898=CARTESIAN_POINT('Ctrl Pts',(215.805037846631,-4.18536656931315,2.25577949894886));
#39899=CARTESIAN_POINT('Ctrl Pts',(215.884227417688,-4.75453455305645,-0.0153509346410333));
#39900=CARTESIAN_POINT('Ctrl Pts',(215.963416988746,-4.17071302062933,-2.28275871851474));
#39901=CARTESIAN_POINT('Ctrl Pts',(216.042606559803,-2.57548052166504,-3.99659036553987));
#39902=CARTESIAN_POINT('Ctrl Pts',(216.121796130861,-0.355685932038883,
-4.74123633508727));
#39903=CARTESIAN_POINT('Ctrl Pts',(216.200985701918,1.95036360980474,-4.33611764796016));
#39904=CARTESIAN_POINT('Ctrl Pts',(216.280175272976,3.78344386943341,-2.87947685426517));
#39905=CARTESIAN_POINT('Ctrl Pts',(216.359364844033,4.69902714427905,-0.724553907401494));
#39906=CARTESIAN_POINT('Ctrl Pts',(216.438554415091,4.47508162338355,1.60607563067777));
#39907=CARTESIAN_POINT('Ctrl Pts',(216.517743986149,3.16591479676605,3.54722679948997));
#39908=CARTESIAN_POINT('Ctrl Pts',(216.596933557206,1.08900371904967,4.6281643626062));
#39909=CARTESIAN_POINT('Ctrl Pts',(216.676123128263,-1.25199417034584,4.58675757641737));
#39910=CARTESIAN_POINT('Ctrl Pts',(216.755312699321,-3.289379553279,3.43304771622419));
#39911=CARTESIAN_POINT('Ctrl Pts',(216.834502270379,-4.52908009507498,1.44681303553627));
#39912=CARTESIAN_POINT('Ctrl Pts',(216.913691841436,-4.6704645326877,-0.890278336425393));
#39913=CARTESIAN_POINT('Ctrl Pts',(216.992881412494,-3.67924669730335,-3.01147442422885));
#39914=CARTESIAN_POINT('Ctrl Pts',(217.072070983551,-1.79580001763215,-4.40237853484619));
#39915=CARTESIAN_POINT('Ctrl Pts',(217.151260554609,0.523133789193805,-4.7256920663545));
#39916=CARTESIAN_POINT('Ctrl Pts',(217.230450125666,2.71520601414163,-3.9030104750271));
#39917=CARTESIAN_POINT('Ctrl Pts',(217.309639696724,4.24883227900368,-2.13383662268189));
#39918=CARTESIAN_POINT('Ctrl Pts',(217.388829267782,4.75210341257143,0.152799291978363));
#39919=CARTESIAN_POINT('Ctrl Pts',(217.468018838839,4.10297458914856,2.40238089989979));
#39920=CARTESIAN_POINT('Ctrl Pts',(217.547208409897,2.45886158092028,4.06937761743443));
#39921=CARTESIAN_POINT('Ctrl Pts',(217.626397980954,0.218466940309538,4.74953752100075));
#39922=CARTESIAN_POINT('Ctrl Pts',(217.705587552012,-2.07490661737412,4.27791970431648));
#39923=CARTESIAN_POINT('Ctrl Pts',(217.784777123069,-3.86510882354723,2.76889296462312));
#39924=CARTESIAN_POINT('Ctrl Pts',(217.863966694127,-4.71801003786133,0.588401011251541));
#39925=CARTESIAN_POINT('Ctrl Pts',(217.943156265184,-4.42677904530272,-1.73478002970719));
#39926=CARTESIAN_POINT('Ctrl Pts',(218.022345836242,-3.06204027344824,-3.63727148164433));
#39927=CARTESIAN_POINT('Ctrl Pts',(218.101535407299,-0.95474714764384,-4.65771321052166));
#39928=CARTESIAN_POINT('Ctrl Pts',(218.180724978357,1.3840751508993,-4.54864490195323));
#39929=CARTESIAN_POINT('Ctrl Pts',(218.259914549415,3.38725489163351,-3.33651596227367));
#39930=CARTESIAN_POINT('Ctrl Pts',(218.339104120472,4.5690147152194,-1.31527145468558));
#39931=CARTESIAN_POINT('Ctrl Pts',(218.41829369153,4.6427741641966,1.02493049894648));
#39932=CARTESIAN_POINT('Ctrl Pts',(218.497483262587,3.5906463412379,3.11658359739587));
#39933=CARTESIAN_POINT('Ctrl Pts',(218.576672833645,1.66777553775722,4.45245541505591));
#39934=CARTESIAN_POINT('Ctrl Pts',(218.655862404702,-0.659536055647559,
4.70859285335895));
#39935=CARTESIAN_POINT('Ctrl Pts',(218.73505197576,-2.82690809046628,3.8228817815175));
#39936=CARTESIAN_POINT('Ctrl Pts',(218.814241546817,-4.30874606193702,2.0101099077275));
#39937=CARTESIAN_POINT('Ctrl Pts',(218.893431117875,-4.74569962215444,-0.29011991259697));
#39938=CARTESIAN_POINT('Ctrl Pts',(218.972620688933,-4.03180616460846,-2.51999474571423));
#39939=CARTESIAN_POINT('Ctrl Pts',(219.05181025999,-2.34018708804546,-4.13876296257075));
#39940=CARTESIAN_POINT('Ctrl Pts',(219.130999831048,-0.0810653152070915,
-4.75386820200902));
#39941=CARTESIAN_POINT('Ctrl Pts',(219.210189402105,2.19771505039481,-4.21614551749227));
#39942=CARTESIAN_POINT('Ctrl Pts',(219.289378973163,3.94354263494978,-2.65599434369417));
#39943=CARTESIAN_POINT('Ctrl Pts',(219.36856854422,4.73304878279435,-0.4517562252931));
#39944=CARTESIAN_POINT('Ctrl Pts',(219.447758115278,4.37477578103172,1.86203419224794));
#39945=CARTESIAN_POINT('Ctrl Pts',(219.526947686335,2.9556059543878,3.72427548790225));
#39946=CARTESIAN_POINT('Ctrl Pts',(219.606137257393,0.819692429425529,4.68336831655856));
#39947=CARTESIAN_POINT('Ctrl Pts',(219.68532682845,-1.51499907623403,4.50672966422574));
#39948=CARTESIAN_POINT('Ctrl Pts',(219.764516399508,-3.48229856225139,3.23719495717262));
#39949=CARTESIAN_POINT('Ctrl Pts',(219.843705970566,-4.60512974340184,1.18263033693475));
#39950=CARTESIAN_POINT('Ctrl Pts',(219.922895541623,-4.61120254252834,-1.15872584297627));
#39951=CARTESIAN_POINT('Ctrl Pts',(220.002085112681,-3.49904428682886,-3.21908737784704));
#39952=CARTESIAN_POINT('Ctrl Pts',(220.081274683738,-1.53835683561813,-4.49881014421679));
#39953=CARTESIAN_POINT('Ctrl Pts',(220.160464254796,0.795386965018984,-4.68755736426519));
#39954=CARTESIAN_POINT('Ctrl Pts',(220.239653825853,2.93624693618633,-3.73955724613973));
#39955=CARTESIAN_POINT('Ctrl Pts',(220.318843396911,4.36505783155326,-1.88470278679332));
#39956=CARTESIAN_POINT('Ctrl Pts',(220.398032967968,4.73532853523991,0.42719799959265));
#39957=CARTESIAN_POINT('Ctrl Pts',(220.477222539026,3.95726724216151,2.63550193347166));
#39958=CARTESIAN_POINT('Ctrl Pts',(220.556412110083,2.21955625225993,4.20468839637894));
#39959=CARTESIAN_POINT('Ctrl Pts',(220.635601681141,-0.0564040787611365,
4.75422475777419));
#39960=CARTESIAN_POINT('Ctrl Pts',(220.714791252199,-2.3186862435803,4.15084672927046));
#39961=CARTESIAN_POINT('Ctrl Pts',(220.793980823256,-4.01867973527754,2.54087537220366));
#39962=CARTESIAN_POINT('Ctrl Pts',(220.873170394314,-4.7441308059444,0.314733781326927));
#39963=CARTESIAN_POINT('Ctrl Pts',(220.952359965371,-4.31911530641839,-1.98773173647174));
#39964=CARTESIAN_POINT('Ctrl Pts',(221.031549536429,-2.8467008113479,-3.8081660854415));
#39965=CARTESIAN_POINT('Ctrl Pts',(221.110739107486,-0.683952477452091,
-4.70510823248726));
#39966=CARTESIAN_POINT('Ctrl Pts',(221.189928678544,1.64465651901248,-4.46104690585135));
#39967=CARTESIAN_POINT('Ctrl Pts',(221.269118249601,3.57443106392721,-3.13516772584365));
#39968=CARTESIAN_POINT('Ctrl Pts',(221.348307820659,4.63739508778881,-1.04900057820502));
#39969=CARTESIAN_POINT('Ctrl Pts',(221.427497391716,4.57577584957209,1.29155254196728));
#39970=CARTESIAN_POINT('Ctrl Pts',(221.506686962774,3.40451755984005,3.31890002529642));
#39971=CARTESIAN_POINT('Ctrl Pts',(221.585876533832,1.40765114992216,4.54140407594682));
#39972=CARTESIAN_POINT('Ctrl Pts',(221.665066104889,-0.930570927433501,
4.66260296168317));
#39973=CARTESIAN_POINT('Ctrl Pts',(221.744255675947,-3.0431354414086,3.65310700279724));
#39974=CARTESIAN_POINT('Ctrl Pts',(221.823445247004,-4.41771141175782,1.75771911177364));
#39975=CARTESIAN_POINT('Ctrl Pts',(221.902634818062,-4.72101826342946,-0.563916692847134));
#39976=CARTESIAN_POINT('Ctrl Pts',(221.98182438912,-3.87937964092229,-2.74880956730796));
#39977=CARTESIAN_POINT('Ctrl Pts',(222.061013960177,-2.09716129213571,-4.26708329290772));
#39978=CARTESIAN_POINT('Ctrl Pts',(222.140203531235,0.193988579230145,-4.75059111312483));
#39979=CARTESIAN_POINT('Ctrl Pts',(222.192996578606,1.68938130567583,-4.30468574388314));
#39980=CARTESIAN_POINT('Ctrl Pts',(222.219393102292,2.33899160943743,-3.91675404524988));
#39981=CARTESIAN_POINT('Ctrl Pts',(209.342,2.5383587572263,-3.55965150255085));
#39982=CARTESIAN_POINT('Ctrl Pts',(209.368396523686,3.12874208667276,-3.13865391518958));
#39983=CARTESIAN_POINT('Ctrl Pts',(209.421189571058,4.09533550545485,-1.99754846162188));
#39984=CARTESIAN_POINT('Ctrl Pts',(209.500379142115,4.55219349719505,0.199542953564506));
#39985=CARTESIAN_POINT('Ctrl Pts',(209.579568713173,3.90500385774559,2.34791981561545));
#39986=CARTESIAN_POINT('Ctrl Pts',(209.65875828423,2.31088729255791,3.92708782806959));
#39987=CARTESIAN_POINT('Ctrl Pts',(209.737947855288,0.156348682839113,4.55384789993644));
#39988=CARTESIAN_POINT('Ctrl Pts',(209.817137426345,-2.03609361756371,4.07632219349179));
#39989=CARTESIAN_POINT('Ctrl Pts',(209.896326997403,-3.73478222633324,2.61025841618883));
#39990=CARTESIAN_POINT('Ctrl Pts',(209.97551656846,-4.52777192009244,0.511206898731814));
#39991=CARTESIAN_POINT('Ctrl Pts',(210.054706139518,-4.22276393917902,-1.71181770547838));
#39992=CARTESIAN_POINT('Ctrl Pts',(210.133895710575,-2.89372191923785,-3.5197193599864));
#39993=CARTESIAN_POINT('Ctrl Pts',(210.213085281633,-0.862943537879242,
-4.47407889498736));
#39994=CARTESIAN_POINT('Ctrl Pts',(210.29227485269,1.37710147802978,-4.3434598905811));
#39995=CARTESIAN_POINT('Ctrl Pts',(210.371464423748,3.2831950149358,-3.15953845045613));
#39996=CARTESIAN_POINT('Ctrl Pts',(210.450653994806,4.39310350826522,-1.20941895478298));
#39997=CARTESIAN_POINT('Ctrl Pts',(210.529843565863,4.43767063245068,1.03398838263629));
#39998=CARTESIAN_POINT('Ctrl Pts',(210.609033136921,3.40608873948736,3.02665031932622));
#39999=CARTESIAN_POINT('Ctrl Pts',(210.688222707978,1.54851965941115,4.28534006751519));
#40000=CARTESIAN_POINT('Ctrl Pts',(210.767412279036,-0.68457028532424,4.50482143573546));
#40001=CARTESIAN_POINT('Ctrl Pts',(210.846601850094,-2.75164979303246,3.63186949857032));
#40002=CARTESIAN_POINT('Ctrl Pts',(210.925791421151,-4.15144560986192,1.87817783712018));
#40003=CARTESIAN_POINT('Ctrl Pts',(211.004980992209,-4.5445028677362,-0.330977831100565));
#40004=CARTESIAN_POINT('Ctrl Pts',(211.084170563266,-3.83550395069923,-2.45987033873152));
#40005=CARTESIAN_POINT('Ctrl Pts',(211.163360134324,-2.19638331619705,-3.99223658715306));
#40006=CARTESIAN_POINT('Ctrl Pts',(211.242549705381,-0.0246328503458637,
-4.55647296294042));
#40007=CARTESIAN_POINT('Ctrl Pts',(211.321739276439,2.1530911588358,-4.01575037833895));
#40008=CARTESIAN_POINT('Ctrl Pts',(211.400928847496,3.80868382039997,-2.501195753153));
#40009=CARTESIAN_POINT('Ctrl Pts',(211.480118418554,4.54065873004066,-0.380093326269416));
#40010=CARTESIAN_POINT('Ctrl Pts',(211.559307989612,4.17150968026545,1.83318292235754));
#40011=CARTESIAN_POINT('Ctrl Pts',(211.638497560669,2.79075647149654,3.60190657238208));
#40012=CARTESIAN_POINT('Ctrl Pts',(211.717687131727,0.733236080175323,4.4971566005755));
#40013=CARTESIAN_POINT('Ctrl Pts',(211.796876702784,-1.50209635644419,4.30183207195806));
#40014=CARTESIAN_POINT('Ctrl Pts',(211.876066273842,-3.37316572337063,3.06329979630588));
#40015=CARTESIAN_POINT('Ctrl Pts',(211.955255844899,-4.42623184056749,1.081907728467));
#40016=CARTESIAN_POINT('Ctrl Pts',(212.034445415957,-4.40592287733015,-1.16185035111622));
#40017=CARTESIAN_POINT('Ctrl Pts',(212.113634987014,-3.31716382083363,-3.1238560826521));
#40018=CARTESIAN_POINT('Ctrl Pts',(212.192824558072,-1.42398215132184,-4.32831693295292));
#40019=CARTESIAN_POINT('Ctrl Pts',(212.272014129129,0.814519648555283,-4.48314737450014));
#40020=CARTESIAN_POINT('Ctrl Pts',(212.351203700187,2.85549788329282,-3.5508005404247));
#40021=CARTESIAN_POINT('Ctrl Pts',(212.430393271244,4.20400894040367,-1.75737345728678));
#40022=CARTESIAN_POINT('Ctrl Pts',(212.509582842302,4.53303466617831,0.462222191803663));
#40023=CARTESIAN_POINT('Ctrl Pts',(212.588772413359,3.76278529189487,2.56972751210507));
#40024=CARTESIAN_POINT('Ctrl Pts',(212.667961984417,2.08004870256613,4.05406586457634));
#40025=CARTESIAN_POINT('Ctrl Pts',(212.747151555475,-0.107106210032759,
4.55528055109042));
#40026=CARTESIAN_POINT('Ctrl Pts',(212.826341126532,-2.2682875313355,3.95182544080049));
#40027=CARTESIAN_POINT('Ctrl Pts',(212.90553069759,-3.87940202399173,2.39004028744685));
#40028=CARTESIAN_POINT('Ctrl Pts',(212.984720268647,-4.5497493789273,0.248662880866296));
#40029=CARTESIAN_POINT('Ctrl Pts',(213.063909839705,-4.11676826362727,-1.95301605291953));
#40030=CARTESIAN_POINT('Ctrl Pts',(213.143099410762,-2.685457954271,-3.68108247872997));
#40031=CARTESIAN_POINT('Ctrl Pts',(213.22228898182,-0.602915682492534,-4.51647487750953));
#40032=CARTESIAN_POINT('Ctrl Pts',(213.301478552877,1.62583553009629,-4.25660797683398));
#40033=CARTESIAN_POINT('Ctrl Pts',(213.380668123935,3.46031653593829,-2.96450031379357));
#40034=CARTESIAN_POINT('Ctrl Pts',(213.459857694992,4.45565994712272,-0.953492042429545));
#40035=CARTESIAN_POINT('Ctrl Pts',(213.53904726605,4.37049186989017,1.28874103472886));
#40036=CARTESIAN_POINT('Ctrl Pts',(213.618236837108,3.22546582964164,3.21845037575295));
#40037=CARTESIAN_POINT('Ctrl Pts',(213.697426408165,1.29825422636,4.36767542327822));
#40038=CARTESIAN_POINT('Ctrl Pts',(213.776615979223,-0.943788091813559,
4.45772550490954));
#40039=CARTESIAN_POINT('Ctrl Pts',(213.85580555028,-2.9569588426014,3.46676319389305));
#40040=CARTESIAN_POINT('Ctrl Pts',(213.934995121338,-4.25305781544302,1.63509995347965));
#40041=CARTESIAN_POINT('Ctrl Pts',(214.014184692395,-4.51777695117311,-0.593080145359114));
#40042=CARTESIAN_POINT('Ctrl Pts',(214.093374263453,-3.68692103050771,-2.6774364519387));
#40043=CARTESIAN_POINT('Ctrl Pts',(214.172563834511,-1.96197521572409,-4.11250603552804));
#40044=CARTESIAN_POINT('Ctrl Pts',(214.251753405568,0.238755732067328,-4.55028002872078));
#40045=CARTESIAN_POINT('Ctrl Pts',(214.330942976626,2.38158766725776,-3.88459686744144));
#40046=CARTESIAN_POINT('Ctrl Pts',(214.410132547683,3.94687713608336,-2.27688680263919));
#40047=CARTESIAN_POINT('Ctrl Pts',(214.489322118741,4.55503654123292,-0.117024558973872));
#40048=CARTESIAN_POINT('Ctrl Pts',(214.568511689798,4.05858532273295,2.07121650666143));
#40049=CARTESIAN_POINT('Ctrl Pts',(214.647701260856,2.57791445552183,3.75718108418821));
#40050=CARTESIAN_POINT('Ctrl Pts',(214.726890831913,0.472091261067617,4.53201748458606));
#40051=CARTESIAN_POINT('Ctrl Pts',(214.806080402971,-1.74821554237347,4.20782545464685));
#40052=CARTESIAN_POINT('Ctrl Pts',(214.885269974028,-3.54457460290309,2.86322257671746));
#40053=CARTESIAN_POINT('Ctrl Pts',(214.964459545086,-4.48136322371341,0.824279258818916));
#40054=CARTESIAN_POINT('Ctrl Pts',(215.043649116144,-4.33140723105327,-1.41455436026672));
#40055=CARTESIAN_POINT('Ctrl Pts',(215.122838687201,-3.13107142267409,-3.31035411783751));
#40056=CARTESIAN_POINT('Ctrl Pts',(215.202028258259,-1.17144099051237,-4.40338263669165));
#40057=CARTESIAN_POINT('Ctrl Pts',(215.281217829316,1.07226754977981,-4.42857707859527));
#40058=CARTESIAN_POINT('Ctrl Pts',(215.360407400374,3.05594785184388,-3.37982771249969));
#40059=CARTESIAN_POINT('Ctrl Pts',(215.439596971431,4.29855123127321,-1.5114595434512));
#40060=CARTESIAN_POINT('Ctrl Pts',(215.518786542489,4.49874247780649,0.723442297456857));
#40061=CARTESIAN_POINT('Ctrl Pts',(215.597976113546,3.60797458733507,2.7829071160415));
#40062=CARTESIAN_POINT('Ctrl Pts',(215.677165684604,1.84226156240618,4.16750824534888));
#40063=CARTESIAN_POINT('Ctrl Pts',(215.756355255662,-0.370205659762209,
4.54147557615916));
#40064=CARTESIAN_POINT('Ctrl Pts',(215.835544826719,-2.49289685027711,3.81412085981142));
#40065=CARTESIAN_POINT('Ctrl Pts',(215.914734397777,-4.01105274902173,2.16182989246041));
#40066=CARTESIAN_POINT('Ctrl Pts',(215.993923968834,-4.5565157970107,-0.0147115927774353));
#40067=CARTESIAN_POINT('Ctrl Pts',(216.073113539892,-3.99700949719232,-2.18768547070287));
#40068=CARTESIAN_POINT('Ctrl Pts',(216.152303110949,-2.46821587915816,-3.83013877206057));
#40069=CARTESIAN_POINT('Ctrl Pts',(216.231492682007,-0.340872182129313,
-4.54377142854046));
#40070=CARTESIAN_POINT('Ctrl Pts',(216.310682253064,1.86913408638018,-4.15552528647124));
#40071=CARTESIAN_POINT('Ctrl Pts',(216.389871824122,3.62586948644518,-2.75955125095293));
#40072=CARTESIAN_POINT('Ctrl Pts',(216.469061395179,4.50332018298729,-0.694377396571518));
#40073=CARTESIAN_POINT('Ctrl Pts',(216.548250966237,4.28870163468497,1.5391851506627));
#40074=CARTESIAN_POINT('Ctrl Pts',(216.627440537294,3.03405951149959,3.39949047947615));
#40075=CARTESIAN_POINT('Ctrl Pts',(216.706630108352,1.04364845674816,4.43540872277824));
#40076=CARTESIAN_POINT('Ctrl Pts',(216.78581967941,-1.19985061656117,4.39572646297605));
#40077=CARTESIAN_POINT('Ctrl Pts',(216.865009250467,-3.15238215846906,3.29006677232181));
#40078=CARTESIAN_POINT('Ctrl Pts',(216.944198821525,-4.3404511564375,1.38655558776074));
#40079=CARTESIAN_POINT('Ctrl Pts',(217.023388392582,-4.47594715846353,-0.853199668314748));
#40080=CARTESIAN_POINT('Ctrl Pts',(217.10257796364,-3.52601195980057,-2.8860513333469));
#40081=CARTESIAN_POINT('Ctrl Pts',(217.181767534697,-1.72100782049271,-4.21902651344751));
#40082=CARTESIAN_POINT('Ctrl Pts',(217.260957105755,0.501346103979698,-4.52887455372684));
#40083=CARTESIAN_POINT('Ctrl Pts',(217.340146676813,2.60212202845841,-3.74045633424341));
#40084=CARTESIAN_POINT('Ctrl Pts',(217.41933624787,4.07187521345992,-2.04496574185997));
#40085=CARTESIAN_POINT('Ctrl Pts',(217.498525818928,4.55418590963663,0.146435445973139));
#40086=CARTESIAN_POINT('Ctrl Pts',(217.577715389985,3.93209226298936,2.3023255796497));
#40087=CARTESIAN_POINT('Ctrl Pts',(217.656904961043,2.35645393068466,3.89989455138609));
#40088=CARTESIAN_POINT('Ctrl Pts',(217.7360945321,0.209368141831046,4.55172688334399));
#40089=CARTESIAN_POINT('Ctrl Pts',(217.815284103158,-1.98849007697495,4.0997511940534));
#40090=CARTESIAN_POINT('Ctrl Pts',(217.894473674215,-3.70413322589841,2.65357300336085));
#40091=CARTESIAN_POINT('Ctrl Pts',(217.973663245273,-4.52151246942783,0.563895050677703));
#40092=CARTESIAN_POINT('Ctrl Pts',(218.05285281633,-4.24241078168862,-1.66252921742216));
#40093=CARTESIAN_POINT('Ctrl Pts',(218.132042387388,-2.93451119586052,-3.48578494470606));
#40094=CARTESIAN_POINT('Ctrl Pts',(218.211231958445,-0.914983456707324,
-4.46372690846136));
#40095=CARTESIAN_POINT('Ctrl Pts',(218.290421529503,1.32643063562732,-4.35920112041638));
#40096=CARTESIAN_POINT('Ctrl Pts',(218.369611100561,3.24618114559881,-3.1975554114556));
#40097=CARTESIAN_POINT('Ctrl Pts',(218.448800671618,4.37872256355528,-1.26049250326289));
#40098=CARTESIAN_POINT('Ctrl Pts',(218.527990242676,4.44941004951064,0.982243783733906));
#40099=CARTESIAN_POINT('Ctrl Pts',(218.607179813733,3.44110166678914,2.98678287764463));
#40100=CARTESIAN_POINT('Ctrl Pts',(218.686369384791,1.59831535534295,4.26701777172829));
#40101=CARTESIAN_POINT('Ctrl Pts',(218.765558955848,-0.632067434303197,
4.51248749559082));
#40102=CARTESIAN_POINT('Ctrl Pts',(218.844748526906,-2.70917189204705,3.66366487259853));
#40103=CARTESIAN_POINT('Ctrl Pts',(218.923938097963,-4.12929368320664,1.92639204659899));
#40104=CARTESIAN_POINT('Ctrl Pts',(219.003127669021,-4.54804882684332,-0.278036882480057));
#40105=CARTESIAN_POINT('Ctrl Pts',(219.082317240079,-3.8638878894494,-2.41504099698875));
#40106=CARTESIAN_POINT('Ctrl Pts',(219.161506811136,-2.24272204053807,-3.96639010792621));
#40107=CARTESIAN_POINT('Ctrl Pts',(219.240696382194,-0.077689074547423,
-4.55587719841812));
#40108=CARTESIAN_POINT('Ctrl Pts',(219.319885953251,2.10618373527536,-4.04054980326089));
#40109=CARTESIAN_POINT('Ctrl Pts',(219.399075524309,3.77930039456389,-2.54537642933601));
#40110=CARTESIAN_POINT('Ctrl Pts',(219.478265095366,4.53592487469901,-0.43294130139881));
#40111=CARTESIAN_POINT('Ctrl Pts',(219.557454666424,4.19257337016016,1.78448344772206));
#40112=CARTESIAN_POINT('Ctrl Pts',(219.636644237481,2.83250969587536,3.569165373325));
#40113=CARTESIAN_POINT('Ctrl Pts',(219.715833808539,0.785553551391572,4.48831352038449));
#40114=CARTESIAN_POINT('Ctrl Pts',(219.795023379596,-1.45190178897309,4.3190315852685));
#40115=CARTESIAN_POINT('Ctrl Pts',(219.874212950654,-3.33726639942199,3.10237096728598));
#40116=CARTESIAN_POINT('Ctrl Pts',(219.953402521712,-4.41333345860431,1.13337567581733));
#40117=CARTESIAN_POINT('Ctrl Pts',(220.032592092769,-4.41915333536473,-1.11046676578087));
#40118=CARTESIAN_POINT('Ctrl Pts',(220.111781663827,-3.35331469136689,-3.08501753966403));
#40119=CARTESIAN_POINT('Ctrl Pts',(220.190971234884,-1.47428673505533,-4.31144190059531));
#40120=CARTESIAN_POINT('Ctrl Pts',(220.270160805942,0.762260370684581,-4.49232810095734));
#40121=CARTESIAN_POINT('Ctrl Pts',(220.349350376999,2.81395694980418,-3.58381067078537));
#40122=CARTESIAN_POINT('Ctrl Pts',(220.428539948057,4.18326015772707,-1.80620793157832));
#40123=CARTESIAN_POINT('Ctrl Pts',(220.507729519115,4.53810967910322,0.409405886501342));
#40124=CARTESIAN_POINT('Ctrl Pts',(220.586919090172,3.79245339384702,2.52573749520784));
#40125=CARTESIAN_POINT('Ctrl Pts',(220.66610866123,2.12711528603252,4.02956985290854));
#40126=CARTESIAN_POINT('Ctrl Pts',(220.745298232287,-0.0540549391371643,
4.55621890420622));
#40127=CARTESIAN_POINT('Ctrl Pts',(220.824487803345,-2.22211667183979,3.97797060507901));
#40128=CARTESIAN_POINT('Ctrl Pts',(220.903677374402,-3.85130815489554,2.43505197879753));
#40129=CARTESIAN_POINT('Ctrl Pts',(220.98286694546,-4.54654534931804,0.30162562296389));
#40130=CARTESIAN_POINT('Ctrl Pts',(221.062056516517,-4.13923106524796,-1.90494589036706));
#40131=CARTESIAN_POINT('Ctrl Pts',(221.141246087575,-2.72814027777575,-3.64956206171641));
#40132=CARTESIAN_POINT('Ctrl Pts',(221.220435658632,-0.655466951210102,
-4.50914800360244));
#40133=CARTESIAN_POINT('Ctrl Pts',(221.29962522969,1.57615920673447,-4.27525144067998));
#40134=CARTESIAN_POINT('Ctrl Pts',(221.378814800747,3.42556172983117,-3.00459300688041));
#40135=CARTESIAN_POINT('Ctrl Pts',(221.458004371805,4.44425500302777,-1.00531138270765));
#40136=CARTESIAN_POINT('Ctrl Pts',(221.537193942863,4.38520210748118,1.23776144530491));
#40137=CARTESIAN_POINT('Ctrl Pts',(221.61638351392,3.26272485129782,3.18067315006488));
#40138=CARTESIAN_POINT('Ctrl Pts',(221.695573084978,1.34902473201658,4.35226186322655));
#40139=CARTESIAN_POINT('Ctrl Pts',(221.774762656035,-0.891814137382579,
4.46841300931145));
#40140=CARTESIAN_POINT('Ctrl Pts',(221.853952227093,-2.91639371982429,3.50096094174254));
#40141=CARTESIAN_POINT('Ctrl Pts',(221.93314179815,-4.23372080057107,1.68451292342707));
#40142=CARTESIAN_POINT('Ctrl Pts',(222.012331369208,-4.52439540721473,-0.540430464955662));
#40143=CARTESIAN_POINT('Ctrl Pts',(222.091520940266,-3.71780968656559,-2.63432604740694));
#40144=CARTESIAN_POINT('Ctrl Pts',(222.170710511323,-2.00981788014407,-4.08936610183967));
#40145=CARTESIAN_POINT('Ctrl Pts',(222.249900082381,0.185909265320968,-4.55273659504203));
#40146=CARTESIAN_POINT('Ctrl Pts',(222.302693129752,1.61902127760079,-4.12540247090247));
#40147=CARTESIAN_POINT('Ctrl Pts',(222.329089653438,2.24157635170112,-3.75362750675853));
#40148=CARTESIAN_POINT('',(222.,2.53382212490982,-4.24300712223271));
#40149=CARTESIAN_POINT('Ctrl Pts',(222.,-4.36842834878726,-0.181075889670495));
#40150=CARTESIAN_POINT('Ctrl Pts',(222.,-4.37098573801141,-0.294564226943176));
#40151=CARTESIAN_POINT('Ctrl Pts',(222.,-4.36909332532532,-0.408000110792678));
#40152=CARTESIAN_POINT('Ctrl Pts',(222.,-4.36272833344689,-0.521122630740717));
#40153=CARTESIAN_POINT('Ctrl Pts',(222.,-4.35524756813103,-0.654075357127793));
#40154=CARTESIAN_POINT('Ctrl Pts',(222.,-4.3415902166335,-0.786595637407321));
#40155=CARTESIAN_POINT('Ctrl Pts',(222.,-4.32194320104597,-0.918301328088664));
#40156=CARTESIAN_POINT('Ctrl Pts',(222.,-4.31073473472777,-0.993438378361748));
#40157=CARTESIAN_POINT('Ctrl Pts',(222.,-4.29757589374814,-1.06831043566032));
#40158=CARTESIAN_POINT('Ctrl Pts',(222.,-4.28249385860505,-1.14284660544086));
#40159=CARTESIAN_POINT('Ctrl Pts',(222.,-4.27226836316086,-1.19338151384594));
#40160=CARTESIAN_POINT('Ctrl Pts',(222.,-4.2611587153347,-1.24376202130847));
#40161=CARTESIAN_POINT('Ctrl Pts',(222.,-4.24917200170829,-1.29396584478053));
#40162=CARTESIAN_POINT('Ctrl Pts',(222.,-4.24463496174222,-1.31296828036392));
#40163=CARTESIAN_POINT('Ctrl Pts',(222.,-4.23997254218613,-1.3319440220672));
#40164=CARTESIAN_POINT('Ctrl Pts',(222.,-4.23518762442552,-1.35088254754639));
#40165=CARTESIAN_POINT('Ctrl Pts',(222.,-4.20189893344145,-1.48263794103715));
#40166=CARTESIAN_POINT('Ctrl Pts',(222.,-4.16265630755129,-1.61271654924556));
#40167=CARTESIAN_POINT('Ctrl Pts',(222.,-4.11765567171295,-1.74072293688837));
#40168=CARTESIAN_POINT('Ctrl Pts',(222.,-4.07248857953235,-1.8692028172869));
#40169=CARTESIAN_POINT('Ctrl Pts',(222.,-4.02152063408476,-1.99559591273624));
#40170=CARTESIAN_POINT('Ctrl Pts',(222.,-3.96489773029065,-2.11949676875068));
#40171=CARTESIAN_POINT('Ctrl Pts',(222.,-3.94205531338401,-2.16947998788162));
#40172=CARTESIAN_POINT('Ctrl Pts',(222.,-3.91829201952593,-2.21905748457378));
#40173=CARTESIAN_POINT('Ctrl Pts',(222.,-3.89361512847883,-2.26820192736284));
#40174=CARTESIAN_POINT('Ctrl Pts',(222.,-3.88019709114222,-2.29492417397697));
#40175=CARTESIAN_POINT('Ctrl Pts',(222.,-3.86650891432765,-2.32151837366928));
#40176=CARTESIAN_POINT('Ctrl Pts',(222.,-3.85255160932784,-2.34798006053391));
#40177=CARTESIAN_POINT('Ctrl Pts',(222.,-3.83952664999993,-2.37267411108051));
#40178=CARTESIAN_POINT('Ctrl Pts',(222.,-3.82626470140156,-2.39725729977753));
#40179=CARTESIAN_POINT('Ctrl Pts',(222.,-3.81278183000108,-2.42169876135494));
#40180=CARTESIAN_POINT('Ctrl Pts',(222.,-3.77582885392445,-2.4886863278844));
#40181=CARTESIAN_POINT('Ctrl Pts',(222.,-3.73719936713687,-2.55464384426184));
#40182=CARTESIAN_POINT('Ctrl Pts',(222.,-3.69692762264733,-2.61950430450256));
#40183=CARTESIAN_POINT('Ctrl Pts',(222.,-3.62547763214162,-2.73457950988876));
#40184=CARTESIAN_POINT('Ctrl Pts',(222.,-3.54886116571452,-2.84620257618153));
#40185=CARTESIAN_POINT('Ctrl Pts',(222.,-3.46744919683223,-2.95414631713669));
#40186=CARTESIAN_POINT('Ctrl Pts',(222.,-3.3848883088047,-3.06361340450265));
#40187=CARTESIAN_POINT('Ctrl Pts',(222.,-3.29739521161876,-3.1692971916575));
#40188=CARTESIAN_POINT('Ctrl Pts',(222.,-3.2053076828989,-3.27093946602781));
#40189=CARTESIAN_POINT('Ctrl Pts',(222.,-3.12292504328557,-3.36186989901187));
#40190=CARTESIAN_POINT('Ctrl Pts',(222.,-3.03686442460084,-3.449565783402));
#40191=CARTESIAN_POINT('Ctrl Pts',(222.,-2.94733923617142,-3.53382207273257));
#40192=CARTESIAN_POINT('Ctrl Pts',(222.,-2.88019534484935,-3.5970142897305));
#40193=CARTESIAN_POINT('Ctrl Pts',(222.,-2.81110205788549,-3.65827137366228));
#40194=CARTESIAN_POINT('Ctrl Pts',(222.,-2.74014107955737,-3.71749798768638));
#40195=CARTESIAN_POINT('Ctrl Pts',(222.,-2.71949941549928,-3.73472627143876));
#40196=CARTESIAN_POINT('Ctrl Pts',(222.,-2.69869477510875,-3.75178651986409));
#40197=CARTESIAN_POINT('Ctrl Pts',(222.,-2.67775618886315,-3.76865475809313));
#40198=CARTESIAN_POINT('Ctrl Pts',(222.,-2.56828725956211,-3.85684351909489));
#40199=CARTESIAN_POINT('Ctrl Pts',(222.,-2.45505249945321,-3.93988052555356));
#40200=CARTESIAN_POINT('Ctrl Pts',(222.,-2.33842175663197,-4.01751530374901));
#40201=CARTESIAN_POINT('Ctrl Pts',(222.,-2.24728794844213,-4.0781781514149));
#40202=CARTESIAN_POINT('Ctrl Pts',(222.,-2.15407959825342,-4.13554221388341));
#40203=CARTESIAN_POINT('Ctrl Pts',(222.,-2.05895545541908,-4.1894747272104));
#40204=CARTESIAN_POINT('Ctrl Pts',(222.,-1.93779588756135,-4.25816853945908));
#40205=CARTESIAN_POINT('Ctrl Pts',(222.,-1.81352904188079,-4.32129707181206));
#40206=CARTESIAN_POINT('Ctrl Pts',(222.,-1.68657664425576,-4.37879834388636));
#40207=CARTESIAN_POINT('Ctrl Pts',(222.,-1.55887908425306,-4.43663712659787));
#40208=CARTESIAN_POINT('Ctrl Pts',(222.,-1.42846364438894,-4.48878270602783));
#40209=CARTESIAN_POINT('Ctrl Pts',(222.,-1.29573422995731,-4.53512593072363));
#40210=CARTESIAN_POINT('Ctrl Pts',(222.,-1.24442289374099,-4.55304157356661));
#40211=CARTESIAN_POINT('Ctrl Pts',(222.,-1.19276552717026,-4.57008955079262));
#40212=CARTESIAN_POINT('Ctrl Pts',(222.,-1.14078481387357,-4.58626157075573));
#40213=CARTESIAN_POINT('Ctrl Pts',(222.,-1.11945747958225,-4.59289684091739));
#40214=CARTESIAN_POINT('Ctrl Pts',(222.,-1.09807373972044,-4.59938514101186));
#40215=CARTESIAN_POINT('Ctrl Pts',(222.,-1.07665683628407,-4.60571966869325));
#40216=CARTESIAN_POINT('Ctrl Pts',(222.,-0.94036242090938,-4.64603178708956));
#40217=CARTESIAN_POINT('Ctrl Pts',(222.,-0.802537508945014,-4.68018040969709));
#40218=CARTESIAN_POINT('Ctrl Pts',(222.,-0.663631693948421,-4.70813488340432));
#40219=CARTESIAN_POINT('Ctrl Pts',(222.,-0.522032220811885,-4.73663144957651));
#40220=CARTESIAN_POINT('Ctrl Pts',(222.,-0.379308809281521,-4.75869170631474));
#40221=CARTESIAN_POINT('Ctrl Pts',(222.,-0.2359104528045,-4.7742353901663));
#40222=CARTESIAN_POINT('Ctrl Pts',(222.,-0.0925120963274796,-4.78977907401787));
#40223=CARTESIAN_POINT('Ctrl Pts',(222.,0.0515620228970814,-4.79880645835128));
#40224=CARTESIAN_POINT('Ctrl Pts',(222.,0.195878260323218,-4.80118506931799));
#40225=CARTESIAN_POINT('Ctrl Pts',(222.,0.29689613471544,-4.80285003944297));
#40226=CARTESIAN_POINT('Ctrl Pts',(222.,0.398032971152377,-4.80125620971581));
#40227=CARTESIAN_POINT('Ctrl Pts',(222.,0.499147154433433,-4.79644184461924));
#40228=CARTESIAN_POINT('Ctrl Pts',(222.,0.543384609618895,-4.79433555988949));
#40229=CARTESIAN_POINT('Ctrl Pts',(222.,0.587617726136605,-4.79161267339));
#40230=CARTESIAN_POINT('Ctrl Pts',(222.,0.631834586924468,-4.78827559687945));
#40231=CARTESIAN_POINT('Ctrl Pts',(222.,0.65953222059132,-4.78618523765763));
#40232=CARTESIAN_POINT('Ctrl Pts',(222.,0.687223474722988,-4.78385387155131));
#40233=CARTESIAN_POINT('Ctrl Pts',(222.,0.714905404701823,-4.78128199606419));
#40234=CARTESIAN_POINT('Ctrl Pts',(222.,0.733390830872528,-4.77956455026205));
#40235=CARTESIAN_POINT('Ctrl Pts',(222.,0.751867033752694,-4.77774029318992));
#40236=CARTESIAN_POINT('Ctrl Pts',(222.,0.770325374548045,-4.77581043336942));
#40237=CARTESIAN_POINT('Ctrl Pts',(222.,0.912376353166609,-4.76095869348995));
#40238=CARTESIAN_POINT('Ctrl Pts',(222.,1.05350857384173,-4.7398439933652));
#40239=CARTESIAN_POINT('Ctrl Pts',(222.,1.19332576755747,-4.71266318948087));
#40240=CARTESIAN_POINT('Ctrl Pts',(222.,1.33571979507934,-4.68498144281214));
#40241=CARTESIAN_POINT('Ctrl Pts',(222.,1.47675060798872,-4.65100794853853));
#40242=CARTESIAN_POINT('Ctrl Pts',(222.,1.61600588548905,-4.61089731421076));
#40243=CARTESIAN_POINT('Ctrl Pts',(222.,1.755439378739,-4.5707353472018));
#40244=CARTESIAN_POINT('Ctrl Pts',(222.,1.89309357002474,-4.52442039296622));
#40245=CARTESIAN_POINT('Ctrl Pts',(222.,2.02854931760949,-4.47205576788645));
#40246=CARTESIAN_POINT('Ctrl Pts',(222.,2.16242889981937,-4.4203004584717));
#40247=CARTESIAN_POINT('Ctrl Pts',(222.,2.29416163637294,-4.36263522966432));
#40248=CARTESIAN_POINT('Ctrl Pts',(222.,2.42332650648257,-4.29911192429263));
#40249=CARTESIAN_POINT('Ctrl Pts',(222.,2.46037320343389,-4.28089235234978));
#40250=CARTESIAN_POINT('Ctrl Pts',(222.,2.49720851529581,-4.26219057786635));
#40251=CARTESIAN_POINT('Ctrl Pts',(222.,2.53382212491006,-4.24300712223256));
#40252=CARTESIAN_POINT('Ctrl Pts',(222.,2.53382212490976,-4.24300712223274));
#40253=CARTESIAN_POINT('Ctrl Pts',(221.973603476314,1.83010136182567,-4.66325228984456));
#40254=CARTESIAN_POINT('Ctrl Pts',(221.947206952628,1.02012428443705,-4.90477621956747));
#40255=CARTESIAN_POINT('Ctrl Pts',(221.920810428943,0.201469858548206,-4.93824110538784));
#40256=CARTESIAN_POINT('Ctrl Pts',(221.894413905257,-0.617184567340706,
-4.97170599120821));
#40257=CARTESIAN_POINT('Ctrl Pts',(221.868017381571,-1.44451634172984,-4.79711183312601));
#40258=CARTESIAN_POINT('Ctrl Pts',(221.841620857885,-2.17996080117718,-4.43569124276262));
#40259=CARTESIAN_POINT('Ctrl Pts',(221.815224334199,-2.91540526062457,-4.07427065239921));
#40260=CARTESIAN_POINT('Ctrl Pts',(221.788827810513,-3.55896240513016,-3.52602362975458));
#40261=CARTESIAN_POINT('Ctrl Pts',(221.762431286827,-4.03269838175349,-2.85741887535226));
#40262=CARTESIAN_POINT('Ctrl Pts',(221.736034763142,-4.50643435837679,-2.18881412094998));
#40263=CARTESIAN_POINT('Ctrl Pts',(221.709638239456,-4.81034916711786,-1.39985163479002));
#40264=CARTESIAN_POINT('Ctrl Pts',(221.68324171577,-4.90754468120046,-0.586200285527234));
#40265=CARTESIAN_POINT('Ctrl Pts',(221.676934628732,-4.9307682152643,-0.391789463134336));
#40266=CARTESIAN_POINT('Ctrl Pts',(221.670627541695,-4.94219003245996,-0.195969140130387));
#40267=CARTESIAN_POINT('Ctrl Pts',(221.664320454657,-4.94199158848527,-0.000125892924181525));
#40268=CARTESIAN_POINT('Origin',(228.,-0.6,-7.5));
#40269=CARTESIAN_POINT('',(226.2,-0.6,7.5));
#40270=CARTESIAN_POINT('Origin',(226.2,0.,0.));
#40271=CARTESIAN_POINT('',(226.2,0.6,-7.5));
#40272=CARTESIAN_POINT('',(226.2,4.163799117101E-16,6.8));
#40273=CARTESIAN_POINT('',(226.2,-1.7,5.1));
#40274=CARTESIAN_POINT('',(226.2,1.575,5.225));
#40275=CARTESIAN_POINT('',(226.2,-1.2491397351303E-15,-6.8));
#40276=CARTESIAN_POINT('',(226.2,1.7,-5.1));
#40277=CARTESIAN_POINT('',(226.2,-1.575,-5.225));
#40278=CARTESIAN_POINT('Origin',(228.,0.6,7.5));
#40279=CARTESIAN_POINT('Origin',(222.5,-1.2491397351303E-15,-6.8));
#40280=CARTESIAN_POINT('',(222.5,-1.2491397351303E-15,-6.8));
#40281=CARTESIAN_POINT('',(222.5,-1.2491397351303E-15,-6.8));
#40282=CARTESIAN_POINT('',(222.5,-1.2491397351303E-15,-6.8));
#40283=CARTESIAN_POINT('Origin',(222.5,6.87448183661356,-1.58319281140051));
#40284=CARTESIAN_POINT('',(227.5,6.56829561876566,-1.75996950669715));
#40285=CARTESIAN_POINT('',(227.5,6.87448183661356,-1.58319281140051));
#40286=CARTESIAN_POINT('',(222.5,6.56829561876566,-1.75996950669715));
#40287=CARTESIAN_POINT('',(222.5,6.56829561876566,-1.75996950669715));
#40288=CARTESIAN_POINT('',(222.5,6.87448183661356,-1.58319281140051));
#40289=CARTESIAN_POINT('Origin',(222.5,6.6890363470518,-1.79232188733496));
#40290=CARTESIAN_POINT('',(222.5,6.56829561876566,-1.75996950669715));
#40291=CARTESIAN_POINT('Origin',(222.5,6.56829561876566,-1.75996950669715));
#40292=CARTESIAN_POINT('',(227.5,6.56829561876566,-1.75996950669715));
#40293=CARTESIAN_POINT('Origin',(227.5,6.6890363470518,-1.79232188733496));
#40294=CARTESIAN_POINT('Origin',(222.5,6.23047909668029,-3.30849364905389));
#40295=CARTESIAN_POINT('',(227.5,5.88897274573418,-3.4));
#40296=CARTESIAN_POINT('',(227.5,6.23047909668029,-3.30849364905389));
#40297=CARTESIAN_POINT('',(222.5,5.88897274573418,-3.4));
#40298=CARTESIAN_POINT('',(222.5,5.88897274573418,-3.4));
#40299=CARTESIAN_POINT('',(222.5,6.23047909668029,-3.30849364905389));
#40300=CARTESIAN_POINT('Origin',(222.5,5.99722592120723,-3.4625));
#40301=CARTESIAN_POINT('',(222.5,5.88897274573418,-3.4));
#40302=CARTESIAN_POINT('Origin',(222.5,5.88897274573418,-3.4));
#40303=CARTESIAN_POINT('',(227.5,5.88897274573418,-3.4));
#40304=CARTESIAN_POINT('Origin',(227.5,5.99722592120723,-3.4625));
#40305=CARTESIAN_POINT('Origin',(222.5,5.1618795026618,-4.80832611206852));
#40306=CARTESIAN_POINT('',(227.5,4.80832611206852,-4.80832611206852));
#40307=CARTESIAN_POINT('',(227.5,5.1618795026618,-4.80832611206852));
#40308=CARTESIAN_POINT('',(222.5,4.80832611206852,-4.80832611206852));
#40309=CARTESIAN_POINT('',(222.5,4.80832611206852,-4.80832611206852));
#40310=CARTESIAN_POINT('',(222.5,5.1618795026618,-4.80832611206852));
#40311=CARTESIAN_POINT('Origin',(222.5,4.89671445971684,-4.89671445971684));
#40312=CARTESIAN_POINT('',(222.5,4.80832611206852,-4.80832611206852));
#40313=CARTESIAN_POINT('Origin',(222.5,4.80832611206852,-4.80832611206852));
#40314=CARTESIAN_POINT('',(227.5,4.80832611206852,-4.80832611206852));
#40315=CARTESIAN_POINT('Origin',(227.5,4.89671445971684,-4.89671445971684));
#40316=CARTESIAN_POINT('Origin',(222.5,3.7415063509461,-5.9804790966803));
#40317=CARTESIAN_POINT('',(227.5,3.39999999999999,-5.88897274573418));
#40318=CARTESIAN_POINT('',(227.5,3.7415063509461,-5.9804790966803));
#40319=CARTESIAN_POINT('',(222.5,3.39999999999999,-5.88897274573418));
#40320=CARTESIAN_POINT('',(222.5,3.39999999999999,-5.88897274573418));
#40321=CARTESIAN_POINT('',(222.5,3.7415063509461,-5.9804790966803));
#40322=CARTESIAN_POINT('Origin',(222.5,3.46249999999999,-5.99722592120724));
#40323=CARTESIAN_POINT('',(222.5,3.39999999999999,-5.88897274573418));
#40324=CARTESIAN_POINT('Origin',(222.5,3.39999999999999,-5.88897274573418));
#40325=CARTESIAN_POINT('',(227.5,3.39999999999999,-5.88897274573418));
#40326=CARTESIAN_POINT('Origin',(227.5,3.46249999999999,-5.99722592120724));
#40327=CARTESIAN_POINT('Origin',(222.5,2.06615572454504,-6.7450723140623));
#40328=CARTESIAN_POINT('',(227.5,1.75996950669714,-6.56829561876567));
#40329=CARTESIAN_POINT('',(227.5,2.06615572454504,-6.7450723140623));
#40330=CARTESIAN_POINT('',(222.5,1.75996950669714,-6.56829561876567));
#40331=CARTESIAN_POINT('',(222.5,1.75996950669714,-6.56829561876567));
#40332=CARTESIAN_POINT('',(222.5,2.06615572454504,-6.7450723140623));
#40333=CARTESIAN_POINT('Origin',(222.5,1.79232188733495,-6.6890363470518));
#40334=CARTESIAN_POINT('',(222.5,1.75996950669714,-6.56829561876567));
#40335=CARTESIAN_POINT('Origin',(222.5,1.75996950669714,-6.56829561876567));
#40336=CARTESIAN_POINT('',(227.5,1.75996950669714,-6.56829561876567));
#40337=CARTESIAN_POINT('Origin',(227.5,1.79232188733495,-6.6890363470518));
#40338=CARTESIAN_POINT('Origin',(222.5,0.249999999999999,-7.05));
#40339=CARTESIAN_POINT('',(222.5,0.249999999999999,-7.05));
#40340=CARTESIAN_POINT('Origin',(222.5,-1.27210186261431E-15,-6.925));
#40341=CARTESIAN_POINT('Origin',(222.5,-1.58319281140051,-6.87448183661356));
#40342=CARTESIAN_POINT('',(227.5,-1.75996950669715,-6.56829561876566));
#40343=CARTESIAN_POINT('',(227.5,-1.58319281140051,-6.87448183661356));
#40344=CARTESIAN_POINT('',(222.5,-1.75996950669715,-6.56829561876566));
#40345=CARTESIAN_POINT('',(222.5,-1.75996950669715,-6.56829561876566));
#40346=CARTESIAN_POINT('',(222.5,-1.58319281140051,-6.87448183661356));
#40347=CARTESIAN_POINT('Origin',(222.5,-1.79232188733496,-6.6890363470518));
#40348=CARTESIAN_POINT('',(222.5,-1.75996950669715,-6.56829561876566));
#40349=CARTESIAN_POINT('Origin',(222.5,-1.75996950669715,-6.56829561876566));
#40350=CARTESIAN_POINT('',(227.5,-1.75996950669715,-6.56829561876566));
#40351=CARTESIAN_POINT('Origin',(227.5,-1.79232188733496,-6.6890363470518));
#40352=CARTESIAN_POINT('Origin',(222.5,-3.30849364905389,-6.23047909668029));
#40353=CARTESIAN_POINT('',(227.5,-3.4,-5.88897274573418));
#40354=CARTESIAN_POINT('',(227.5,-3.30849364905389,-6.23047909668029));
#40355=CARTESIAN_POINT('',(222.5,-3.4,-5.88897274573418));
#40356=CARTESIAN_POINT('',(222.5,-3.4,-5.88897274573418));
#40357=CARTESIAN_POINT('',(222.5,-3.30849364905389,-6.23047909668029));
#40358=CARTESIAN_POINT('Origin',(222.5,-3.4625,-5.99722592120723));
#40359=CARTESIAN_POINT('',(222.5,-3.4,-5.88897274573418));
#40360=CARTESIAN_POINT('Origin',(222.5,-3.4,-5.88897274573418));
#40361=CARTESIAN_POINT('',(227.5,-3.4,-5.88897274573418));
#40362=CARTESIAN_POINT('Origin',(227.5,-3.4625,-5.99722592120723));
#40363=CARTESIAN_POINT('Origin',(222.5,-4.80832611206853,-5.16187950266179));
#40364=CARTESIAN_POINT('',(227.5,-4.80832611206853,-4.80832611206852));
#40365=CARTESIAN_POINT('',(227.5,-4.80832611206853,-5.16187950266179));
#40366=CARTESIAN_POINT('',(222.5,-4.80832611206853,-4.80832611206852));
#40367=CARTESIAN_POINT('',(222.5,-4.80832611206853,-4.80832611206852));
#40368=CARTESIAN_POINT('',(222.5,-4.80832611206853,-5.16187950266179));
#40369=CARTESIAN_POINT('Origin',(222.5,-4.89671445971684,-4.89671445971684));
#40370=CARTESIAN_POINT('',(222.5,-4.80832611206853,-4.80832611206852));
#40371=CARTESIAN_POINT('Origin',(222.5,-4.80832611206853,-4.80832611206852));
#40372=CARTESIAN_POINT('',(227.5,-4.80832611206853,-4.80832611206852));
#40373=CARTESIAN_POINT('Origin',(227.5,-4.89671445971684,-4.89671445971684));
#40374=CARTESIAN_POINT('Origin',(222.5,-5.98047909668029,-3.74150635094611));
#40375=CARTESIAN_POINT('',(227.5,-5.88897274573418,-3.4));
#40376=CARTESIAN_POINT('',(227.5,-5.98047909668029,-3.74150635094611));
#40377=CARTESIAN_POINT('',(222.5,-5.88897274573418,-3.4));
#40378=CARTESIAN_POINT('',(222.5,-5.88897274573418,-3.4));
#40379=CARTESIAN_POINT('',(222.5,-5.98047909668029,-3.74150635094611));
#40380=CARTESIAN_POINT('Origin',(222.5,-5.99722592120724,-3.4625));
#40381=CARTESIAN_POINT('',(222.5,-5.88897274573418,-3.4));
#40382=CARTESIAN_POINT('Origin',(222.5,-5.88897274573418,-3.4));
#40383=CARTESIAN_POINT('',(227.5,-5.88897274573418,-3.4));
#40384=CARTESIAN_POINT('Origin',(227.5,-5.99722592120724,-3.4625));
#40385=CARTESIAN_POINT('Origin',(222.5,-6.7450723140623,-2.06615572454504));
#40386=CARTESIAN_POINT('',(227.5,-6.56829561876567,-1.75996950669714));
#40387=CARTESIAN_POINT('',(227.5,-6.7450723140623,-2.06615572454504));
#40388=CARTESIAN_POINT('',(222.5,-6.56829561876567,-1.75996950669714));
#40389=CARTESIAN_POINT('',(222.5,-6.56829561876567,-1.75996950669714));
#40390=CARTESIAN_POINT('',(222.5,-6.7450723140623,-2.06615572454504));
#40391=CARTESIAN_POINT('Origin',(222.5,-6.6890363470518,-1.79232188733495));
#40392=CARTESIAN_POINT('',(222.5,-6.56829561876567,-1.75996950669714));
#40393=CARTESIAN_POINT('Origin',(222.5,-6.56829561876567,-1.75996950669714));
#40394=CARTESIAN_POINT('',(227.5,-6.56829561876567,-1.75996950669714));
#40395=CARTESIAN_POINT('Origin',(227.5,-6.6890363470518,-1.79232188733495));
#40396=CARTESIAN_POINT('Origin',(222.5,-7.05,-0.249999999999999));
#40397=CARTESIAN_POINT('',(227.5,-6.8,8.327598234202E-16));
#40398=CARTESIAN_POINT('',(227.5,-7.05,-0.249999999999999));
#40399=CARTESIAN_POINT('',(222.5,-6.8,8.327598234202E-16));
#40400=CARTESIAN_POINT('',(222.5,-6.8,8.327598234202E-16));
#40401=CARTESIAN_POINT('',(222.5,-7.05,-0.249999999999999));
#40402=CARTESIAN_POINT('Origin',(222.5,-6.925,8.48067908409542E-16));
#40403=CARTESIAN_POINT('',(222.5,-6.8,8.327598234202E-16));
#40404=CARTESIAN_POINT('Origin',(222.5,-6.8,8.327598234202E-16));
#40405=CARTESIAN_POINT('',(227.5,-6.8,8.327598234202E-16));
#40406=CARTESIAN_POINT('Origin',(227.5,-6.925,8.48067908409542E-16));
#40407=CARTESIAN_POINT('Origin',(222.5,-6.87448183661356,1.58319281140051));
#40408=CARTESIAN_POINT('',(227.5,-6.56829561876566,1.75996950669714));
#40409=CARTESIAN_POINT('',(227.5,-6.87448183661356,1.58319281140051));
#40410=CARTESIAN_POINT('',(222.5,-6.56829561876566,1.75996950669714));
#40411=CARTESIAN_POINT('',(222.5,-6.56829561876566,1.75996950669714));
#40412=CARTESIAN_POINT('',(222.5,-6.87448183661356,1.58319281140051));
#40413=CARTESIAN_POINT('Origin',(222.5,-6.6890363470518,1.79232188733496));
#40414=CARTESIAN_POINT('',(222.5,-6.56829561876566,1.75996950669714));
#40415=CARTESIAN_POINT('Origin',(222.5,-6.56829561876566,1.75996950669714));
#40416=CARTESIAN_POINT('',(227.5,-6.56829561876566,1.75996950669714));
#40417=CARTESIAN_POINT('Origin',(227.5,-6.6890363470518,1.79232188733496));
#40418=CARTESIAN_POINT('Origin',(222.5,-6.23047909668029,3.30849364905389));
#40419=CARTESIAN_POINT('',(227.5,-5.88897274573418,3.4));
#40420=CARTESIAN_POINT('',(227.5,-6.23047909668029,3.30849364905389));
#40421=CARTESIAN_POINT('',(222.5,-5.88897274573418,3.4));
#40422=CARTESIAN_POINT('',(222.5,-5.88897274573418,3.4));
#40423=CARTESIAN_POINT('',(222.5,-6.23047909668029,3.30849364905389));
#40424=CARTESIAN_POINT('Origin',(222.5,-5.99722592120724,3.4625));
#40425=CARTESIAN_POINT('',(222.5,-5.88897274573418,3.4));
#40426=CARTESIAN_POINT('Origin',(222.5,-5.88897274573418,3.4));
#40427=CARTESIAN_POINT('',(227.5,-5.88897274573418,3.4));
#40428=CARTESIAN_POINT('Origin',(227.5,-5.99722592120724,3.4625));
#40429=CARTESIAN_POINT('Origin',(222.5,-5.1618795026618,4.80832611206852));
#40430=CARTESIAN_POINT('',(227.5,-4.80832611206852,4.80832611206852));
#40431=CARTESIAN_POINT('',(227.5,-5.1618795026618,4.80832611206852));
#40432=CARTESIAN_POINT('',(222.5,-4.80832611206852,4.80832611206852));
#40433=CARTESIAN_POINT('',(222.5,-4.80832611206852,4.80832611206852));
#40434=CARTESIAN_POINT('',(222.5,-5.1618795026618,4.80832611206852));
#40435=CARTESIAN_POINT('Origin',(222.5,-4.89671445971684,4.89671445971684));
#40436=CARTESIAN_POINT('',(222.5,-4.80832611206852,4.80832611206852));
#40437=CARTESIAN_POINT('Origin',(222.5,-4.80832611206852,4.80832611206852));
#40438=CARTESIAN_POINT('',(227.5,-4.80832611206852,4.80832611206852));
#40439=CARTESIAN_POINT('Origin',(227.5,-4.89671445971684,4.89671445971684));
#40440=CARTESIAN_POINT('Origin',(222.5,-3.74150635094611,5.98047909668029));
#40441=CARTESIAN_POINT('',(227.5,-3.4,5.88897274573418));
#40442=CARTESIAN_POINT('',(227.5,-3.74150635094611,5.98047909668029));
#40443=CARTESIAN_POINT('',(222.5,-3.4,5.88897274573418));
#40444=CARTESIAN_POINT('',(222.5,-3.4,5.88897274573418));
#40445=CARTESIAN_POINT('',(222.5,-3.74150635094611,5.98047909668029));
#40446=CARTESIAN_POINT('Origin',(222.5,-3.4625,5.99722592120724));
#40447=CARTESIAN_POINT('',(222.5,-3.4,5.88897274573418));
#40448=CARTESIAN_POINT('Origin',(222.5,-3.4,5.88897274573418));
#40449=CARTESIAN_POINT('',(227.5,-3.4,5.88897274573418));
#40450=CARTESIAN_POINT('Origin',(227.5,-3.4625,5.99722592120724));
#40451=CARTESIAN_POINT('Origin',(222.5,-2.06615572454504,6.7450723140623));
#40452=CARTESIAN_POINT('',(227.5,-1.75996950669714,6.56829561876566));
#40453=CARTESIAN_POINT('',(227.5,-2.06615572454504,6.7450723140623));
#40454=CARTESIAN_POINT('',(222.5,-1.75996950669714,6.56829561876566));
#40455=CARTESIAN_POINT('',(222.5,-1.75996950669714,6.56829561876566));
#40456=CARTESIAN_POINT('',(222.5,-2.06615572454504,6.7450723140623));
#40457=CARTESIAN_POINT('Origin',(222.5,-1.79232188733496,6.6890363470518));
#40458=CARTESIAN_POINT('',(222.5,-1.75996950669714,6.56829561876566));
#40459=CARTESIAN_POINT('Origin',(222.5,-1.75996950669714,6.56829561876566));
#40460=CARTESIAN_POINT('',(227.5,-1.75996950669714,6.56829561876566));
#40461=CARTESIAN_POINT('Origin',(227.5,-1.79232188733496,6.6890363470518));
#40462=CARTESIAN_POINT('Origin',(222.5,-0.25,7.05));
#40463=CARTESIAN_POINT('',(222.5,4.163799117101E-16,6.8));
#40464=CARTESIAN_POINT('',(222.5,4.163799117101E-16,6.8));
#40465=CARTESIAN_POINT('',(222.5,-0.25,7.05));
#40466=CARTESIAN_POINT('Origin',(222.5,4.24033954204771E-16,6.925));
#40467=CARTESIAN_POINT('',(222.5,4.163799117101E-16,6.8));
#40468=CARTESIAN_POINT('Origin',(222.5,4.163799117101E-16,6.8));
#40469=CARTESIAN_POINT('Origin',(222.5,1.58319281140051,6.87448183661356));
#40470=CARTESIAN_POINT('',(227.5,1.75996950669714,6.56829561876566));
#40471=CARTESIAN_POINT('',(227.5,1.58319281140051,6.87448183661356));
#40472=CARTESIAN_POINT('',(222.5,1.75996950669714,6.56829561876566));
#40473=CARTESIAN_POINT('',(222.5,1.75996950669714,6.56829561876566));
#40474=CARTESIAN_POINT('',(222.5,1.58319281140051,6.87448183661356));
#40475=CARTESIAN_POINT('Origin',(222.5,1.79232188733496,6.6890363470518));
#40476=CARTESIAN_POINT('',(222.5,1.75996950669714,6.56829561876566));
#40477=CARTESIAN_POINT('Origin',(222.5,1.75996950669714,6.56829561876566));
#40478=CARTESIAN_POINT('',(227.5,1.75996950669714,6.56829561876566));
#40479=CARTESIAN_POINT('Origin',(227.5,1.79232188733496,6.6890363470518));
#40480=CARTESIAN_POINT('Origin',(222.5,3.30849364905389,6.23047909668029));
#40481=CARTESIAN_POINT('',(227.5,3.4,5.88897274573418));
#40482=CARTESIAN_POINT('',(227.5,3.30849364905389,6.23047909668029));
#40483=CARTESIAN_POINT('',(222.5,3.4,5.88897274573418));
#40484=CARTESIAN_POINT('',(222.5,3.4,5.88897274573418));
#40485=CARTESIAN_POINT('',(222.5,3.30849364905389,6.23047909668029));
#40486=CARTESIAN_POINT('Origin',(222.5,3.4625,5.99722592120724));
#40487=CARTESIAN_POINT('',(222.5,3.4,5.88897274573418));
#40488=CARTESIAN_POINT('Origin',(222.5,3.4,5.88897274573418));
#40489=CARTESIAN_POINT('',(227.5,3.4,5.88897274573418));
#40490=CARTESIAN_POINT('Origin',(227.5,3.4625,5.99722592120724));
#40491=CARTESIAN_POINT('Origin',(222.5,4.80832611206852,5.1618795026618));
#40492=CARTESIAN_POINT('',(227.5,4.80832611206852,4.80832611206852));
#40493=CARTESIAN_POINT('',(227.5,4.80832611206852,5.1618795026618));
#40494=CARTESIAN_POINT('',(222.5,4.80832611206852,4.80832611206852));
#40495=CARTESIAN_POINT('',(222.5,4.80832611206852,4.80832611206852));
#40496=CARTESIAN_POINT('',(222.5,4.80832611206852,5.1618795026618));
#40497=CARTESIAN_POINT('Origin',(222.5,4.89671445971684,4.89671445971684));
#40498=CARTESIAN_POINT('',(222.5,4.80832611206852,4.80832611206852));
#40499=CARTESIAN_POINT('Origin',(222.5,4.80832611206852,4.80832611206852));
#40500=CARTESIAN_POINT('',(227.5,4.80832611206852,4.80832611206852));
#40501=CARTESIAN_POINT('Origin',(227.5,4.89671445971684,4.89671445971684));
#40502=CARTESIAN_POINT('Origin',(222.5,5.98047909668029,3.74150635094611));
#40503=CARTESIAN_POINT('',(227.5,5.88897274573418,3.4));
#40504=CARTESIAN_POINT('',(227.5,5.98047909668029,3.74150635094611));
#40505=CARTESIAN_POINT('',(222.5,5.88897274573418,3.4));
#40506=CARTESIAN_POINT('',(222.5,5.88897274573418,3.4));
#40507=CARTESIAN_POINT('',(222.5,5.98047909668029,3.74150635094611));
#40508=CARTESIAN_POINT('Origin',(222.5,5.99722592120724,3.4625));
#40509=CARTESIAN_POINT('',(222.5,5.88897274573418,3.4));
#40510=CARTESIAN_POINT('Origin',(222.5,5.88897274573418,3.4));
#40511=CARTESIAN_POINT('',(227.5,5.88897274573418,3.4));
#40512=CARTESIAN_POINT('Origin',(227.5,5.99722592120724,3.4625));
#40513=CARTESIAN_POINT('Origin',(222.5,6.7450723140623,2.06615572454504));
#40514=CARTESIAN_POINT('',(227.5,6.56829561876566,1.75996950669714));
#40515=CARTESIAN_POINT('',(227.5,6.7450723140623,2.06615572454504));
#40516=CARTESIAN_POINT('',(222.5,6.56829561876566,1.75996950669714));
#40517=CARTESIAN_POINT('',(222.5,6.56829561876566,1.75996950669714));
#40518=CARTESIAN_POINT('',(222.5,6.7450723140623,2.06615572454504));
#40519=CARTESIAN_POINT('Origin',(222.5,6.6890363470518,1.79232188733496));
#40520=CARTESIAN_POINT('',(222.5,6.56829561876566,1.75996950669714));
#40521=CARTESIAN_POINT('Origin',(222.5,6.56829561876566,1.75996950669714));
#40522=CARTESIAN_POINT('',(227.5,6.56829561876566,1.75996950669714));
#40523=CARTESIAN_POINT('Origin',(227.5,6.6890363470518,1.79232188733496));
#40524=CARTESIAN_POINT('Origin',(222.5,7.05,0.25));
#40525=CARTESIAN_POINT('',(227.5,6.8,0.));
#40526=CARTESIAN_POINT('',(227.5,7.05,0.25));
#40527=CARTESIAN_POINT('',(222.5,6.8,0.));
#40528=CARTESIAN_POINT('',(222.5,6.8,0.));
#40529=CARTESIAN_POINT('',(222.5,7.05,0.25));
#40530=CARTESIAN_POINT('Origin',(222.5,6.925,0.));
#40531=CARTESIAN_POINT('',(222.5,6.8,0.));
#40532=CARTESIAN_POINT('Origin',(222.5,6.8,0.));
#40533=CARTESIAN_POINT('',(227.5,6.8,0.));
#40534=CARTESIAN_POINT('Origin',(227.5,6.925,0.));
#40535=CARTESIAN_POINT('Origin',(209.,4.6,0.));
#40536=CARTESIAN_POINT('',(209.,-4.59999999999999,-5.63337527607781E-16));
#40537=CARTESIAN_POINT('Origin',(209.,0.,0.));
#40538=CARTESIAN_POINT('Origin',(209.2,0.,0.));
#40539=CARTESIAN_POINT('',(209.2,-4.8,-5.87830463590729E-16));
#40540=CARTESIAN_POINT('Origin',(215.7,0.,0.));
#40541=CARTESIAN_POINT('Origin',(222.,0.,0.));
#40542=CARTESIAN_POINT('Origin',(222.,6.6,0.));
#40543=CARTESIAN_POINT('',(222.,-6.60000000000001,-8.08266887437254E-16));
#40544=CARTESIAN_POINT('Origin',(222.,0.,0.));
#40545=CARTESIAN_POINT('Origin',(222.2,0.,0.));
#40546=CARTESIAN_POINT('',(222.2,-6.8,-8.327598234202E-16));
#40547=CARTESIAN_POINT('Origin',(227.8,0.,0.));
#45204=UNCERTAINTY_MEASURE_WITH_UNIT(LENGTH_MEASURE(0.01),#45237,
'DISTANCE_ACCURACY_VALUE',
'Maximum model space distance between geometric entities at asserted c
onnectivities');
#45214=UNCERTAINTY_MEASURE_WITH_UNIT(LENGTH_MEASURE(0.01),#45237,
'DISTANCE_ACCURACY_VALUE',
'Maximum model space distance between geometric entities at asserted c
onnectivities');
#45226=(
GEOMETRIC_REPRESENTATION_CONTEXT(3)
GLOBAL_UNCERTAINTY_ASSIGNED_CONTEXT((#45204))
GLOBAL_UNIT_ASSIGNED_CONTEXT((#45237,#45239,#45240))
REPRESENTATION_CONTEXT('','3D')
);
#45236=(
GEOMETRIC_REPRESENTATION_CONTEXT(3)
GLOBAL_UNCERTAINTY_ASSIGNED_CONTEXT((#45214))
GLOBAL_UNIT_ASSIGNED_CONTEXT((#45237,#45239,#45240))
REPRESENTATION_CONTEXT('','3D')
);
#45237=(
LENGTH_UNIT()
NAMED_UNIT(*)
SI_UNIT(.MILLI.,.METRE.)
);
#45239=(
NAMED_UNIT(*)
PLANE_ANGLE_UNIT()
SI_UNIT($,.RADIAN.)
);
#45240=(
NAMED_UNIT(*)
SI_UNIT($,.STERADIAN.)
SOLID_ANGLE_UNIT()
);
#45252=SHAPE_DEFINITION_REPRESENTATION(#45273,#45324);
#45273=PRODUCT_DEFINITION_SHAPE('',$,#45346);
#45324=SHAPE_REPRESENTATION('',(#17342),#45226);
#45334=PRODUCT_DEFINITION_CONTEXT('part definition',#45399,'design');
#45346=PRODUCT_DEFINITION('2026-10-25-23-38-26-935',
'17_Faucet_Oil_Filler_Screw_M10x1',#45367,#45334);
#45367=PRODUCT_DEFINITION_FORMATION('',$,#45412);
#45399=APPLICATION_CONTEXT(
'Core Data for Automotive Mechanical Design Process');
#45400=PRODUCT_CONTEXT('part definition',#45399,'mechanical');
#45412=PRODUCT('2026-10-25-23-38-26-935',
'17_Faucet_Oil_Filler_Screw_M10x1',$,(#45400));
#45485=COLOUR_RGB('Black',0.12,0.14,0.17);
#45486=FILL_AREA_STYLE_COLOUR('',#45485);
#45487=FILL_AREA_STYLE('',(#45486));
#45488=SURFACE_STYLE_FILL_AREA(#45487);
#45489=SURFACE_SIDE_STYLE('',(#45488));
#45490=SURFACE_STYLE_USAGE(.BOTH.,#45489);
#45491=PRESENTATION_STYLE_ASSIGNMENT((#45490));
ENDSEC;
END-ISO-10303-21;
